ISO-10303-21;
HEADER;
FILE_DESCRIPTION (('STEP AP214'),
    '1' );
FILE_NAME ('short pitch roller chain wheel_s_iso_Chain wheel ISO - 20Z 05B-1 --20SA8.0N.step',
    '2026-10-31T03:41:51',
    ( '' ),
    ( '' ),
    'SwSTEP 2.0',
    'SolidWorks 2026',
    '' );
FILE_SCHEMA (( 'AUTOMOTIVE_DESIGN' ));
ENDSEC;

DATA;
#2=CARTESIAN_POINT ( 'NONE',  ( 1.749999999999998002, 19.67366047555530528, 20.02152543075352753 ) ) ;
#3=CARTESIAN_POINT ( 'NONE',  ( 0.000000000000000000, 0.000000000000000000, 0.000000000000000000 ) ) ;
#4=ORIENTED_EDGE ( 'NONE', *, *, #1307, .T. ) ;
#11=EDGE_CURVE ( 'NONE', #14793, #10954, #11402, .T. ) ;
#16=CARTESIAN_POINT ( 'NONE',  ( 0.7592463834391185440, 12.05220173035438513, 24.80264696524887214 ) ) ;
#23=CARTESIAN_POINT ( 'NONE',  ( 2.718184745196084773, 21.92234060054363809, -12.74223776959176568 ) ) ;
#24=CARTESIAN_POINT ( 'NONE',  ( 0.006931054464085539824, -24.42321038836781355, -2.248820353273226491 ) ) ;
#30=ORIENTED_EDGE ( 'NONE', *, *, #9953, .F. ) ;
#32=CARTESIAN_POINT ( 'NONE',  ( 1.039999999999997593, 0.000000000000000000, 0.000000000000000000 ) ) ;
#34=DIRECTION ( 'NONE',  ( -1.000000000000000000, 0.000000000000000000, -0.000000000000000000 ) ) ;
#39=CARTESIAN_POINT ( 'NONE',  ( 0.07186813532171011654, 25.22589920183360945, 2.577209017047096484 ) ) ;
#47=EDGE_CURVE ( 'NONE', #3966, #1296, #12443, .T. ) ;
#59=CARTESIAN_POINT ( 'NONE',  ( 2.257825459230520693, -26.58873630738055738, 4.993157874727710777 ) ) ;
#60=CARTESIAN_POINT ( 'NONE',  ( 0.02436607992776151574, -16.37294372382871188, 18.55949924794887096 ) ) ;
#61=DIRECTION ( 'NONE',  ( 1.000000000000000000, -0.000000000000000000, 0.000000000000000000 ) ) ;
#64=ORIENTED_EDGE ( 'NONE', *, *, #823, .T. ) ;
#68=B_SPLINE_CURVE_WITH_KNOTS ( 'NONE', 3,
 ( #9226, #12751, #12598, #7922 ),
 .UNSPECIFIED., .F., .F.,
 ( 4, 4 ),
 ( 0.005258214619651953650, 0.005948481662034169060 ),
 .UNSPECIFIED. ) ;
#70=DIRECTION ( 'NONE',  ( -1.000000000000000000, 0.000000000000000000, -0.000000000000000000 ) ) ;
#72=ORIENTED_EDGE ( 'NONE', *, *, #10132, .F. ) ;
#73=ORIENTED_EDGE ( 'NONE', *, *, #10146, .F. ) ;
#74=VECTOR ( 'NONE', #9395, 1000.000000000000000 ) ;
#75=CARTESIAN_POINT ( 'NONE',  ( 1.039999999999996705, -20.02152543075359503, 19.67366047555523423 ) ) ;
#78=DIRECTION ( 'NONE',  ( 0.000000000000000000, 0.000000000000000000, 1.000000000000000000 ) ) ;
#79=CIRCLE ( 'NONE', #12614, 2.524999999999995914 ) ;
#85=VERTEX_POINT ( 'NONE', #12565 ) ;
#86=DIRECTION ( 'NONE',  ( -1.000000000000000000, -0.000000000000000000, 0.000000000000000000 ) ) ;
#92=CARTESIAN_POINT ( 'NONE',  ( 0.000000000000000000, 24.34211360614310848, -7.909232158574561744 ) ) ;
#94=LINE ( 'NONE', #4592, #6321 ) ;
#96=DIRECTION ( 'NONE',  ( -1.000000000000000000, 0.000000000000000000, 0.000000000000000000 ) ) ;
#103=LINE ( 'NONE', #14195, #2432 ) ;
#104=AXIS2_PLACEMENT_3D ( 'NONE', #9255, #12995, #7014 ) ;
#106=ORIENTED_EDGE ( 'NONE', *, *, #6088, .F. ) ;
#109=EDGE_CURVE ( 'NONE', #389, #2825, #14096, .T. ) ;
#120=ORIENTED_EDGE ( 'NONE', *, *, #11422, .T. ) ;
#122=CARTESIAN_POINT ( 'NONE',  ( 50.00050000000000239, 0.000000000000000000, 4.000000000000000000 ) ) ;
#124=DIRECTION ( 'NONE',  ( -1.000000000000000000, -0.000000000000000000, -0.000000000000000000 ) ) ;
#129=CIRCLE ( 'NONE', #8981, 24.12539914357697768 ) ;
#133=EDGE_LOOP ( 'NONE', ( #203, #10433, #5275, #14056, #9292, #1957 ) ) ;
#141=CARTESIAN_POINT ( 'NONE',  ( 0.7589665349472735079, 4.828387785248019703, 27.14933624560909919 ) ) ;
#146=EDGE_CURVE ( 'NONE', #14971, #5007, #13767, .T. ) ;
#147=ADVANCED_FACE ( 'NONE', ( #4891 ), #11848, .T. ) ;
#148=CIRCLE ( 'NONE', #8022, 2.524999999999995914 ) ;
#153=EDGE_LOOP ( 'NONE', ( #4267, #3860, #12401, #12111, #6299, #3424, #1299, #11169 ) ) ;
#155=AXIS2_PLACEMENT_3D ( 'NONE', #13835, #4322, #4404 ) ;
#163=EDGE_CURVE ( 'NONE', #12063, #1974, #3422, .T. ) ;
#164=ADVANCED_FACE ( 'NONE', ( #8330 ), #7536, .T. ) ;
#166=FACE_OUTER_BOUND ( 'NONE', #10902, .T. ) ;
#167=AXIS2_PLACEMENT_3D ( 'NONE', #499, #13191, #7439 ) ;
#168=EDGE_LOOP ( 'NONE', ( #13851, #5539, #1139, #30 ) ) ;
#174=ORIENTED_EDGE ( 'NONE', *, *, #12406, .F. ) ;
#175=DIRECTION ( 'NONE',  ( 1.000000000000000000, 0.000000000000000000, 0.000000000000000000 ) ) ;
#183=CARTESIAN_POINT ( 'NONE',  ( -10.00000000000000000, 0.000000000000000000, 0.000000000000000000 ) ) ;
#187=AXIS2_PLACEMENT_3D ( 'NONE', #8087, #3532, #12761 ) ;
#192=CARTESIAN_POINT ( 'NONE',  ( 2.789999999999999147, 22.25075486061738772, 9.324097380959527115 ) ) ;
#197=CARTESIAN_POINT ( 'NONE',  ( 0.02436607992775674525, 9.836394144776026138, -22.71065055754441531 ) ) ;
#198=CARTESIAN_POINT ( 'NONE',  ( 2.789999999999999147, 1.991882183130632589, -24.04302995059963877 ) ) ;
#203=ORIENTED_EDGE ( 'NONE', *, *, #12220, .F. ) ;
#206=ORIENTED_EDGE ( 'NONE', *, *, #5456, .T. ) ;
#215=ORIENTED_EDGE ( 'NONE', *, *, #3281, .T. ) ;
#217=LINE ( 'NONE', #14226, #7341 ) ;
#221=LINE ( 'NONE', #525, #10167 ) ;
#223=ORIENTED_EDGE ( 'NONE', *, *, #14809, .T. ) ;
#227=EDGE_CURVE ( 'NONE', #9499, #4705, #4811, .T. ) ;
#229=CYLINDRICAL_SURFACE ( 'NONE', #11421, 13.19999999999999929 ) ;
#230=DIRECTION ( 'NONE',  ( 0.000000000000000000, 0.000000000000000000, 1.000000000000000000 ) ) ;
#231=ORIENTED_EDGE ( 'NONE', *, *, #8908, .F. ) ;
#232=ORIENTED_EDGE ( 'NONE', *, *, #7399, .F. ) ;
#235=ORIENTED_EDGE ( 'NONE', *, *, #9615, .F. ) ;
#245=EDGE_LOOP ( 'NONE', ( #3924, #9701, #3037, #7641 ) ) ;
#248=ORIENTED_EDGE ( 'NONE', *, *, #1307, .F. ) ;
#249=EDGE_CURVE ( 'NONE', #5007, #12521, #11742, .T. ) ;
#251=DIRECTION ( 'NONE',  ( -1.000000000000000000, 0.000000000000000000, -0.000000000000000000 ) ) ;
#254=CARTESIAN_POINT ( 'NONE',  ( 0.07181525696555157712, 5.344212458769712626, -24.78695292654915860 ) ) ;
#255=LINE ( 'NONE', #4972, #14719 ) ;
#259=EDGE_LOOP ( 'NONE', ( #3282, #14256 ) ) ;
#260=DIRECTION ( 'NONE',  ( 0.000000000000000000, 0.000000000000000000, -1.000000000000000000 ) ) ;
#268=B_SPLINE_CURVE_WITH_KNOTS ( 'NONE', 3,
 ( #6737, #12274, #4444, #11193 ),
 .UNSPECIFIED., .F., .F.,
 ( 4, 4 ),
 ( 0.005258120783916825358, 0.005948386350302978416 ),
 .UNSPECIFIED. ) ;
#269=VERTEX_POINT ( 'NONE', #10859 ) ;
#270=CARTESIAN_POINT ( 'NONE',  ( 2.789999999999999147, -24.04302995059964587, -1.991882183130548878 ) ) ;
#273=CARTESIAN_POINT ( 'NONE',  ( 1.749999999999998002, -27.68468304288262516, 4.633866840648810381 ) ) ;
#277=CYLINDRICAL_SURFACE ( 'NONE', #11037, 13.19999999999999574 ) ;
#286=ORIENTED_EDGE ( 'NONE', *, *, #13802, .T. ) ;
#295=CARTESIAN_POINT ( 'NONE',  ( 0.000000000000000000, -8.936381166381891568E-14, 25.59481291497571220 ) ) ;
#297=EDGE_CURVE ( 'NONE', #1055, #15218, #8747, .T. ) ;
#301=CIRCLE ( 'NONE', #10863, 28.06981291497571362 ) ;
#302=ORIENTED_EDGE ( 'NONE', *, *, #9017, .F. ) ;
#305=CYLINDRICAL_SURFACE ( 'NONE', #14089, 28.06981291497571362 ) ;
#306=ADVANCED_FACE ( 'NONE', ( #9862 ), #2790, .F. ) ;
#311=ORIENTED_EDGE ( 'NONE', *, *, #14820, .T. ) ;
#313=EDGE_CURVE ( 'NONE', #13918, #6218, #8504, .T. ) ;
#315=CARTESIAN_POINT ( 'NONE',  ( 2.789999999999999147, 15.74360496233381390, 18.28042085475283685 ) ) ;
#316=VERTEX_POINT ( 'NONE', #2870 ) ;
#317=CARTESIAN_POINT ( 'NONE',  ( 0.5279273381794611364, 3.461047254864636713, -26.82026385750174668 ) ) ;
#318=CARTESIAN_POINT ( 'NONE',  ( 2.789999999999999147, 20.70663861606272249, 15.04425356660767932 ) ) ;
#321=EDGE_CURVE ( 'NONE', #3392, #9499, #13955, .T. ) ;
#322=CARTESIAN_POINT ( 'NONE',  ( 0.1855656748306453718, 25.77772010606605946, 2.851997810081739360 ) ) ;
#325=DIRECTION ( 'NONE',  ( -1.000000000000000000, -0.000000000000000000, -0.000000000000000000 ) ) ;
#331=EDGE_CURVE ( 'NONE', #13647, #13720, #7540, .T. ) ;
#333=TOROIDAL_SURFACE ( 'NONE', #14843, 24.12539914357697768, 8.000000000000000000 ) ;
#336=AXIS2_PLACEMENT_3D ( 'NONE', #12347, #8023, #13657 ) ;
#338=CARTESIAN_POINT ( 'NONE',  ( 0.0003207540509381473352, -20.70663861606275447, -12.51925356660783528 ) ) ;
#339=CARTESIAN_POINT ( 'NONE',  ( 2.790000000000000480, -18.34424029220122776, 15.96500990068118497 ) ) ;
#345=ADVANCED_FACE ( 'NONE', ( #14325 ), #11163, .T. ) ;
#346=AXIS2_PLACEMENT_3D ( 'NONE', #7761, #8835, #8986 ) ;
#347=ORIENTED_EDGE ( 'NONE', *, *, #9380, .F. ) ;
#350=CARTESIAN_POINT ( 'NONE',  ( 5.139549990269394683E-16, -2.133490293297187979, 24.22479935914660132 ) ) ;
#352=DIRECTION ( 'NONE',  ( -1.000000000000000000, 0.000000000000000000, 0.000000000000000000 ) ) ;
#364=EDGE_CURVE ( 'NONE', #6867, #6366, #11210, .T. ) ;
#366=CARTESIAN_POINT ( 'NONE',  ( 0.02436607992776541887, 12.59161484032942901, -21.30679549418617924 ) ) ;
#368=VERTEX_POINT ( 'NONE', #2951 ) ;
#375=DIRECTION ( 'NONE',  ( 0.000000000000000000, 0.000000000000000000, 1.000000000000000000 ) ) ;
#376=EDGE_CURVE ( 'NONE', #14085, #567, #7640, .T. ) ;
#379=CARTESIAN_POINT ( 'NONE',  ( -7.595268335593441642E-14, -22.38018801136484015, 9.515416771311118183 ) ) ;
#382=ORIENTED_EDGE ( 'NONE', *, *, #13166, .T. ) ;
#383=VERTEX_POINT ( 'NONE', #7122 ) ;
#384=DIRECTION ( 'NONE',  ( 0.000000000000000000, 0.000000000000000000, 1.000000000000000000 ) ) ;
#389=VERTEX_POINT ( 'NONE', #11725 ) ;
#390=CIRCLE ( 'NONE', #4832, 2.524999999999996358 ) ;
#392=LINE ( 'NONE', #9787, #6528 ) ;
#394=CARTESIAN_POINT ( 'NONE',  ( 0.000000000000000000, -15.04425356660744839, -18.18163861606288378 ) ) ;
#396=CARTESIAN_POINT ( 'NONE',  ( 0.000000000000000000, 7.909232158575156824, -21.81711360614291806 ) ) ;
#398=CARTESIAN_POINT ( 'NONE',  ( 1.039999999999995595, 4.147968289691676524, -27.76164181293047051 ) ) ;
#400=CARTESIAN_POINT ( 'NONE',  ( 0.7589665326895891351, 12.98167595241022276, 24.32849926382755257 ) ) ;
#405=ORIENTED_EDGE ( 'NONE', *, *, #2597, .T. ) ;
#408=CARTESIAN_POINT ( 'NONE',  ( 1.749999999999998002, 4.633866840648922292, 27.68468304288260384 ) ) ;
#410=CARTESIAN_POINT ( 'NONE',  ( 2.789999999999999147, -14.55412442567604003, -19.64056340710890325 ) ) ;
#411=ORIENTED_EDGE ( 'NONE', *, *, #420, .T. ) ;
#420=EDGE_CURVE ( 'NONE', #2610, #7436, #6553, .T. ) ;
#423=DIRECTION ( 'NONE',  ( 0.000000000000000000, 0.000000000000000000, 1.000000000000000000 ) ) ;
#431=FACE_OUTER_BOUND ( 'NONE', #11888, .T. ) ;
#432=CARTESIAN_POINT ( 'NONE',  ( 2.262072637928881580, 12.96450951081251191, -23.73240184472483350 ) ) ;
#434=EDGE_CURVE ( 'NONE', #952, #7149, #14309, .T. ) ;
#439=VECTOR ( 'NONE', #10989, 1000.000000000000000 ) ;
#440=CARTESIAN_POINT ( 'NONE',  ( 1.749999999999998002, -24.89775460606821866, -12.96210679857815684 ) ) ;
#441=ORIENTED_EDGE ( 'NONE', *, *, #8796, .T. ) ;
#442=AXIS2_PLACEMENT_3D ( 'NONE', #13011, #2427, #5893 ) ;
#446=VERTEX_POINT ( 'NONE', #11865 ) ;
#447=VERTEX_POINT ( 'NONE', #12796 ) ;
#450=CARTESIAN_POINT ( 'NONE',  ( 0.6102186610125081012, 23.94322454545469370, 12.96989951879415770 ) ) ;
#456=CARTESIAN_POINT ( 'NONE',  ( 2.262072706628475149, 19.66369668717060293, -18.56460150496918260 ) ) ;
#457=CIRCLE ( 'NONE', #14962, 24.12539914357697413 ) ;
#458=CIRCLE ( 'NONE', #14217, 28.06981291497571362 ) ;
#461=ORIENTED_EDGE ( 'NONE', *, *, #12360, .F. ) ;
#462=CARTESIAN_POINT ( 'NONE',  ( 0.000000000000000000, 0.000000000000000000, 0.000000000000000000 ) ) ;
#467=CIRCLE ( 'NONE', #9076, 28.06981291497571362 ) ;
#469=B_SPLINE_CURVE_WITH_KNOTS ( 'NONE', 3,
 ( #4535, #14047, #3516, #14126, #2370, #7062 ),
 .UNSPECIFIED., .F., .F.,
 ( 4, 2, 4 ),
 ( 4.462636682232942879E-07, 0.001879885020955589887, 0.003759323778242956802 ),
 .UNSPECIFIED. ) ;
#471=B_SPLINE_CURVE_WITH_KNOTS ( 'NONE', 3,
 ( #9307, #4845, #14216, #12817 ),
 .UNSPECIFIED., .F., .F.,
 ( 4, 4 ),
 ( 0.005258139959819249469, 0.005948405594583416715 ),
 .UNSPECIFIED. ) ;
#473=ORIENTED_EDGE ( 'NONE', *, *, #8532, .T. ) ;
#474=CARTESIAN_POINT ( 'NONE',  ( 0.02436607992776628623, 24.63872515616082737, -2.336989772644355590 ) ) ;
#475=DIRECTION ( 'NONE',  ( 1.000000000000000000, 0.000000000000000000, 0.000000000000000000 ) ) ;
#483=DIRECTION ( 'NONE',  ( -1.000000000000000000, 0.000000000000000000, 0.000000000000000000 ) ) ;
#492=B_SPLINE_CURVE_WITH_KNOTS ( 'NONE', 3,
 ( #6585, #14735, #5589, #12414, #5439, #11333 ),
 .UNSPECIFIED., .F., .F.,
 ( 4, 2, 4 ),
 ( 2.321268216996885854E-07, 0.001878622960950492504, 0.003757013795079285415 ),
 .UNSPECIFIED. ) ;
#494=CARTESIAN_POINT ( 'NONE',  ( 2.789999999999999147, -7.909232158574647009, -24.34211360614308006 ) ) ;
#495=VERTEX_POINT ( 'NONE', #11574 ) ;
#499=CARTESIAN_POINT ( 'NONE',  ( 8.000000000000000000, 0.000000000000000000, 0.000000000000000000 ) ) ;
#502=CARTESIAN_POINT ( 'NONE',  ( 2.789999999999999147, -7.772527002114268058, -23.17675759782048672 ) ) ;
#505=EDGE_CURVE ( 'NONE', #1110, #13796, #457, .T. ) ;
#512=CARTESIAN_POINT ( 'NONE',  ( 2.179781338987520467, -23.94322454545470436, 12.96989951879399072 ) ) ;
#520=EDGE_CURVE ( 'NONE', #3390, #5744, #103, .T. ) ;
#521=ADVANCED_FACE ( 'NONE', ( #12728 ), #10775, .T. ) ;
#522=B_SPLINE_CURVE_WITH_KNOTS ( 'NONE', 3,
 ( #4119, #4034, #8795, #7354, #2800, #7502 ),
 .UNSPECIFIED., .F., .F.,
 ( 4, 2, 4 ),
 ( 1.979325885420663221E-07, 0.001878588715165609505, 0.003756979497742676637 ),
 .UNSPECIFIED. ) ;
#523=CYLINDRICAL_SURFACE ( 'NONE', #12954, 13.20000000000000107 ) ;
#524=DIRECTION ( 'NONE',  ( -1.000000000000000000, -0.000000000000000000, -0.000000000000000000 ) ) ;
#525=CARTESIAN_POINT ( 'NONE',  ( 1.394999999999999574, -4.147968289691484678, 27.76164181293050603 ) ) ;
#526=VECTOR ( 'NONE', #5455, 1000.000000000000000 ) ;
#529=CARTESIAN_POINT ( 'NONE',  ( -5.209999999999999964, 0.000000000000000000, 0.000000000000000000 ) ) ;
#537=ORIENTED_EDGE ( 'NONE', *, *, #12943, .T. ) ;
#543=CYLINDRICAL_SURFACE ( 'NONE', #2690, 2.524999999999996358 ) ;
#549=CARTESIAN_POINT ( 'NONE',  ( 0.000000000000000000, 9.324097380959415204, 22.25075486061743391 ) ) ;
#551=CARTESIAN_POINT ( 'NONE',  ( 0.000000000000000000, 9.324097380959777581, -22.25075486061729535 ) ) ;
#552=VERTEX_POINT ( 'NONE', #6420 ) ;
#557=CARTESIAN_POINT ( 'NONE',  ( 2.718131914667133220, -10.24630254990500511, -23.19485392143224445 ) ) ;
#559=CARTESIAN_POINT ( 'NONE',  ( 1.039999999999996039, 27.68468304288258963, 4.633866840649018215 ) ) ;
#560=ADVANCED_FACE ( 'NONE', ( #7432 ), #3730, .T. ) ;
#561=CARTESIAN_POINT ( 'NONE',  ( 2.765633920072238183, -18.55949924794904504, 16.37294372382852004 ) ) ;
#565=DIRECTION ( 'NONE',  ( -1.000000000000000000, 0.000000000000000000, 0.000000000000000000 ) ) ;
#567=VERTEX_POINT ( 'NONE', #338 ) ;
#569=PRODUCT_DEFINITION_FORMATION_WITH_SPECIFIED_SOURCE ( 'ANY', '', #11166, .NOT_KNOWN. ) ;
#570=ORIENTED_EDGE ( 'NONE', *, *, #3691, .F. ) ;
#572=CARTESIAN_POINT ( 'NONE',  ( 0.1882239034349769691, -22.54313264455003463, -12.84621645676869939 ) ) ;
#573=CARTESIAN_POINT ( 'NONE',  ( 1.039999999999996483, -19.67366047555544384, 20.02152543075338897 ) ) ;
#575=B_SPLINE_CURVE_WITH_KNOTS ( 'NONE', 3,
 ( #11221, #14616, #14475, #6311 ),
 .UNSPECIFIED., .F., .F.,
 ( 4, 4 ),
 ( 0.005258214619651938905, 0.005948481662034165590 ),
 .UNSPECIFIED. ) ;
#576=AXIS2_PLACEMENT_3D ( 'NONE', #8107, #2415, #2263 ) ;
#583=DIRECTION ( 'NONE',  ( -1.000000000000000000, 0.000000000000000000, 0.000000000000000000 ) ) ;
#586=FACE_OUTER_BOUND ( 'NONE', #1000, .T. ) ;
#587=CIRCLE ( 'NONE', #5034, 28.06981291497571007 ) ;
#589=EDGE_CURVE ( 'NONE', #6696, #11628, #955, .T. ) ;
#595=CARTESIAN_POINT ( 'NONE',  ( 0.000000000000000000, 0.000000000000000000, 0.000000000000000000 ) ) ;
#597=ORIENTED_EDGE ( 'NONE', *, *, #7976, .F. ) ;
#601=CARTESIAN_POINT ( 'NONE',  ( 0.5321745326902582729, -3.467596033028097935, -26.83036154824997510 ) ) ;
#603=AXIS2_PLACEMENT_3D ( 'NONE', #6035, #9572, #1266 ) ;
#604=AXIS2_PLACEMENT_3D ( 'NONE', #13155, #1321, #10708 ) ;
#607=ORIENTED_EDGE ( 'NONE', *, *, #4698, .T. ) ;
#608=CARTESIAN_POINT ( 'NONE',  ( 2.789999999999999147, -1.991882183130462503, 24.04302995059964942 ) ) ;
#612=EDGE_CURVE ( 'NONE', #9447, #14273, #3176, .T. ) ;
#615=CIRCLE ( 'NONE', #1363, 2.524999999999996358 ) ;
#616=( GEOMETRIC_REPRESENTATION_CONTEXT ( 3 ) GLOBAL_UNCERTAINTY_ASSIGNED_CONTEXT ( ( #15080 ) ) GLOBAL_UNIT_ASSIGNED_CONTEXT ( ( #11232, #1944, #14708 ) ) REPRESENTATION_CONTEXT ( 'NONE', 'WORKASPACE' ) );
#622=EDGE_CURVE ( 'NONE', #7127, #13976, #12098, .T. ) ;
#623=FACE_OUTER_BOUND ( 'NONE', #13605, .T. ) ;
#626=VERTEX_POINT ( 'NONE', #4045 ) ;
#629=EDGE_CURVE ( 'NONE', #5767, #14821, #3491, .T. ) ;
#632=DIRECTION ( 'NONE',  ( -1.000000000000000000, -0.000000000000000000, -0.000000000000000000 ) ) ;
#633=CARTESIAN_POINT ( 'NONE',  ( 0.1882238946918236844, 2.857713464478689680, 25.78859396478529220 ) ) ;
#634=CARTESIAN_POINT ( 'NONE',  ( 2.789999999999999147, -7.334849878007672963, 23.31896751603329676 ) ) ;
#637=TOROIDAL_SURFACE ( 'NONE', #8487, 24.12539914357697413, 8.000000000000000000 ) ;
#638=CARTESIAN_POINT ( 'NONE',  ( 0.5321745407694743468, -26.58873630738047922, -4.993157874728098022 ) ) ;
#640=ORIENTED_EDGE ( 'NONE', *, *, #10463, .F. ) ;
#642=DIRECTION ( 'NONE',  ( 0.000000000000000000, 0.000000000000000000, 1.000000000000000000 ) ) ;
#644=CARTESIAN_POINT ( 'NONE',  ( 2.789999999999999147, 19.64056340710875048, 14.55412442567624609 ) ) ;
#645=ADVANCED_FACE ( 'NONE', ( #2669 ), #12027, .F. ) ;
#646=EDGE_CURVE ( 'NONE', #8930, #9867, #6269, .T. ) ;
#649=AXIS2_PLACEMENT_3D ( 'NONE', #720, #6335, #5200 ) ;
#655=AXIS2_PLACEMENT_3D ( 'NONE', #13246, #8630, #13392 ) ;
#658=ORIENTED_EDGE ( 'NONE', *, *, #9106, .F. ) ;
#659=ORIENTED_EDGE ( 'NONE', *, *, #7931, .T. ) ;
#663=CARTESIAN_POINT ( 'NONE',  ( 0.5321745227542320489, -18.57583492944406700, -19.66801664102725056 ) ) ;
#668=DIRECTION ( 'NONE',  ( -1.000000000000000000, 0.000000000000000000, -0.000000000000000000 ) ) ;
#671=DIRECTION ( 'NONE',  ( 0.000000000000000000, 0.000000000000000000, 1.000000000000000000 ) ) ;
#672=VERTEX_POINT ( 'NONE', #7141 ) ;
#673=CARTESIAN_POINT ( 'NONE',  ( 2.789999999999999147, 21.30679549418649543, -12.59161484032888723 ) ) ;
#689=CARTESIAN_POINT ( 'NONE',  ( 0.02436607992776238310, -2.336989772644097574, -24.63872515616085224 ) ) ;
#690=CARTESIAN_POINT ( 'NONE',  ( 0.000000000000000000, 24.04302995059966719, 1.991882183130389228 ) ) ;
#691=CIRCLE ( 'NONE', #2900, 24.12539914357697768 ) ;
#696=CARTESIAN_POINT ( 'NONE',  ( 0.02436607992776455150, -22.71065055754459650, 9.836394144775621129 ) ) ;
#698=AXIS2_PLACEMENT_3D ( 'NONE', #11572, #5829, #3434 ) ;
#701=SURFACE_SIDE_STYLE ('',( #2164 ) ) ;
#702=ORIENTED_EDGE ( 'NONE', *, *, #8327, .F. ) ;
#704=ORIENTED_EDGE ( 'NONE', *, *, #12281, .T. ) ;
#705=DIRECTION ( 'NONE',  ( -1.000000000000000000, 0.000000000000000000, -0.000000000000000000 ) ) ;
#706=CARTESIAN_POINT ( 'NONE',  ( 2.030753610301994083, 19.12676442129372134, -19.86438386685639657 ) ) ;
#709=CARTESIAN_POINT ( 'NONE',  ( 2.789999999999999147, -9.836394144775550075, -22.71065055754462492 ) ) ;
#711=EDGE_CURVE ( 'NONE', #10374, #7184, #4924, .T. ) ;
#712=ORIENTED_EDGE ( 'NONE', *, *, #3705, .T. ) ;
#719=ORIENTED_EDGE ( 'NONE', *, *, #1592, .F. ) ;
#720=CARTESIAN_POINT ( 'NONE',  ( 0.000000000000000000, 0.000000000000000000, 0.000000000000000000 ) ) ;
#722=ORIENTED_EDGE ( 'NONE', *, *, #3716, .F. ) ;
#730=AXIS2_PLACEMENT_3D ( 'NONE', #2087, #9008, #2245 ) ;
#732=B_SPLINE_CURVE_WITH_KNOTS ( 'NONE', 3,
 ( #13639, #6799, #14655, #14965, #5506, #14801 ),
 .UNSPECIFIED., .F., .F.,
 ( 4, 2, 4 ),
 ( 2.321268216996908089E-07, 0.001878622960950487733, 0.003757013795079275874 ),
 .UNSPECIFIED. ) ;
#733=FACE_OUTER_BOUND ( 'NONE', #168, .T. ) ;
#738=DIRECTION ( 'NONE',  ( 0.000000000000000000, 0.000000000000000000, 1.000000000000000000 ) ) ;
#741=AXIS2_PLACEMENT_3D ( 'NONE', #2504, #7190, #11721 ) ;
#742=EDGE_CURVE ( 'NONE', #7471, #6879, #3519, .T. ) ;
#745=FACE_OUTER_BOUND ( 'NONE', #3548, .T. ) ;
#748=CARTESIAN_POINT ( 'NONE',  ( 2.789999999999999147, -24.34211360614305875, 7.909232158574721616 ) ) ;
#751=DIRECTION ( 'NONE',  ( 0.000000000000000000, 0.000000000000000000, 1.000000000000000000 ) ) ;
#755=DIRECTION ( 'NONE',  ( -1.000000000000000000, 0.000000000000000000, 0.000000000000000000 ) ) ;
#759=FACE_OUTER_BOUND ( 'NONE', #2011, .T. ) ;
#763=CYLINDRICAL_SURFACE ( 'NONE', #4849, 28.06981291497571362 ) ;
#764=FACE_OUTER_BOUND ( 'NONE', #9154, .T. ) ;
#766=DIRECTION ( 'NONE',  ( 0.000000000000000000, 1.374038396813314756E-15, -1.000000000000000000 ) ) ;
#767=DIRECTION ( 'NONE',  ( -1.000000000000000000, -0.000000000000000000, -0.000000000000000000 ) ) ;
#770=ORIENTED_EDGE ( 'NONE', *, *, #10353, .F. ) ;
#771=CARTESIAN_POINT ( 'NONE',  ( -7.755480735455585059E-14, 24.22524813288762502, -2.133839912090887303 ) ) ;
#773=ORIENTED_EDGE ( 'NONE', *, *, #13006, .T. ) ;
#775=ORIENTED_EDGE ( 'NONE', *, *, #109, .T. ) ;
#780=LINE ( 'NONE', #13773, #10301 ) ;
#781=ORIENTED_EDGE ( 'NONE', *, *, #7792, .F. ) ;
#787=ADVANCED_FACE ( 'NONE', ( #11592 ), #14342, .T. ) ;
#789=CARTESIAN_POINT ( 'NONE',  ( 2.789999999999999147, 2.680914349914567470E-13, -25.59481291497571220 ) ) ;
#793=ORIENTED_EDGE ( 'NONE', *, *, #2254, .F. ) ;
#795=EDGE_CURVE ( 'NONE', #10796, #2610, #10470, .T. ) ;
#796=CARTESIAN_POINT ( 'NONE',  ( 0.02436607992776151574, -16.37294372382871188, 18.55949924794887096 ) ) ;
#801=CARTESIAN_POINT ( 'NONE',  ( 0.000000000000000000, 15.74360496233383522, 18.28042085475283329 ) ) ;
#802=ORIENTED_EDGE ( 'NONE', *, *, #10049, .T. ) ;
#803=CARTESIAN_POINT ( 'NONE',  ( 2.601776096565022289, 12.84621645676845070, 22.54313264455018384 ) ) ;
#804=EDGE_CURVE ( 'NONE', #11628, #8517, #3296, .T. ) ;
#806=ORIENTED_EDGE ( 'NONE', *, *, #13764, .F. ) ;
#807=VERTEX_POINT ( 'NONE', #12276 ) ;
#808=ORIENTED_EDGE ( 'NONE', *, *, #12374, .T. ) ;
#810=CARTESIAN_POINT ( 'NONE',  ( 2.789999999999999147, -14.55412442567631537, 19.64056340710869719 ) ) ;
#811=ADVANCED_FACE ( 'NONE', ( #2827 ), #9663, .F. ) ;
#815=CARTESIAN_POINT ( 'NONE',  ( 2.789999999999999147, 20.70663861606293210, -15.04425356660737556 ) ) ;
#816=CARTESIAN_POINT ( 'NONE',  ( 0.000000000000000000, -15.74360496233395956, 18.28042085475273026 ) ) ;
#817=EDGE_CURVE ( 'NONE', #7184, #9117, #7348, .T. ) ;
#821=LINE ( 'NONE', #8895, #898 ) ;
#823=EDGE_CURVE ( 'NONE', #14366, #10930, #6243, .T. ) ;
#826=B_SPLINE_CURVE_WITH_KNOTS ( 'NONE', 3,
 ( #8174, #2337, #1325, #5806 ),
 .UNSPECIFIED., .F., .F.,
 ( 4, 4 ),
 ( 0.005258214619651955385, 0.005948481662034169927 ),
 .UNSPECIFIED. ) ;
#832=DIRECTION ( 'NONE',  ( -1.000000000000000000, 0.000000000000000000, 0.000000000000000000 ) ) ;
#835=CARTESIAN_POINT ( 'NONE',  ( 2.031033465052725084, -4.828387785248216879, 27.14933624560906367 ) ) ;
#839=CARTESIAN_POINT ( 'NONE',  ( 2.765633920072236407, 2.336989772644613161, -24.63872515616080250 ) ) ;
#842=EDGE_CURVE ( 'NONE', #85, #7278, #10281, .T. ) ;
#847=CARTESIAN_POINT ( 'NONE',  ( 8.000000000000000000, 0.000000000000000000, 0.000000000000000000 ) ) ;
#848=ADVANCED_FACE ( 'NONE', ( #7599 ), #15085, .T. ) ;
#850=ORIENTED_EDGE ( 'NONE', *, *, #1681, .T. ) ;
#852=VERTEX_POINT ( 'NONE', #6139 ) ;
#856=CARTESIAN_POINT ( 'NONE',  ( 0.02436607992775544421, -22.71065055754445439, -9.836394144775947979 ) ) ;
#858=TOROIDAL_SURFACE ( 'NONE', #3786, 24.12539914357697413, 8.000000000000000000 ) ;
#859=LINE ( 'NONE', #13924, #966 ) ;
#860=VERTEX_POINT ( 'NONE', #8511 ) ;
#866=CARTESIAN_POINT ( 'NONE',  ( 0.1570303611602991700, -22.37100459959352605, 12.81671916049007365 ) ) ;
#869=CARTESIAN_POINT ( 'NONE',  ( 0.02436607992775978102, -12.59161484032896361, -21.30679549418645280 ) ) ;
#875=CYLINDRICAL_SURFACE ( 'NONE', #11476, 13.19999999999999929 ) ;
#876=EDGE_CURVE ( 'NONE', #4522, #1158, #13844, .T. ) ;
#879=CARTESIAN_POINT ( 'NONE',  ( 2.789999999999999147, -24.34211360614305875, 7.909232158574721616 ) ) ;
#886=CARTESIAN_POINT ( 'NONE',  ( 2.789999999999999147, 24.04302995059966364, -1.991882183130384121 ) ) ;
#887=DIRECTION ( 'NONE',  ( -1.000000000000000000, -0.000000000000000000, -0.000000000000000000 ) ) ;
#888=CARTESIAN_POINT ( 'NONE',  ( 0.8291131470075423504, 24.44424927289185945, 12.96989951879416125 ) ) ;
#892=CARTESIAN_POINT ( 'NONE',  ( 2.789679245949058917, 20.70663861606308487, -12.51925356660738053 ) ) ;
#895=DIRECTION ( 'NONE',  ( -1.000000000000000000, -0.000000000000000000, -0.000000000000000000 ) ) ;
#896=CARTESIAN_POINT ( 'NONE',  ( 1.394999999999999574, 4.633866840649313090, -27.68468304288253989 ) ) ;
#898=VECTOR ( 'NONE', #12581, 1000.000000000000000 ) ;
#899=CIRCLE ( 'NONE', #10472, 24.12539914357697413 ) ;
#902=DIRECTION ( 'NONE',  ( -1.000000000000000000, -0.000000000000000000, -0.000000000000000000 ) ) ;
#906=EDGE_LOOP ( 'NONE', ( #12011, #939, #11934, #6137, #14725, #5584 ) ) ;
#908=DIRECTION ( 'NONE',  ( 0.000000000000000000, 0.000000000000000000, 1.000000000000000000 ) ) ;
#909=LINE ( 'NONE', #10292, #5851 ) ;
#910=VERTEX_POINT ( 'NONE', #9890 ) ;
#912=DIRECTION ( 'NONE',  ( -1.000000000000000000, -0.000000000000000000, -0.000000000000000000 ) ) ;
#916=AXIS2_PLACEMENT_3D ( 'NONE', #8393, #86, #2266 ) ;
#917=ADVANCED_FACE ( 'NONE', ( #15187 ), #1318, .T. ) ;
#918=CARTESIAN_POINT ( 'NONE',  ( 0.1855657168891864939, -12.84444904262008436, -22.53097606932998787 ) ) ;
#920=ORIENTED_EDGE ( 'NONE', *, *, #6461, .F. ) ;
#922=CIRCLE ( 'NONE', #14681, 24.12539914357697768 ) ;
#925=ORIENTED_EDGE ( 'NONE', *, *, #3499, .F. ) ;
#929=VERTEX_POINT ( 'NONE', #11555 ) ;
#930=ADVANCED_FACE ( 'NONE', ( #12777 ), #3415, .T. ) ;
#934=CIRCLE ( 'NONE', #4638, 28.06981291497571362 ) ;
#938=CARTESIAN_POINT ( 'NONE',  ( 2.604434283110813375, -12.84444904262041121, 22.53097606932980312 ) ) ;
#939=ORIENTED_EDGE ( 'NONE', *, *, #14144, .F. ) ;
#949=VERTEX_POINT ( 'NONE', #7667 ) ;
#952=VERTEX_POINT ( 'NONE', #6947 ) ;
#955=CIRCLE ( 'NONE', #5146, 2.524999999999995470 ) ;
#956=AXIS2_PLACEMENT_3D ( 'NONE', #3416, #10487, #78 ) ;
#959=CARTESIAN_POINT ( 'NONE',  ( -5.209999999999999964, 0.000000000000000000, 0.000000000000000000 ) ) ;
#963=EDGE_LOOP ( 'NONE', ( #14010, #3340, #770, #13005 ) ) ;
#965=CARTESIAN_POINT ( 'NONE',  ( 2.262072661820536901, 3.461047254864260125, 26.82026385750179287 ) ) ;
#966=VECTOR ( 'NONE', #4326, 1000.000000000000000 ) ;
#973=CARTESIAN_POINT ( 'NONE',  ( 2.718131864678288601, -25.22589920183363432, 2.577209017046923289 ) ) ;
#984=ORIENTED_EDGE ( 'NONE', *, *, #4943, .F. ) ;
#986=CARTESIAN_POINT ( 'NONE',  ( 1.394999999999999574, 20.02152543075346003, 19.67366047555537634 ) ) ;
#987=EDGE_CURVE ( 'NONE', #4130, #12548, #3711, .T. ) ;
#989=CARTESIAN_POINT ( 'NONE',  ( 2.262072625383133140, -4.996265754456554298, 26.57710921259759829 ) ) ;
#990=CARTESIAN_POINT ( 'NONE',  ( 0.006930995026450116094, -5.408431875071277872, -23.92277630352801054 ) ) ;
#996=ORIENTED_EDGE ( 'NONE', *, *, #9649, .F. ) ;
#997=CARTESIAN_POINT ( 'NONE',  ( 0.02436607992775978102, 24.63872515616082737, 2.336989772644355146 ) ) ;
#999=DIRECTION ( 'NONE',  ( -1.000000000000000000, -0.000000000000000000, -0.000000000000000000 ) ) ;
#1000=EDGE_LOOP ( 'NONE', ( #10311, #6178, #2088, #10360 ) ) ;
#1005=ORIENTED_EDGE ( 'NONE', *, *, #4117, .F. ) ;
#1008=CARTESIAN_POINT ( 'NONE',  ( 1.394999999999999574, -19.67366047555544739, 20.02152543075338897 ) ) ;
#1011=CYLINDRICAL_SURFACE ( 'NONE', #187, 13.19999999999999929 ) ;
#1015=DIRECTION ( 'NONE',  ( 0.000000000000000000, -1.374038396813314756E-15, -1.000000000000000000 ) ) ;
#1016=ADVANCED_FACE ( 'NONE', ( #8104 ), #8886, .T. ) ;
#1018=CARTESIAN_POINT ( 'NONE',  ( 2.765633920072238627, 5.391175441198956086, -24.15498966839956907 ) ) ;
#1026=ORIENTED_EDGE ( 'NONE', *, *, #9932, .T. ) ;
#1027=DIRECTION ( 'NONE',  ( 0.000000000000000000, 0.000000000000000000, 1.000000000000000000 ) ) ;
#1029=ORIENTED_EDGE ( 'NONE', *, *, #3499, .T. ) ;
#1037=DIRECTION ( 'NONE',  ( -1.000000000000000000, 0.000000000000000000, 0.000000000000000000 ) ) ;
#1038=ORIENTED_EDGE ( 'NONE', *, *, #13176, .T. ) ;
#1039=AXIS2_PLACEMENT_3D ( 'NONE', #11466, #13547, #2022 ) ;
#1040=AXIS2_PLACEMENT_3D ( 'NONE', #959, #9113, #11262 ) ;
#1042=CARTESIAN_POINT ( 'NONE',  ( 1.039999999999996483, -12.96210679857803783, 24.89775460606827551 ) ) ;
#1046=CARTESIAN_POINT ( 'NONE',  ( 0.02436607992776585255, -5.391175441198789109, 24.15498966839961170 ) ) ;
#1048=CARTESIAN_POINT ( 'NONE',  ( 2.765633920072239516, -24.15498966839958683, -5.391175441198872598 ) ) ;
#1050=FACE_OUTER_BOUND ( 'NONE', #6316, .T. ) ;
#1052=CARTESIAN_POINT ( 'NONE',  ( 2.789999999999999147, 14.55412442567645215, -19.64056340710859772 ) ) ;
#1055=VERTEX_POINT ( 'NONE', #4726 ) ;
#1056=B_SPLINE_CURVE_WITH_KNOTS ( 'NONE', 3,
 ( #14995, #4461, #9141, #9299 ),
 .UNSPECIFIED., .F., .F.,
 ( 4, 4 ),
 ( 2.324263106244727961E-07, 0.0006888201370294844746 ),
 .UNSPECIFIED. ) ;
#1057=EDGE_CURVE ( 'NONE', #10796, #3392, #11919, .T. ) ;
#1062=CARTESIAN_POINT ( 'NONE',  ( 2.789999999999999147, -25.59481291497571220, -1.787276233276378314E-13 ) ) ;
#1063=DIRECTION ( 'NONE',  ( -1.000000000000000000, -0.000000000000000000, -0.000000000000000000 ) ) ;
#1064=ORIENTED_EDGE ( 'NONE', *, *, #629, .F. ) ;
#1065=CARTESIAN_POINT ( 'NONE',  ( 2.789999999999999147, 7.909232158575156824, -24.34211360614291664 ) ) ;
#1072=CARTESIAN_POINT ( 'NONE',  ( 2.789999999999999147, -24.63872515616080960, -2.336989772644527008 ) ) ;
#1088=AXIS2_PLACEMENT_3D ( 'NONE', #3058, #5452, #751 ) ;
#1092=AXIS2_PLACEMENT_3D ( 'NONE', #13318, #5127, #5044 ) ;
#1096=LINE ( 'NONE', #15093, #3554 ) ;
#1097=ORIENTED_EDGE ( 'NONE', *, *, #1791, .T. ) ;
#1100=AXIS2_PLACEMENT_3D ( 'NONE', #502, #5221, #6207 ) ;
#1102=AXIS2_PLACEMENT_3D ( 'NONE', #2865, #3021, #11084 ) ;
#1103=ADVANCED_FACE ( 'NONE', ( #9624 ), #2487, .F. ) ;
#1104=VERTEX_POINT ( 'NONE', #14401 ) ;
#1110=VERTEX_POINT ( 'NONE', #14319 ) ;
#1112=CARTESIAN_POINT ( 'NONE',  ( 1.394999999999999574, -25.12109765559644714, -12.52377138324250616 ) ) ;
#1113=ORIENTED_EDGE ( 'NONE', *, *, #10018, .F. ) ;
#1120=DIRECTION ( 'NONE',  ( 1.000000000000000000, -0.000000000000000000, 0.000000000000000000 ) ) ;
#1123=DIRECTION ( 'NONE',  ( 0.000000000000000000, 0.000000000000000000, 1.000000000000000000 ) ) ;
#1126=EDGE_CURVE ( 'NONE', #1971, #10848, #12626, .T. ) ;
#1130=PLANE ( 'NONE',  #5867 ) ;
#1135=EDGE_LOOP ( 'NONE', ( #6017, #411, #13009, #12237, #2229, #1097, #5536, #3727 ) ) ;
#1139=ORIENTED_EDGE ( 'NONE', *, *, #2318, .T. ) ;
#1144=CARTESIAN_POINT ( 'NONE',  ( 1.039999999999997593, 0.000000000000000000, 0.000000000000000000 ) ) ;
#1146=DIRECTION ( 'NONE',  ( 1.000000000000000000, 0.000000000000000000, 0.000000000000000000 ) ) ;
#1150=AXIS2_PLACEMENT_3D ( 'NONE', #1436, #14196, #4910 ) ;
#1151=AXIS2_PLACEMENT_3D ( 'NONE', #529, #13228, #10915 ) ;
#1153=ORIENTED_EDGE ( 'NONE', *, *, #7233, .F. ) ;
#1158=VERTEX_POINT ( 'NONE', #12922 ) ;
#1162=CARTESIAN_POINT ( 'NONE',  ( 1.749999999999998002, -27.68468304288262516, 4.633866840648810381 ) ) ;
#1165=CARTESIAN_POINT ( 'NONE',  ( 1.749999999999998002, -24.89775460606842117, 12.96210679857777137 ) ) ;
#1172=VECTOR ( 'NONE', #15011, 1000.000000000000000 ) ;
#1173=ORIENTED_EDGE ( 'NONE', *, *, #10150, .T. ) ;
#1176=ORIENTED_EDGE ( 'NONE', *, *, #2059, .T. ) ;
#1177=ORIENTED_EDGE ( 'NONE', *, *, #2258, .T. ) ;
#1180=DIRECTION ( 'NONE',  ( 0.000000000000000000, 0.000000000000000000, 1.000000000000000000 ) ) ;
#1189=ORIENTED_EDGE ( 'NONE', *, *, #8120, .T. ) ;
#1190=TOROIDAL_SURFACE ( 'NONE', #14951, 24.12539914357697768, 8.000000000000000000 ) ;
#1195=ADVANCED_FACE ( 'NONE', ( #13619 ), #7733, .T. ) ;
#1198=CYLINDRICAL_SURFACE ( 'NONE', #442, 2.524999999999995914 ) ;
#1206=DIRECTION ( 'NONE',  ( 0.000000000000000000, 0.000000000000000000, -1.000000000000000000 ) ) ;
#1207=CARTESIAN_POINT ( 'NONE',  ( 0.07181525480391370841, -12.74223776959215826, 21.92234060054341427 ) ) ;
#1209=CARTESIAN_POINT ( 'NONE',  ( 2.718184749312773540, -2.576941577947583273, 25.22524549359949120 ) ) ;
#1210=EDGE_CURVE ( 'NONE', #13239, #949, #1314, .T. ) ;
#1215=CARTESIAN_POINT ( 'NONE',  ( 2.765633920072236851, -22.71065055754445439, -9.836394144775947979 ) ) ;
#1217=CARTESIAN_POINT ( 'NONE',  ( 2.789999999999999147, -7.772527002114597572, 23.17675759782038369 ) ) ;
#1221=B_SPLINE_CURVE_WITH_KNOTS ( 'NONE', 3,
 ( #5472, #4235, #9145, #3233, #7918, #8909 ),
 .UNSPECIFIED., .F., .F.,
 ( 4, 2, 4 ),
 ( 4.462636882273700183E-07, 0.001879885203074810199, 0.003759324142461393028 ),
 .UNSPECIFIED. ) ;
#1226=ADVANCED_BREP_SHAPE_REPRESENTATION ( '', ( #8904, #1376 ), #11929 ) ;
#1232=ORIENTED_EDGE ( 'NONE', *, *, #3988, .F. ) ;
#1242=B_SPLINE_CURVE_WITH_KNOTS ( 'NONE', 3,
 ( #4683, #11726, #11866, #3506, #1209, #9581 ),
 .UNSPECIFIED., .F., .F.,
 ( 4, 2, 4 ),
 ( 4.462636732217463004E-07, 0.001879885066975006029, 0.003759323870276790047 ),
 .UNSPECIFIED. ) ;
#1246=FACE_OUTER_BOUND ( 'NONE', #3129, .T. ) ;
#1255=CARTESIAN_POINT ( 'NONE',  ( 1.749999999999998002, -4.147968289691484678, 27.76164181293050603 ) ) ;
#1262=ORIENTED_EDGE ( 'NONE', *, *, #9472, .T. ) ;
#1266=DIRECTION ( 'NONE',  ( 0.000000000000000000, -6.870191984066573782E-16, -1.000000000000000000 ) ) ;
#1276=ORIENTED_EDGE ( 'NONE', *, *, #7099, .T. ) ;
#1284=DIRECTION ( 'NONE',  ( -1.000000000000000000, -0.000000000000000000, -0.000000000000000000 ) ) ;
#1289=DIRECTION ( 'NONE',  ( -1.000000000000000000, 0.000000000000000000, -0.000000000000000000 ) ) ;
#1290=EDGE_CURVE ( 'NONE', #12512, #11686, #5017, .T. ) ;
#1291=ADVANCED_FACE ( 'NONE', ( #1554 ), #4791, .T. ) ;
#1292=ORIENTED_EDGE ( 'NONE', *, *, #13403, .F. ) ;
#1294=CARTESIAN_POINT ( 'NONE',  ( 0.02436607992776064838, 18.55949924794892780, 16.37294372382865504 ) ) ;
#1295=CARTESIAN_POINT ( 'NONE',  ( 0.9661342547375842971, -24.74813374239834474, 12.96725027898183669 ) ) ;
#1296=VERTEX_POINT ( 'NONE', #394 ) ;
#1299=ORIENTED_EDGE ( 'NONE', *, *, #10463, .T. ) ;
#1307=EDGE_CURVE ( 'NONE', #316, #446, #12152, .T. ) ;
#1310=EDGE_CURVE ( 'NONE', #6398, #6064, #7237, .T. ) ;
#1313=DIRECTION ( 'NONE',  ( 0.000000000000000000, 0.000000000000000000, 1.000000000000000000 ) ) ;
#1314=B_SPLINE_CURVE_WITH_KNOTS ( 'NONE', 3,
 ( #7561, #2785, #3102, #7705, #8623, #5420 ),
 .UNSPECIFIED., .F., .F.,
 ( 4, 2, 4 ),
 ( 4.462636882221863355E-07, 0.001879885203074805429, 0.003759324142461388692 ),
 .UNSPECIFIED. ) ;
#1315=B_SPLINE_CURVE_WITH_KNOTS ( 'NONE', 3,
 ( #10884, #14355, #9966, #14666, #3817, #7661 ),
 .UNSPECIFIED., .F., .F.,
 ( 4, 2, 4 ),
 ( 2.586195665735896780E-07, 0.001878649493629692057, 0.003757040367692810780 ),
 .UNSPECIFIED. ) ;
#1318=TOROIDAL_SURFACE ( 'NONE', #336, 24.12539914357697413, 8.000000000000000000 ) ;
#1321=DIRECTION ( 'NONE',  ( -1.000000000000000000, -0.000000000000000000, -0.000000000000000000 ) ) ;
#1325=CARTESIAN_POINT ( 'NONE',  ( 2.783069004973548921, -5.408431875071614492, 23.92277630352793238 ) ) ;
#1329=DIRECTION ( 'NONE',  ( 0.000000000000000000, 0.000000000000000000, 1.000000000000000000 ) ) ;
#1331=ORIENTED_EDGE ( 'NONE', *, *, #249, .F. ) ;
#1334=ORIENTED_EDGE ( 'NONE', *, *, #7370, .T. ) ;
#1336=VECTOR ( 'NONE', #4511, 1000.000000000000000 ) ;
#1337=CARTESIAN_POINT ( 'NONE',  ( 2.789999999999999147, 12.59161484032942901, -21.30679549418617924 ) ) ;
#1339=VECTOR ( 'NONE', #483, 1000.000000000000000 ) ;
#1341=DIRECTION ( 'NONE',  ( -1.000000000000000000, -0.000000000000000000, 0.000000000000000000 ) ) ;
#1344=DIRECTION ( 'NONE',  ( -1.000000000000000000, -0.000000000000000000, -0.000000000000000000 ) ) ;
#1345=ORIENTED_EDGE ( 'NONE', *, *, #9712, .T. ) ;
#1350=CIRCLE ( 'NONE', #11659, 2.524999999999996358 ) ;
#1352=ORIENTED_EDGE ( 'NONE', *, *, #13563, .T. ) ;
#1355=ORIENTED_EDGE ( 'NONE', *, *, #11067, .T. ) ;
#1356=CARTESIAN_POINT ( 'NONE',  ( 1.039999999999997593, 0.000000000000000000, 0.000000000000000000 ) ) ;
#1363=AXIS2_PLACEMENT_3D ( 'NONE', #789, #12619, #15020 ) ;
#1370=EDGE_CURVE ( 'NONE', #13796, #1588, #6008, .T. ) ;
#1372=CARTESIAN_POINT ( 'NONE',  ( 0.8291131470075020493, -24.44424927289185590, 12.96989951879399072 ) ) ;
#1373=VERTEX_POINT ( 'NONE', #9323 ) ;
#1376=AXIS2_PLACEMENT_3D ( 'NONE', #7353, #6187, #9640 ) ;
#1380=CARTESIAN_POINT ( 'NONE',  ( 0.000000000000000000, 1.991882183130315953, 24.04302995059967074 ) ) ;
#1386=CARTESIAN_POINT ( 'NONE',  ( 0.02436607992776151574, -16.37294372382871188, 18.55949924794887096 ) ) ;
#1388=DIRECTION ( 'NONE',  ( 0.000000000000000000, 0.000000000000000000, 1.000000000000000000 ) ) ;
#1390=VERTEX_POINT ( 'NONE', #5491 ) ;
#1394=EDGE_CURVE ( 'NONE', #5482, #4132, #14540, .T. ) ;
#1403=AXIS2_PLACEMENT_3D ( 'NONE', #1515, #9820, #3977 ) ;
#1405=DIRECTION ( 'NONE',  ( -1.000000000000000000, 0.000000000000000000, -0.000000000000000000 ) ) ;
#1415=CIRCLE ( 'NONE', #4364, 2.524999999999995914 ) ;
#1417=CARTESIAN_POINT ( 'NONE',  ( 1.039999999999996261, 12.96210679857786197, 24.89775460606836788 ) ) ;
#1423=VERTEX_POINT ( 'NONE', #12766 ) ;
#1426=DIRECTION ( 'NONE',  ( 0.000000000000000000, 0.000000000000000000, -1.000000000000000000 ) ) ;
#1427=CARTESIAN_POINT ( 'NONE',  ( 0.5321745407694753460, 4.993157874728185952, -26.58873630738046501 ) ) ;
#1430=DIRECTION ( 'NONE',  ( 0.000000000000000000, 0.000000000000000000, 1.000000000000000000 ) ) ;
#1431=AXIS2_PLACEMENT_3D ( 'NONE', #92, #11853, #9271 ) ;
#1434=DIRECTION ( 'NONE',  ( 0.000000000000000000, 0.000000000000000000, 1.000000000000000000 ) ) ;
#1436=CARTESIAN_POINT ( 'NONE',  ( 0.000000000000000000, -15.04425356660774682, 20.70663861606266209 ) ) ;
#1442=CARTESIAN_POINT ( 'NONE',  ( 0.5321745326902582729, -26.83036154824997155, 3.467596033028195635 ) ) ;
#1444=EDGE_CURVE ( 'NONE', #6713, #2082, #10507, .T. ) ;
#1446=CARTESIAN_POINT ( 'NONE',  ( 2.765633920072237295, 12.59161484032912171, 21.30679549418635688 ) ) ;
#1454=CARTESIAN_POINT ( 'NONE',  ( 2.257825459230522913, 26.58873630738059290, -4.993157874727537582 ) ) ;
#1458=ORIENTED_EDGE ( 'NONE', *, *, #5920, .T. ) ;
#1466=B_SPLINE_CURVE_WITH_KNOTS ( 'NONE', 3,
 ( #796, #4196, #13559, #2103, #5501, #7719 ),
 .UNSPECIFIED., .F., .F.,
 ( 4, 2, 4 ),
 ( 2.321268216997199256E-07, 0.001878622960950494455, 0.003757013795079288884 ),
 .UNSPECIFIED. ) ;
#1467=ADVANCED_FACE ( 'NONE', ( #6862 ), #9694, .T. ) ;
#1471=CARTESIAN_POINT ( 'NONE',  ( 2.789999999999999147, 0.000000000000000000, 0.000000000000000000 ) ) ;
#1472=ORIENTED_EDGE ( 'NONE', *, *, #5616, .F. ) ;
#1473=DIRECTION ( 'NONE',  ( 1.000000000000000000, 0.000000000000000000, 0.000000000000000000 ) ) ;
#1478=EDGE_LOOP ( 'NONE', ( #3332, #9837, #9394, #9371, #9412, #4981 ) ) ;
#1479=CARTESIAN_POINT ( 'NONE',  ( 1.039999999999995817, 27.76164181293051669, 4.147968289691385202 ) ) ;
#1481=EDGE_LOOP ( 'NONE', ( #11695, #14531, #10098, #7397 ) ) ;
#1487=CARTESIAN_POINT ( 'NONE',  ( 0.02436607992775978102, 2.336989772644613161, -24.63872515616080250 ) ) ;
#1492=CARTESIAN_POINT ( 'NONE',  ( 2.257825467309741541, 3.467596033028661928, -26.83036154824990760 ) ) ;
#1498=ORIENTED_EDGE ( 'NONE', *, *, #12801, .T. ) ;
#1501=CARTESIAN_POINT ( 'NONE',  ( 0.000000000000000000, 20.62201879784932856, -12.52067188844328705 ) ) ;
#1507=CARTESIAN_POINT ( 'NONE',  ( 2.789999999999999147, -8.936381166381891568E-14, 25.59481291497571220 ) ) ;
#1511=ADVANCED_FACE ( 'NONE', ( #9456 ), #12987, .T. ) ;
#1514=DIRECTION ( 'NONE',  ( -1.000000000000000000, -0.000000000000000000, -0.000000000000000000 ) ) ;
#1515=CARTESIAN_POINT ( 'NONE',  ( 2.789999999999999147, -23.31896751603337137, 7.334849878007427826 ) ) ;
#1528=VERTEX_POINT ( 'NONE', #10692 ) ;
#1531=ORIENTED_EDGE ( 'NONE', *, *, #3062, .T. ) ;
#1535=AXIS2_PLACEMENT_3D ( 'NONE', #15062, #1284, #13903 ) ;
#1536=CARTESIAN_POINT ( 'NONE',  ( 2.718131885465892239, 16.91241718341998634, 18.89333555428560274 ) ) ;
#1537=B_SPLINE_CURVE_WITH_KNOTS ( 'NONE', 3,
 ( #2299, #14055, #8211, #14291 ),
 .UNSPECIFIED., .F., .F.,
 ( 4, 4 ),
 ( 2.034713381942770827E-07, 0.0006887909409525120848 ),
 .UNSPECIFIED. ) ;
#1546=( LENGTH_UNIT ( ) NAMED_UNIT ( * ) SI_UNIT ( .MILLI., .METRE. ) );
#1547=VERTEX_POINT ( 'NONE', #11683 ) ;
#1548=ORIENTED_EDGE ( 'NONE', *, *, #7466, .F. ) ;
#1552=CARTESIAN_POINT ( 'NONE',  ( 0.02436607992776628623, 24.63872515616082737, -2.336989772644355590 ) ) ;
#1554=FACE_OUTER_BOUND ( 'NONE', #1889, .T. ) ;
#1556=B_SPLINE_CURVE_WITH_KNOTS ( 'NONE', 3,
 ( #690, #4387, #4304, #13594 ),
 .UNSPECIFIED., .F., .F.,
 ( 4, 4 ),
 ( 0.005258120783916789796, 0.005948386350302922905 ),
 .UNSPECIFIED. ) ;
#1562=ORIENTED_EDGE ( 'NONE', *, *, #1939, .T. ) ;
#1563=DIRECTION ( 'NONE',  ( -1.000000000000000000, -0.000000000000000000, 0.000000000000000000 ) ) ;
#1565=VERTEX_POINT ( 'NONE', #14306 ) ;
#1566=VERTEX_POINT ( 'NONE', #10772 ) ;
#1574=AXIS2_PLACEMENT_3D ( 'NONE', #13243, #10929, #13389 ) ;
#1575=DIRECTION ( 'NONE',  ( -1.000000000000000000, 0.000000000000000000, -0.000000000000000000 ) ) ;
#1580=CARTESIAN_POINT ( 'NONE',  ( 2.789999999999999147, -15.04425356660744839, -20.70663861606288236 ) ) ;
#1582=VERTEX_POINT ( 'NONE', #3767 ) ;
#1583=EDGE_CURVE ( 'NONE', #12872, #5857, #2627, .T. ) ;
#1584=ORIENTED_EDGE ( 'NONE', *, *, #11111, .T. ) ;
#1585=TOROIDAL_SURFACE ( 'NONE', #6489, 24.12539914357697768, 8.000000000000000000 ) ;
#1586=EDGE_CURVE ( 'NONE', #13319, #1997, #3119, .T. ) ;
#1588=VERTEX_POINT ( 'NONE', #12905 ) ;
#1590=CARTESIAN_POINT ( 'NONE',  ( 0.7592463941534255412, -27.31305418910211813, 3.797885586973120287 ) ) ;
#1591=DIRECTION ( 'NONE',  ( 0.000000000000000000, 0.000000000000000000, 1.000000000000000000 ) ) ;
#1592=EDGE_CURVE ( 'NONE', #8603, #8358, #5211, .T. ) ;
#1599=ORIENTED_EDGE ( 'NONE', *, *, #10293, .T. ) ;
#1600=CARTESIAN_POINT ( 'NONE',  ( 0.1855655959470677019, -19.17825124759764677, -17.45907811351477079 ) ) ;
#1604=ORIENTED_EDGE ( 'NONE', *, *, #6490, .T. ) ;
#1606=CARTESIAN_POINT ( 'NONE',  ( 1.823865745262398308, 24.74813374239829145, 12.96725027898200899 ) ) ;
#1607=VECTOR ( 'NONE', #13853, 1000.000000000000000 ) ;
#1608=B_SPLINE_CURVE_WITH_KNOTS ( 'NONE', 3,
 ( #9989, #1536, #7461, #6225, #9842, #12362 ),
 .UNSPECIFIED., .F., .F.,
 ( 4, 2, 4 ),
 ( 2.321268216997094965E-07, 0.001878622960950493588, 0.003757013795079287150 ),
 .UNSPECIFIED. ) ;
#1609=CARTESIAN_POINT ( 'NONE',  ( 2.358581579527286198, -23.43037373958380343, 12.94152279942367656 ) ) ;
#1612=CARTESIAN_POINT ( 'NONE',  ( -7.634507448887241432E-14, 22.38018801136490055, -9.515416771310970745 ) ) ;
#1617=AXIS2_PLACEMENT_3D ( 'NONE', #644, #5052, #5207 ) ;
#1618=CARTESIAN_POINT ( 'NONE',  ( 0.02436607992776455150, 21.30679549418631780, 12.59161484032919986 ) ) ;
#1622=DIRECTION ( 'NONE',  ( -1.000000000000000000, -0.000000000000000000, -0.000000000000000000 ) ) ;
#1625=DIRECTION ( 'NONE',  ( 0.000000000000000000, 2.061057595219972332E-15, -1.000000000000000000 ) ) ;
#1627=B_SPLINE_CURVE_WITH_KNOTS ( 'NONE', 3,
 ( #6678, #11358, #1995, #10355 ),
 .UNSPECIFIED., .F., .F.,
 ( 4, 4 ),
 ( 0.005258139959819237326, 0.005948405594583419317 ),
 .UNSPECIFIED. ) ;
#1628=ORIENTED_EDGE ( 'NONE', *, *, #6271, .F. ) ;
#1630=CARTESIAN_POINT ( 'NONE',  ( 0.000000000000000000, 22.25075486061737351, 9.324097380959511128 ) ) ;
#1633=AXIS2_PLACEMENT_3D ( 'NONE', #12047, #11057, #10829 ) ;
#1635=DIRECTION ( 'NONE',  ( 0.000000000000000000, 0.000000000000000000, 1.000000000000000000 ) ) ;
#1642=CARTESIAN_POINT ( 'NONE',  ( 0.02436607992776455150, 5.391175441198956086, -24.15498966839956907 ) ) ;
#1645=ORIENTED_EDGE ( 'NONE', *, *, #13717, .T. ) ;
#1647=CYLINDRICAL_SURFACE ( 'NONE', #13911, 13.20000000000000107 ) ;
#1648=EDGE_CURVE ( 'NONE', #7241, #13039, #7780, .T. ) ;
#1650=ORIENTED_EDGE ( 'NONE', *, *, #4884, .T. ) ;
#1651=ORIENTED_EDGE ( 'NONE', *, *, #10497, .F. ) ;
#1652=CARTESIAN_POINT ( 'NONE',  ( 0.000000000000000000, -9.324097380959594616, 22.25075486061734509 ) ) ;
#1656=CYLINDRICAL_SURFACE ( 'NONE', #1617, 13.19999999999999929 ) ;
#1657=DIRECTION ( 'NONE',  ( 0.000000000000000000, 0.000000000000000000, 1.000000000000000000 ) ) ;
#1663=TOROIDAL_SURFACE ( 'NONE', #14929, 24.12539914357697768, 8.000000000000000000 ) ;
#1665=CYLINDRICAL_SURFACE ( 'NONE', #14918, 13.19999999999999929 ) ;
#1666=ADVANCED_FACE ( 'NONE', ( #5181 ), #2375, .T. ) ;
#1667=EDGE_CURVE ( 'NONE', #6064, #9763, #575, .T. ) ;
#1672=CARTESIAN_POINT ( 'NONE',  ( 0.000000000000000000, 0.000000000000000000, 0.000000000000000000 ) ) ;
#1676=CARTESIAN_POINT ( 'NONE',  ( 2.030753616560876829, -24.80264696524875490, -12.05220173035465336 ) ) ;
#1680=CARTESIAN_POINT ( 'NONE',  ( 2.718131853594927261, 12.74240566899015903, -21.92302674874949986 ) ) ;
#1681=EDGE_CURVE ( 'NONE', #15005, #6121, #9575, .T. ) ;
#1686=EDGE_CURVE ( 'NONE', #13918, #15033, #10957, .T. ) ;
#1690=DIRECTION ( 'NONE',  ( 0.000000000000000000, 0.000000000000000000, 1.000000000000000000 ) ) ;
#1691=CARTESIAN_POINT ( 'NONE',  ( 0.02436607992776325046, -18.55949924794904504, 16.37294372382852004 ) ) ;
#1696=EDGE_CURVE ( 'NONE', #6713, #2610, #6547, .T. ) ;
#1697=CARTESIAN_POINT ( 'NONE',  ( 0.02436607992775978102, 2.336989772644613161, -24.63872515616080250 ) ) ;
#1698=DIRECTION ( 'NONE',  ( 0.000000000000000000, 0.000000000000000000, 1.000000000000000000 ) ) ;
#1699=CARTESIAN_POINT ( 'NONE',  ( -5.209999999999999964, 0.000000000000000000, 0.000000000000000000 ) ) ;
#1707=ORIENTED_EDGE ( 'NONE', *, *, #7385, .T. ) ;
#1712=EDGE_CURVE ( 'NONE', #4813, #13461, #899, .T. ) ;
#1715=DIRECTION ( 'NONE',  ( -1.000000000000000000, 0.000000000000000000, -0.000000000000000000 ) ) ;
#1727=ORIENTED_EDGE ( 'NONE', *, *, #13983, .T. ) ;
#1728=ORIENTED_EDGE ( 'NONE', *, *, #15096, .F. ) ;
#1730=CARTESIAN_POINT ( 'NONE',  ( 2.783025228907522131, -9.686319561461109728, 22.53337530003400246 ) ) ;
#1740=ORIENTED_EDGE ( 'NONE', *, *, #12994, .T. ) ;
#1741=B_SPLINE_CURVE_WITH_KNOTS ( 'NONE', 3,
 ( #7225, #13048, #4937, #12897 ),
 .UNSPECIFIED., .F., .F.,
 ( 4, 4 ),
 ( 1.981826382900813409E-07, 0.0006887856082032219702 ),
 .UNSPECIFIED. ) ;
#1743=VERTEX_POINT ( 'NONE', #12059 ) ;
#1746=DIRECTION ( 'NONE',  ( -1.000000000000000000, -0.000000000000000000, -0.000000000000000000 ) ) ;
#1748=DIRECTION ( 'NONE',  ( 0.000000000000000000, 0.000000000000000000, 1.000000000000000000 ) ) ;
#1761=EDGE_LOOP ( 'NONE', ( #3897, #12840, #9108, #15209, #13536, #5396, #5250, #11117 ) ) ;
#1762=ORIENTED_EDGE ( 'NONE', *, *, #7585, .F. ) ;
#1765=DIRECTION ( 'NONE',  ( 0.000000000000000000, 0.000000000000000000, 1.000000000000000000 ) ) ;
#1766=DIRECTION ( 'NONE',  ( 0.000000000000000000, 0.000000000000000000, 1.000000000000000000 ) ) ;
#1767=CYLINDRICAL_SURFACE ( 'NONE', #9922, 28.06981291497571362 ) ;
#1770=AXIS2_PLACEMENT_3D ( 'NONE', #1052, #6044, #3580 ) ;
#1779=VERTEX_POINT ( 'NONE', #997 ) ;
#1783=CARTESIAN_POINT ( 'NONE',  ( 2.790000000000000036, -20.65025570340076655, -12.51972505885016140 ) ) ;
#1790=CARTESIAN_POINT ( 'NONE',  ( 0.000000000000000000, -23.48180575137736170, 5.535312321042622052 ) ) ;
#1791=EDGE_CURVE ( 'NONE', #4429, #1582, #9724, .T. ) ;
#1794=CARTESIAN_POINT ( 'NONE',  ( 2.789999999999999147, 0.000000000000000000, 0.000000000000000000 ) ) ;
#1801=DIRECTION ( 'NONE',  ( 0.000000000000000000, 0.000000000000000000, 1.000000000000000000 ) ) ;
#1812=ORIENTED_EDGE ( 'NONE', *, *, #14545, .F. ) ;
#1816=EDGE_CURVE ( 'NONE', #10954, #10191, #12750, .T. ) ;
#1818=LINE ( 'NONE', #8729, #2381 ) ;
#1820=CARTESIAN_POINT ( 'NONE',  ( 2.601776091974071115, -5.251266773802197640, -25.40949241676359094 ) ) ;
#1822=CYLINDRICAL_SURFACE ( 'NONE', #7593, 2.524999999999995914 ) ;
#1823=AXIS2_PLACEMENT_3D ( 'NONE', #2979, #11196, #671 ) ;
#1831=ORIENTED_EDGE ( 'NONE', *, *, #2240, .T. ) ;
#1832=AXIS2_PLACEMENT_3D ( 'NONE', #5697, #10372, #5476 ) ;
#1835=CARTESIAN_POINT ( 'NONE',  ( 0.02436607992776411782, 22.71065055754465689, -9.836394144775473691 ) ) ;
#1837=ORIENTED_EDGE ( 'NONE', *, *, #14433, .F. ) ;
#1838=CARTESIAN_POINT ( 'NONE',  ( 2.790000000000000036, 24.22479935914659777, -2.133490293297098273 ) ) ;
#1840=EDGE_CURVE ( 'NONE', #3303, #4132, #9475, .T. ) ;
#1841=CARTESIAN_POINT ( 'NONE',  ( 0.006931054464085153848, 2.248820353273311756, -24.42321038836780644 ) ) ;
#1844=CIRCLE ( 'NONE', #13857, 2.524999999999995914 ) ;
#1847=CARTESIAN_POINT ( 'NONE',  ( 1.749999999999998002, 0.000000000000000000, 0.000000000000000000 ) ) ;
#1848=CARTESIAN_POINT ( 'NONE',  ( 2.789999999999999147, 5.535312321043049266, -23.48180575137724446 ) ) ;
#1849=VERTEX_POINT ( 'NONE', #3083 ) ;
#1850=DIRECTION ( 'NONE',  ( -1.000000000000000000, -0.000000000000000000, -0.000000000000000000 ) ) ;
#1852=ORIENTED_EDGE ( 'NONE', *, *, #2015, .F. ) ;
#1854=EDGE_CURVE ( 'NONE', #11686, #6526, #3965, .T. ) ;
#1858=VECTOR ( 'NONE', #2108, 1000.000000000000000 ) ;
#1864=CARTESIAN_POINT ( 'NONE',  ( -10.00000000000000000, 0.000000000000000000, 0.000000000000000000 ) ) ;
#1867=ORIENTED_EDGE ( 'NONE', *, *, #8472, .T. ) ;
#1869=CARTESIAN_POINT ( 'NONE',  ( -10.00000000000000000, 0.000000000000000000, 0.000000000000000000 ) ) ;
#1870=ADVANCED_FACE ( 'NONE', ( #4540 ), #2857, .T. ) ;
#1875=ORIENTED_EDGE ( 'NONE', *, *, #1681, .F. ) ;
#1877=AXIS2_PLACEMENT_3D ( 'NONE', #12439, #902, #10287 ) ;
#1879=ORIENTED_EDGE ( 'NONE', *, *, #987, .F. ) ;
#1884=CARTESIAN_POINT ( 'NONE',  ( 1.749999999999998002, 20.02152543075374069, -19.67366047555509212 ) ) ;
#1889=EDGE_LOOP ( 'NONE', ( #1852, #6443, #10065, #13180, #5022, #10812 ) ) ;
#1891=CARTESIAN_POINT ( 'NONE',  ( 2.789999999999999147, 2.680914349914567470E-13, -25.59481291497571220 ) ) ;
#1892=VECTOR ( 'NONE', #10156, 1000.000000000000000 ) ;
#1897=ORIENTED_EDGE ( 'NONE', *, *, #4607, .T. ) ;
#1898=ORIENTED_EDGE ( 'NONE', *, *, #14445, .F. ) ;
#1902=CARTESIAN_POINT ( 'NONE',  ( 0.000000000000000000, 20.70663861606272249, 15.04425356660767932 ) ) ;
#1904=AXIS2_PLACEMENT_3D ( 'NONE', #1144, #4834, #7284 ) ;
#1910=CARTESIAN_POINT ( 'NONE',  ( 0.02436607992776368414, 18.55949924794916228, -16.37294372382838148 ) ) ;
#1911=DIRECTION ( 'NONE',  ( 0.000000000000000000, -0.3090169943749486170, 0.9510565162951530871 ) ) ;
#1919=TOROIDAL_SURFACE ( 'NONE', #3876, 24.12539914357697413, 8.000000000000000000 ) ;
#1934=VECTOR ( 'NONE', #13923, 1000.000000000000000 ) ;
#1935=TOROIDAL_SURFACE ( 'NONE', #13710, 24.12539914357697413, 8.000000000000000000 ) ;
#1938=ORIENTED_EDGE ( 'NONE', *, *, #3558, .T. ) ;
#1939=EDGE_CURVE ( 'NONE', #929, #11100, #10710, .T. ) ;
#1940=VERTEX_POINT ( 'NONE', #7066 ) ;
#1941=ORIENTED_EDGE ( 'NONE', *, *, #12061, .F. ) ;
#1942=ORIENTED_EDGE ( 'NONE', *, *, #6245, .F. ) ;
#1944=( NAMED_UNIT ( * ) PLANE_ANGLE_UNIT ( ) SI_UNIT ( $, .RADIAN. ) );
#1948=CARTESIAN_POINT ( 'NONE',  ( 1.039999999999996705, -20.02152543075359503, 19.67366047555523423 ) ) ;
#1950=ORIENTED_EDGE ( 'NONE', *, *, #14469, .T. ) ;
#1955=DIRECTION ( 'NONE',  ( 1.000000000000000000, -0.000000000000000000, -0.000000000000000000 ) ) ;
#1957=ORIENTED_EDGE ( 'NONE', *, *, #1648, .T. ) ;
#1960=ORIENTED_EDGE ( 'NONE', *, *, #1370, .F. ) ;
#1962=B_SPLINE_CURVE_WITH_KNOTS ( 'NONE', 3,
 ( #10367, #4391, #918, #5621, #2999, #4464 ),
 .UNSPECIFIED., .F., .F.,
 ( 4, 2, 4 ),
 ( 2.032124546189808531E-07, 0.001878594002992309232, 0.003756984793529999193 ),
 .UNSPECIFIED. ) ;
#1963=CARTESIAN_POINT ( 'NONE',  ( 1.394999999999999574, -4.633866840649122132, 27.68468304288257542 ) ) ;
#1965=CARTESIAN_POINT ( 'NONE',  ( 8.000000000000000000, 0.000000000000000000, 0.000000000000000000 ) ) ;
#1971=VERTEX_POINT ( 'NONE', #4765 ) ;
#1974=VERTEX_POINT ( 'NONE', #1294 ) ;
#1978=ORIENTED_EDGE ( 'NONE', *, *, #12875, .F. ) ;
#1979=EDGE_CURVE ( 'NONE', #6140, #8705, #471, .T. ) ;
#1983=CARTESIAN_POINT ( 'NONE',  ( 2.789999999999999147, 19.91106274590533687, -14.18181402625721077 ) ) ;
#1990=DIRECTION ( 'NONE',  ( 0.000000000000000000, 0.000000000000000000, 1.000000000000000000 ) ) ;
#1991=CYLINDRICAL_SURFACE ( 'NONE', #10235, 2.524999999999995914 ) ;
#1994=DIRECTION ( 'NONE',  ( 1.000000000000000000, 0.000000000000000000, 0.000000000000000000 ) ) ;
#1995=CARTESIAN_POINT ( 'NONE',  ( 2.783068961317272993, 12.53626894672858683, -21.08061549536601476 ) ) ;
#1997=VERTEX_POINT ( 'NONE', #2689 ) ;
#1998=FACE_OUTER_BOUND ( 'NONE', #11226, .T. ) ;
#2009=B_SPLINE_CURVE_WITH_KNOTS ( 'NONE', 3,
 ( #6961, #4674, #9408, #14105 ),
 .UNSPECIFIED., .F., .F.,
 ( 4, 4 ),
 ( 0.005258139959819248602, 0.005948405594583415848 ),
 .UNSPECIFIED. ) ;
#2010=ORIENTED_EDGE ( 'NONE', *, *, #14740, .T. ) ;
#2011=EDGE_LOOP ( 'NONE', ( #1942, #5259, #13694, #8912 ) ) ;
#2012=ORIENTED_EDGE ( 'NONE', *, *, #987, .T. ) ;
#2014=CARTESIAN_POINT ( 'NONE',  ( 0.7589665089996491254, -24.80232951178369660, -12.05173163741749320 ) ) ;
#2015=EDGE_CURVE ( 'NONE', #446, #4654, #8716, .T. ) ;
#2016=CARTESIAN_POINT ( 'NONE',  ( 2.031033467310410234, -12.98167595241039329, 24.32849926382746020 ) ) ;
#2022=DIRECTION ( 'NONE',  ( 0.000000000000000000, 0.000000000000000000, -1.000000000000000000 ) ) ;
#2024=CARTESIAN_POINT ( 'NONE',  ( 0.5279273746168626769, -4.996265754456183927, -26.57710921259766224 ) ) ;
#2025=CARTESIAN_POINT ( 'NONE',  ( 2.783025325906567371, -24.42374957165203853, -2.249040938978752013 ) ) ;
#2026=ORIENTED_EDGE ( 'NONE', *, *, #4399, .F. ) ;
#2035=ORIENTED_EDGE ( 'NONE', *, *, #8689, .F. ) ;
#2036=DIRECTION ( 'NONE',  ( 0.000000000000000000, -1.000000000000000000, -4.122115190439943875E-15 ) ) ;
#2038=FACE_OUTER_BOUND ( 'NONE', #14776, .T. ) ;
#2041=EDGE_CURVE ( 'NONE', #1528, #2696, #6707, .T. ) ;
#2045=DIRECTION ( 'NONE',  ( 0.000000000000000000, 0.000000000000000000, 1.000000000000000000 ) ) ;
#2047=CARTESIAN_POINT ( 'NONE',  ( 0.8956445960621760571, 24.59653223688280121, 12.96989951879416125 ) ) ;
#2049=CARTESIAN_POINT ( 'NONE',  ( 2.789999999999999147, -22.71065055754445439, -9.836394144775947979 ) ) ;
#2050=CARTESIAN_POINT ( 'NONE',  ( 0.07186814640506890284, 21.92302674874982316, -12.74240566898960303 ) ) ;
#2059=EDGE_CURVE ( 'NONE', #12893, #11975, #10007, .T. ) ;
#2063=VERTEX_POINT ( 'NONE', #2830 ) ;
#2064=CARTESIAN_POINT ( 'NONE',  ( 2.789999999999999147, 0.000000000000000000, 0.000000000000000000 ) ) ;
#2067=CARTESIAN_POINT ( 'NONE',  ( 2.789999999999999147, 23.48180575137737947, -5.535312321042476391 ) ) ;
#2068=CARTESIAN_POINT ( 'NONE',  ( 1.749999999999998002, 0.000000000000000000, 0.000000000000000000 ) ) ;
#2082=VERTEX_POINT ( 'NONE', #14368 ) ;
#2087=CARTESIAN_POINT ( 'NONE',  ( 0.000000000000000000, 0.000000000000000000, 0.000000000000000000 ) ) ;
#2088=ORIENTED_EDGE ( 'NONE', *, *, #3845, .T. ) ;
#2090=CARTESIAN_POINT ( 'NONE',  ( 2.789999999999999147, -25.59481291497571220, -1.787276233276378314E-13 ) ) ;
#2091=DIRECTION ( 'NONE',  ( -1.000000000000000000, 0.000000000000000000, 0.000000000000000000 ) ) ;
#2094=CARTESIAN_POINT ( 'NONE',  ( 2.765633920072236407, 2.336989772644613161, -24.63872515616080250 ) ) ;
#2100=AXIS2_PLACEMENT_3D ( 'NONE', #4098, #12236, #6166 ) ;
#2103=CARTESIAN_POINT ( 'NONE',  ( 0.5279272933715191130, -18.56460150496952366, 19.66369668717026897 ) ) ;
#2108=DIRECTION ( 'NONE',  ( -1.000000000000000000, -0.000000000000000000, 0.000000000000000000 ) ) ;
#2114=CARTESIAN_POINT ( 'NONE',  ( 0.000000000000000000, -15.04425356660744839, -20.70663861606288236 ) ) ;
#2124=CARTESIAN_POINT ( 'NONE',  ( 2.789999999999999147, 7.909232158574813099, 24.34211360614303388 ) ) ;
#2125=AXIS2_PLACEMENT_3D ( 'NONE', #5682, #15053, #13520 ) ;
#2127=CARTESIAN_POINT ( 'NONE',  ( 2.765633920072239071, -16.37294372382844543, -18.55949924794910544 ) ) ;
#2128=AXIS2_PLACEMENT_3D ( 'NONE', #318, #3791, #5040 ) ;
#2132=EDGE_CURVE ( 'NONE', #10310, #8382, #9978, .T. ) ;
#2134=LINE ( 'NONE', #13661, #3366 ) ;
#2136=ORIENTED_EDGE ( 'NONE', *, *, #7399, .T. ) ;
#2138=CARTESIAN_POINT ( 'NONE',  ( 2.765633920072234631, -21.30679549418640306, 12.59161484032904887 ) ) ;
#2143=CARTESIAN_POINT ( 'NONE',  ( 2.789999999999999147, 9.836394144776026138, -22.71065055754441531 ) ) ;
#2145=ORIENTED_EDGE ( 'NONE', *, *, #13176, .F. ) ;
#2149=DIRECTION ( 'NONE',  ( -1.000000000000000000, -0.000000000000000000, -0.000000000000000000 ) ) ;
#2154=ADVANCED_FACE ( 'NONE', ( #586 ), #5306, .T. ) ;
#2155=EDGE_CURVE ( 'NONE', #15073, #14161, #12432, .T. ) ;
#2159=AXIS2_PLACEMENT_3D ( 'NONE', #2430, #13082, #1426 ) ;
#2160=FACE_OUTER_BOUND ( 'NONE', #10784, .T. ) ;
#2164=SURFACE_STYLE_FILL_AREA ( #4316 ) ;
#2166=EDGE_LOOP ( 'NONE', ( #14014, #1064, #11022, #7668, #9543, #14118 ) ) ;
#2168=CARTESIAN_POINT ( 'NONE',  ( 2.601776105308174269, 25.78859396478527799, 2.857713464478781162 ) ) ;
#2170=AXIS2_PLACEMENT_3D ( 'NONE', #13922, #4406, #15077 ) ;
#2178=ADVANCED_FACE ( 'NONE', ( #15050 ), #4288, .T. ) ;
#2198=ORIENTED_EDGE ( 'NONE', *, *, #7466, .T. ) ;
#2199=B_SPLINE_CURVE_WITH_KNOTS ( 'NONE', 3,
 ( #8355, #4992, #13032, #2519, #3743, #9658 ),
 .UNSPECIFIED., .F., .F.,
 ( 4, 2, 4 ),
 ( 1.979325885420574018E-07, 0.001878588715165606469, 0.003756979497742670565 ),
 .UNSPECIFIED. ) ;
#2205=CARTESIAN_POINT ( 'NONE',  ( 0.02436607992776541887, 12.59161484032942901, -21.30679549418617924 ) ) ;
#2210=ORIENTED_EDGE ( 'NONE', *, *, #5514, .F. ) ;
#2211=FACE_OUTER_BOUND ( 'NONE', #12320, .T. ) ;
#2213=DIRECTION ( 'NONE',  ( 0.000000000000000000, 0.000000000000000000, 1.000000000000000000 ) ) ;
#2215=DIRECTION ( 'NONE',  ( -1.000000000000000000, 0.000000000000000000, -0.000000000000000000 ) ) ;
#2217=FACE_OUTER_BOUND ( 'NONE', #7652, .T. ) ;
#2219=ORIENTED_EDGE ( 'NONE', *, *, #4884, .F. ) ;
#2223=ORIENTED_EDGE ( 'NONE', *, *, #10206, .F. ) ;
#2224=DIRECTION ( 'NONE',  ( -1.000000000000000000, -0.000000000000000000, -0.000000000000000000 ) ) ;
#2226=CARTESIAN_POINT ( 'NONE',  ( 2.789999999999999147, 0.000000000000000000, 0.000000000000000000 ) ) ;
#2229=ORIENTED_EDGE ( 'NONE', *, *, #2615, .T. ) ;
#2230=DIRECTION ( 'NONE',  ( 0.000000000000000000, 0.000000000000000000, 1.000000000000000000 ) ) ;
#2236=ORIENTED_EDGE ( 'NONE', *, *, #15083, .T. ) ;
#2237=ORIENTED_EDGE ( 'NONE', *, *, #14137, .T. ) ;
#2240=EDGE_CURVE ( 'NONE', #4703, #11571, #13885, .T. ) ;
#2245=DIRECTION ( 'NONE',  ( 0.000000000000000000, 0.000000000000000000, 1.000000000000000000 ) ) ;
#2248=EDGE_CURVE ( 'NONE', #6366, #11582, #5471, .T. ) ;
#2250=ADVANCED_FACE ( 'NONE', ( #6674 ), #11281, .F. ) ;
#2254=EDGE_CURVE ( 'NONE', #10930, #7241, #8915, .T. ) ;
#2257=CYLINDRICAL_SURFACE ( 'NONE', #4821, 2.524999999999995914 ) ;
#2258=EDGE_CURVE ( 'NONE', #14366, #3394, #7658, .T. ) ;
#2263=DIRECTION ( 'NONE',  ( 0.000000000000000000, 0.000000000000000000, 1.000000000000000000 ) ) ;
#2266=DIRECTION ( 'NONE',  ( 0.000000000000000000, 0.000000000000000000, 1.000000000000000000 ) ) ;
#2267=CARTESIAN_POINT ( 'NONE',  ( 2.601776121706764311, -19.18368891937477727, -17.47009390565512632 ) ) ;
#2270=VECTOR ( 'NONE', #14877, 1000.000000000000000 ) ;
#2271=ORIENTED_EDGE ( 'NONE', *, *, #6899, .F. ) ;
#2272=CARTESIAN_POINT ( 'NONE',  ( 0.000000000000000000, 20.62201879784911540, 12.52067188844362100 ) ) ;
#2273=CARTESIAN_POINT ( 'NONE',  ( 1.039999999999998259, 12.52377138324223615, 25.12109765559657859 ) ) ;
#2274=CARTESIAN_POINT ( 'NONE',  ( 2.765633920072238183, -5.391175441198789109, 24.15498966839961170 ) ) ;
#2279=ADVANCED_FACE ( 'NONE', ( #14982 ), #13582, .T. ) ;
#2280=ORIENTED_EDGE ( 'NONE', *, *, #13596, .T. ) ;
#2289=VERTEX_POINT ( 'NONE', #5677 ) ;
#2291=CARTESIAN_POINT ( 'NONE',  ( 2.790000000000076419, 2.133839912091138213, -24.22524813288759660 ) ) ;
#2292=DIRECTION ( 'NONE',  ( -1.000000000000000000, -0.000000000000000000, -0.000000000000000000 ) ) ;
#2293=CARTESIAN_POINT ( 'NONE',  ( 1.394999999999999574, 12.52377138324224148, 25.12109765559658570 ) ) ;
#2294=CARTESIAN_POINT ( 'NONE',  ( -7.680503837993603605E-14, 23.69897269326676437, 5.456611084821939350 ) ) ;
#2295=CARTESIAN_POINT ( 'NONE',  ( 0.1855656748306439008, -25.77772010606603814, -2.851997810081915663 ) ) ;
#2299=CARTESIAN_POINT ( 'NONE',  ( 0.02436607992776238310, -12.59161484032927092, 21.30679549418627161 ) ) ;
#2301=EDGE_CURVE ( 'NONE', #6946, #2063, #10610, .T. ) ;
#2303=ORIENTED_EDGE ( 'NONE', *, *, #4453, .F. ) ;
#2304=ORIENTED_EDGE ( 'NONE', *, *, #1712, .T. ) ;
#2305=ORIENTED_EDGE ( 'NONE', *, *, #376, .T. ) ;
#2306=CARTESIAN_POINT ( 'NONE',  ( 0.02436607992776281678, 2.336989772644269436, 24.63872515616083447 ) ) ;
#2315=DIRECTION ( 'NONE',  ( 1.000000000000000000, -0.000000000000000000, -0.000000000000000000 ) ) ;
#2317=ADVANCED_FACE ( 'NONE', ( #7046 ), #3504, .T. ) ;
#2318=EDGE_CURVE ( 'NONE', #13976, #8350, #7453, .T. ) ;
#2319=VECTOR ( 'NONE', #61, 1000.000000000000000 ) ;
#2324=CARTESIAN_POINT ( 'NONE',  ( 2.790000000000077751, -24.22524813288760370, -2.133839912091053836 ) ) ;
#2325=ORIENTED_EDGE ( 'NONE', *, *, #10306, .F. ) ;
#2337=CARTESIAN_POINT ( 'NONE',  ( 2.789999999999999147, -5.456805104201270851, 23.69843731927166885 ) ) ;
#2343=ADVANCED_FACE ( 'NONE', ( #11864 ), #11794, .T. ) ;
#2345=ORIENTED_EDGE ( 'NONE', *, *, #10163, .F. ) ;
#2347=DIRECTION ( 'NONE',  ( -1.000000000000000000, 0.000000000000000000, -0.000000000000000000 ) ) ;
#2349=CARTESIAN_POINT ( 'NONE',  ( 2.789999999999999147, -16.37294372382844543, -18.55949924794910544 ) ) ;
#2352=CARTESIAN_POINT ( 'NONE',  ( 0.000000000000000000, -12.52067188844335988, -20.62201879784928238 ) ) ;
#2354=ORIENTED_EDGE ( 'NONE', *, *, #6108, .T. ) ;
#2358=CARTESIAN_POINT ( 'NONE',  ( 0.000000000000000000, 15.74360496233409634, -18.28042085475261302 ) ) ;
#2360=VERTEX_POINT ( 'NONE', #12949 ) ;
#2362=CYLINDRICAL_SURFACE ( 'NONE', #1092, 13.19999999999999929 ) ;
#2363=ORIENTED_EDGE ( 'NONE', *, *, #4205, .F. ) ;
#2370=CARTESIAN_POINT ( 'NONE',  ( 2.718184743034449014, 5.344212458769360907, 24.78695292654923676 ) ) ;
#2375=TOROIDAL_SURFACE ( 'NONE', #1151, 24.12539914357697413, 8.000000000000000000 ) ;
#2381=VECTOR ( 'NONE', #10886, 1000.000000000000000 ) ;
#2384=ORIENTED_EDGE ( 'NONE', *, *, #8908, .T. ) ;
#2385=ORIENTED_EDGE ( 'NONE', *, *, #2155, .T. ) ;
#2388=AXIS2_PLACEMENT_3D ( 'NONE', #6723, #11403, #738 ) ;
#2389=B_SPLINE_CURVE_WITH_KNOTS ( 'NONE', 3,
 ( #7204, #12035, #2594, #11959 ),
 .UNSPECIFIED., .F., .F.,
 ( 4, 4 ),
 ( 2.324263106244727961E-07, 0.0006888201370294890283 ),
 .UNSPECIFIED. ) ;
#2390=FACE_OUTER_BOUND ( 'NONE', #5694, .T. ) ;
#2391=DIRECTION ( 'NONE',  ( -1.000000000000000000, 0.000000000000000000, 0.000000000000000000 ) ) ;
#2393=AXIS2_PLACEMENT_3D ( 'NONE', #1217, #10439, #7132 ) ;
#2394=CARTESIAN_POINT ( 'NONE',  ( 2.789999999999999147, -18.55949924794880346, -16.37294372382878649 ) ) ;
#2395=CIRCLE ( 'NONE', #2159, 2.524999999999995914 ) ;
#2403=ORIENTED_EDGE ( 'NONE', *, *, #11173, .F. ) ;
#2406=AXIS2_PLACEMENT_3D ( 'NONE', #11566, #11272, #2045 ) ;
#2407=EDGE_LOOP ( 'NONE', ( #8366, #13231, #9644, #13437 ) ) ;
#2413=AXIS2_PLACEMENT_3D ( 'NONE', #8905, #2769, #2926 ) ;
#2415=DIRECTION ( 'NONE',  ( -1.000000000000000000, -0.000000000000000000, -0.000000000000000000 ) ) ;
#2418=AXIS2_PLACEMENT_3D ( 'NONE', #5707, #13632, #1801 ) ;
#2423=ORIENTED_EDGE ( 'NONE', *, *, #8775, .T. ) ;
#2427=DIRECTION ( 'NONE',  ( -1.000000000000000000, 0.000000000000000000, -0.000000000000000000 ) ) ;
#2430=CARTESIAN_POINT ( 'NONE',  ( 0.000000000000000000, 7.909232158575156824, -24.34211360614291664 ) ) ;
#2431=CARTESIAN_POINT ( 'NONE',  ( 8.000000000000000000, 0.000000000000000000, 0.000000000000000000 ) ) ;
#2432=VECTOR ( 'NONE', #3661, 1000.000000000000000 ) ;
#2433=AXIS2_PLACEMENT_3D ( 'NONE', #2124, #4741, #7117 ) ;
#2434=CARTESIAN_POINT ( 'NONE',  ( 2.262072706628476926, -18.56460150496924655, -19.66369668717053898 ) ) ;
#2436=ORIENTED_EDGE ( 'NONE', *, *, #14820, .F. ) ;
#2437=FACE_BOUND ( 'NONE', #12966, .T. ) ;
#2439=DIRECTION ( 'NONE',  ( 0.000000000000000000, 0.000000000000000000, 1.000000000000000000 ) ) ;
#2446=CARTESIAN_POINT ( 'NONE',  ( 1.039999999999995817, 27.76164181293051669, 4.147968289691385202 ) ) ;
#2452=DIRECTION ( 'NONE',  ( -1.000000000000000000, -0.000000000000000000, -0.000000000000000000 ) ) ;
#2464=ORIENTED_EDGE ( 'NONE', *, *, #795, .F. ) ;
#2474=B_SPLINE_CURVE_WITH_KNOTS ( 'NONE', 3,
 ( #11763, #4784, #4713, #9321, #141, #9454 ),
 .UNSPECIFIED., .F., .F.,
 ( 4, 2, 4 ),
 ( 1.979325885386966398E-07, 0.001878588715165604951, 0.003756979497742671432 ),
 .UNSPECIFIED. ) ;
#2476=DIRECTION ( 'NONE',  ( -1.000000000000000000, 0.000000000000000000, 0.000000000000000000 ) ) ;
#2477=B_SPLINE_CURVE_WITH_KNOTS ( 'NONE', 3,
 ( #7391, #2924, #3995, #9764 ),
 .UNSPECIFIED., .F., .F.,
 ( 4, 4 ),
 ( 0.005258105385878691744, 0.005948373736081389272 ),
 .UNSPECIFIED. ) ;
#2478=ORIENTED_EDGE ( 'NONE', *, *, #10100, .F. ) ;
#2482=DIRECTION ( 'NONE',  ( -1.000000000000000000, -0.000000000000000000, -0.000000000000000000 ) ) ;
#2483=ORIENTED_EDGE ( 'NONE', *, *, #12170, .T. ) ;
#2487=CYLINDRICAL_SURFACE ( 'NONE', #9206, 2.524999999999995914 ) ;
#2488=CARTESIAN_POINT ( 'NONE',  ( 0.02436607992776021470, 21.30679549418649543, -12.59161484032888723 ) ) ;
#2490=VERTEX_POINT ( 'NONE', #3806 ) ;
#2492=DIRECTION ( 'NONE',  ( 1.000000000000000000, -0.000000000000000000, -0.000000000000000000 ) ) ;
#2497=CARTESIAN_POINT ( 'NONE',  ( 0.000000000000000000, -5.535312321042547445, -23.48180575137738302 ) ) ;
#2500=CARTESIAN_POINT ( 'NONE',  ( 1.749999999999998002, 0.000000000000000000, 0.000000000000000000 ) ) ;
#2504=CARTESIAN_POINT ( 'NONE',  ( 2.789999999999999147, 0.000000000000000000, 0.000000000000000000 ) ) ;
#2506=DIRECTION ( 'NONE',  ( 0.000000000000000000, 0.000000000000000000, 1.000000000000000000 ) ) ;
#2507=CARTESIAN_POINT ( 'NONE',  ( 2.789999999999999147, -24.44424927289185590, -0.2301004812060095106 ) ) ;
#2508=DIRECTION ( 'NONE',  ( 0.000000000000000000, -0.8090169943749488946, 0.5877852522924711387 ) ) ;
#2511=AXIS2_PLACEMENT_3D ( 'NONE', #8718, #9956, #1434 ) ;
#2519=CARTESIAN_POINT ( 'NONE',  ( 0.5279273746168618997, -26.57710921259763737, 4.996265754456265640 ) ) ;
#2524=CARTESIAN_POINT ( 'NONE',  ( 2.789999999999999147, 7.909232158574813099, 24.34211360614303388 ) ) ;
#2527=EDGE_CURVE ( 'NONE', #13334, #8127, #4234, .T. ) ;
#2529=CARTESIAN_POINT ( 'NONE',  ( 0.07181524296601557444, 18.89296398180216130, -16.91181672897712929 ) ) ;
#2532=ORIENTED_EDGE ( 'NONE', *, *, #9310, .F. ) ;
#2534=VERTEX_POINT ( 'NONE', #11102 ) ;
#2537=CARTESIAN_POINT ( 'NONE',  ( 2.601776091974069782, -25.40949241676357317, 5.251266773802275800 ) ) ;
#2538=EDGE_CURVE ( 'NONE', #1940, #7326, #14049, .T. ) ;
#2542=ORIENTED_EDGE ( 'NONE', *, *, #11030, .T. ) ;
#2552=CARTESIAN_POINT ( 'NONE',  ( 2.789999999999999147, -9.324097380959294412, -22.25075486061747654 ) ) ;
#2553=VERTEX_POINT ( 'NONE', #7583 ) ;
#2560=ORIENTED_EDGE ( 'NONE', *, *, #11056, .F. ) ;
#2565=DIRECTION ( 'NONE',  ( 0.000000000000000000, -0.5877852522924684742, -0.8090169943749507819 ) ) ;
#2569=CARTESIAN_POINT ( 'NONE',  ( 0.02436607992775891365, -24.63872515616080960, -2.336989772644527008 ) ) ;
#2576=CARTESIAN_POINT ( 'NONE',  ( 0.000000000000000000, -24.04302995059965653, -1.991882183130557094 ) ) ;
#2591=DIRECTION ( 'NONE',  ( 0.000000000000000000, 0.000000000000000000, 1.000000000000000000 ) ) ;
#2594=CARTESIAN_POINT ( 'NONE',  ( 2.790000000000079527, -15.96555658743774941, 18.34439787333500860 ) ) ;
#2597=EDGE_CURVE ( 'NONE', #860, #3207, #5585, .T. ) ;
#2599=ORIENTED_EDGE ( 'NONE', *, *, #10498, .F. ) ;
#2601=CARTESIAN_POINT ( 'NONE',  ( 0.02436607992776368414, -9.836394144775550075, -22.71065055754462492 ) ) ;
#2606=AXIS2_PLACEMENT_3D ( 'NONE', #12672, #14922, #7993 ) ;
#2609=DIRECTION ( 'NONE',  ( 0.000000000000000000, 0.000000000000000000, 1.000000000000000000 ) ) ;
#2610=VERTEX_POINT ( 'NONE', #11484 ) ;
#2613=ORIENTED_EDGE ( 'NONE', *, *, #6588, .F. ) ;
#2615=EDGE_CURVE ( 'NONE', #7149, #4429, #11088, .T. ) ;
#2626=ORIENTED_EDGE ( 'NONE', *, *, #11252, .T. ) ;
#2627=LINE ( 'NONE', #8453, #11685 ) ;
#2628=CIRCLE ( 'NONE', #155, 2.524999999999998135 ) ;
#2629=AXIS2_PLACEMENT_3D ( 'NONE', #634, #5352, #14638 ) ;
#2634=CARTESIAN_POINT ( 'NONE',  ( 2.718184767880468478, 23.19431517146933430, 10.24584646439546987 ) ) ;
#2635=ORIENTED_EDGE ( 'NONE', *, *, #2615, .F. ) ;
#2640=CARTESIAN_POINT ( 'NONE',  ( 2.765633920072241736, -9.836394144775550075, -22.71065055754462492 ) ) ;
#2644=EDGE_CURVE ( 'NONE', #8358, #1528, #8892, .T. ) ;
#2650=CARTESIAN_POINT ( 'NONE',  ( 1.749999999999998002, 4.147968289691672084, -27.76164181293047406 ) ) ;
#2655=ORIENTED_EDGE ( 'NONE', *, *, #14537, .T. ) ;
#2669=FACE_OUTER_BOUND ( 'NONE', #9939, .T. ) ;
#2673=EDGE_CURVE ( 'NONE', #5525, #1940, #4244, .T. ) ;
#2675=AXIS2_PLACEMENT_3D ( 'NONE', #1580, #13093, #8575 ) ;
#2677=DIRECTION ( 'NONE',  ( 0.000000000000000000, 0.000000000000000000, 1.000000000000000000 ) ) ;
#2679=EDGE_CURVE ( 'NONE', #12188, #5632, #12812, .T. ) ;
#2686=CARTESIAN_POINT ( 'NONE',  ( 2.789999999999999147, -15.04425356660774682, 20.70663861606266209 ) ) ;
#2689=CARTESIAN_POINT ( 'NONE',  ( 2.789999999999999147, 12.52067188844381107, -20.62201879784899461 ) ) ;
#2690=AXIS2_PLACEMENT_3D ( 'NONE', #3725, #5256, #9926 ) ;
#2691=CARTESIAN_POINT ( 'NONE',  ( 0.000000000000000000, 1.991882183130641248, -24.04302995059964942 ) ) ;
#2696=VERTEX_POINT ( 'NONE', #4432 ) ;
#2699=CARTESIAN_POINT ( 'NONE',  ( 2.718131914667133220, 10.24630254990516143, 23.19485392143217339 ) ) ;
#2704=CARTESIAN_POINT ( 'NONE',  ( -5.209999999999999964, 0.000000000000000000, 0.000000000000000000 ) ) ;
#2707=ADVANCED_FACE ( 'NONE', ( #14733 ), #15038, .T. ) ;
#2711=CARTESIAN_POINT ( 'NONE',  ( 2.262072637928883800, -23.73240184472485836, -12.96450951081243375 ) ) ;
#2712=DIRECTION ( 'NONE',  ( -1.000000000000000000, 0.000000000000000000, 0.000000000000000000 ) ) ;
#2715=B_SPLINE_CURVE_WITH_KNOTS ( 'NONE', 3,
 ( #2759, #7451, #12117, #7972, #12650, #8974 ),
 .UNSPECIFIED., .F., .F.,
 ( 4, 2, 4 ),
 ( 4.462636808902389156E-07, 0.001879885123572231200, 0.003759323983463572477 ),
 .UNSPECIFIED. ) ;
#2722=ADVANCED_FACE ( 'NONE', ( #6800 ), #6656, .F. ) ;
#2724=ORIENTED_EDGE ( 'NONE', *, *, #2527, .F. ) ;
#2734=CARTESIAN_POINT ( 'NONE',  ( 2.765633920072241736, -9.836394144775550075, -22.71065055754462492 ) ) ;
#2737=CARTESIAN_POINT ( 'NONE',  ( 0.02436607992776498519, -21.30679549418621832, -12.59161484032935618 ) ) ;
#2742=CARTESIAN_POINT ( 'NONE',  ( 2.783068930044319433, -18.43696893154769612, 16.17493693894872564 ) ) ;
#2744=ORIENTED_EDGE ( 'NONE', *, *, #2132, .F. ) ;
#2745=ORIENTED_EDGE ( 'NONE', *, *, #3571, .F. ) ;
#2756=CARTESIAN_POINT ( 'NONE',  ( 0.02436607992775544421, -22.71065055754445439, -9.836394144775947979 ) ) ;
#2758=CARTESIAN_POINT ( 'NONE',  ( 2.789999999999999147, 1.991882183130294637, 24.04302995059966364 ) ) ;
#2759=CARTESIAN_POINT ( 'NONE',  ( 1.749999999999998002, -19.67366047555545094, 20.02152543075338187 ) ) ;
#2761=FACE_OUTER_BOUND ( 'NONE', #3674, .T. ) ;
#2764=ORIENTED_EDGE ( 'NONE', *, *, #11047, .F. ) ;
#2768=AXIS2_PLACEMENT_3D ( 'NONE', #14208, #5916, #4694 ) ;
#2769=DIRECTION ( 'NONE',  ( -1.000000000000000000, -0.000000000000000000, -0.000000000000000000 ) ) ;
#2771=DIRECTION ( 'NONE',  ( 0.000000000000000000, 0.000000000000000000, 1.000000000000000000 ) ) ;
#2772=CARTESIAN_POINT ( 'NONE',  ( 2.604434514863827488, 23.63475234378997314, -10.67816411292140444 ) ) ;
#2779=CARTESIAN_POINT ( 'NONE',  ( 2.789999999999999147, 7.909232158575156824, -21.81711360614291806 ) ) ;
#2783=ORIENTED_EDGE ( 'NONE', *, *, #612, .F. ) ;
#2785=CARTESIAN_POINT ( 'NONE',  ( 2.030753616560878161, -12.05220173035456632, 24.80264696524878687 ) ) ;
#2786=CARTESIAN_POINT ( 'NONE',  ( 0.7589665283901001480, -3.797536611356509439, 27.31260702007174146 ) ) ;
#2788=LINE ( 'NONE', #10855, #6478 ) ;
#2790=CYLINDRICAL_SURFACE ( 'NONE', #2128, 2.524999999999997691 ) ;
#2800=CARTESIAN_POINT ( 'NONE',  ( 2.031033465052724196, 27.14933624560908498, 4.828387785248115627 ) ) ;
#2801=AXIS2_PLACEMENT_3D ( 'NONE', #12055, #14466, #11903 ) ;
#2802=EDGE_CURVE ( 'NONE', #12114, #8930, #826, .T. ) ;
#2807=DIRECTION ( 'NONE',  ( -1.000000000000000000, -0.000000000000000000, -0.000000000000000000 ) ) ;
#2810=CARTESIAN_POINT ( 'NONE',  ( 0.000000000000000000, 9.324097380959415204, 22.25075486061743391 ) ) ;
#2813=ORIENTED_EDGE ( 'NONE', *, *, #2248, .F. ) ;
#2818=CARTESIAN_POINT ( 'NONE',  ( 0.02436607992776411782, -24.63872515616084513, 2.336989772644183283 ) ) ;
#2825=VERTEX_POINT ( 'NONE', #8481 ) ;
#2827=FACE_OUTER_BOUND ( 'NONE', #8620, .T. ) ;
#2829=CARTESIAN_POINT ( 'NONE',  ( 1.749999999999998002, -12.96210679857804671, 24.89775460606827551 ) ) ;
#2830=CARTESIAN_POINT ( 'NONE',  ( 1.039999999999995817, 4.633866840648921404, 27.68468304288260029 ) ) ;
#2832=CARTESIAN_POINT ( 'NONE',  ( 1.039999999999996039, 19.67366047555559305, -20.02152543075323976 ) ) ;
#2833=ADVANCED_FACE ( 'NONE', ( #7022 ), #8246, .F. ) ;
#2840=CIRCLE ( 'NONE', #104, 28.06981291497571007 ) ;
#2845=DIRECTION ( 'NONE',  ( -1.000000000000000000, 0.000000000000000000, -0.000000000000000000 ) ) ;
#2851=B_SPLINE_CURVE_WITH_KNOTS ( 'NONE', 3,
 ( #1630, #5335, #12229, #10004 ),
 .UNSPECIFIED., .F., .F.,
 ( 4, 4 ),
 ( 0.005258105385878670927, 0.005948373736081390140 ),
 .UNSPECIFIED. ) ;
#2852=ORIENTED_EDGE ( 'NONE', *, *, #3382, .F. ) ;
#2853=VERTEX_POINT ( 'NONE', #5884 ) ;
#2857=TOROIDAL_SURFACE ( 'NONE', #5337, 24.12539914357697768, 8.000000000000000000 ) ;
#2861=PRODUCT_DEFINITION_CONTEXT ( 'detailed design', #4900, 'design' ) ;
#2863=FACE_OUTER_BOUND ( 'NONE', #10289, .T. ) ;
#2865=CARTESIAN_POINT ( 'NONE',  ( -5.209999999999999964, 0.000000000000000000, 0.000000000000000000 ) ) ;
#2866=DIRECTION ( 'NONE',  ( -1.000000000000000000, -0.000000000000000000, -0.000000000000000000 ) ) ;
#2868=DIRECTION ( 'NONE',  ( 0.000000000000000000, 0.000000000000000000, 1.000000000000000000 ) ) ;
#2869=B_SPLINE_CURVE_WITH_KNOTS ( 'NONE', 3,
 ( #10220, #5473, #5547, #13598, #9075, #11298 ),
 .UNSPECIFIED., .F., .F.,
 ( 4, 2, 4 ),
 ( 1.979325885420462316E-07, 0.001878588715165608420, 0.003756979497742674902 ),
 .UNSPECIFIED. ) ;
#2870=CARTESIAN_POINT ( 'NONE',  ( 1.039999999999997815, 27.68468304288265003, -4.633866840648637186 ) ) ;
#2884=EDGE_CURVE ( 'NONE', #12893, #13854, #12925, .T. ) ;
#2885=AXIS2_PLACEMENT_3D ( 'NONE', #14830, #4299, #6831 ) ;
#2888=ORIENTED_EDGE ( 'NONE', *, *, #5568, .T. ) ;
#2889=DIRECTION ( 'NONE',  ( 0.000000000000000000, 0.000000000000000000, 1.000000000000000000 ) ) ;
#2893=DIRECTION ( 'NONE',  ( -1.000000000000000000, 0.000000000000000000, 0.000000000000000000 ) ) ;
#2894=CARTESIAN_POINT ( 'NONE',  ( 2.765633920072238183, -18.55949924794904504, 16.37294372382852004 ) ) ;
#2900=AXIS2_PLACEMENT_3D ( 'NONE', #9533, #14382, #8301 ) ;
#2901=CARTESIAN_POINT ( 'NONE',  ( 2.765633920072238183, 2.336989772644269436, 24.63872515616083447 ) ) ;
#2909=DIRECTION ( 'NONE',  ( -1.000000000000000000, -0.000000000000000000, -0.000000000000000000 ) ) ;
#2910=ORIENTED_EDGE ( 'NONE', *, *, #3691, .T. ) ;
#2912=DIRECTION ( 'NONE',  ( 0.000000000000000000, 0.000000000000000000, 1.000000000000000000 ) ) ;
#2913=EDGE_CURVE ( 'NONE', #8078, #6064, #6238, .T. ) ;
#2914=CARTESIAN_POINT ( 'NONE',  ( 1.039999999999995373, -12.96210679857767900, -24.89775460606846380 ) ) ;
#2916=ORIENTED_EDGE ( 'NONE', *, *, #163, .T. ) ;
#2922=EDGE_LOOP ( 'NONE', ( #11069, #10023, #658, #4273, #10697, #2464 ) ) ;
#2924=CARTESIAN_POINT ( 'NONE',  ( 2.789999999999999147, -9.514945144208585504, -22.37986894186682107 ) ) ;
#2926=DIRECTION ( 'NONE',  ( 0.000000000000000000, 0.000000000000000000, 1.000000000000000000 ) ) ;
#2927=FACE_OUTER_BOUND ( 'NONE', #11823, .T. ) ;
#2931=VECTOR ( 'NONE', #1289, 1000.000000000000000 ) ;
#2934=VERTEX_POINT ( 'NONE', #4085 ) ;
#2935=CARTESIAN_POINT ( 'NONE',  ( 2.262072625383134916, -26.57710921259758408, -4.996265754456650221 ) ) ;
#2938=ORIENTED_EDGE ( 'NONE', *, *, #2248, .T. ) ;
#2939=AXIS2_PLACEMENT_3D ( 'NONE', #3535, #12830, #11606 ) ;
#2941=CARTESIAN_POINT ( 'NONE',  ( 2.718184757033982546, 16.91181672897760535, -18.89296398180173497 ) ) ;
#2944=ORIENTED_EDGE ( 'NONE', *, *, #6661, .F. ) ;
#2946=CARTESIAN_POINT ( 'NONE',  ( -5.209999999999999964, 0.000000000000000000, 0.000000000000000000 ) ) ;
#2951=CARTESIAN_POINT ( 'NONE',  ( 0.000000000000000000, -18.28042085475288303, 15.74360496233377305 ) ) ;
#2962=ORIENTED_EDGE ( 'NONE', *, *, #13779, .T. ) ;
#2963=DIRECTION ( 'NONE',  ( -1.000000000000000000, 0.000000000000000000, 0.000000000000000000 ) ) ;
#2965=ORIENTED_EDGE ( 'NONE', *, *, #10146, .T. ) ;
#2973=CARTESIAN_POINT ( 'NONE',  ( 0.02436607992775934733, -2.336989772644440855, 24.63872515616082026 ) ) ;
#2979=CARTESIAN_POINT ( 'NONE',  ( 2.789999999999999147, -14.18181402625728360, -19.91106274590529068 ) ) ;
#2981=ORIENTED_EDGE ( 'NONE', *, *, #10353, .T. ) ;
#2983=EDGE_CURVE ( 'NONE', #6106, #14255, #4870, .T. ) ;
#2984=CARTESIAN_POINT ( 'NONE',  ( 2.789999999999999147, 23.31896751603342821, -7.334849878007252855 ) ) ;
#2989=CYLINDRICAL_SURFACE ( 'NONE', #12160, 13.19999999999999929 ) ;
#2990=EDGE_LOOP ( 'NONE', ( #6073, #12287, #2136, #1334, #14701, #11260, #2012, #5617 ) ) ;
#2995=DIRECTION ( 'NONE',  ( 0.000000000000000000, 0.000000000000000000, 1.000000000000000000 ) ) ;
#2999=CARTESIAN_POINT ( 'NONE',  ( 0.7589665326895889130, -12.98167595241004335, -24.32849926382764849 ) ) ;
#3007=B_SPLINE_CURVE_WITH_KNOTS ( 'NONE', 3,
 ( #12550, #2025, #2324, #13934 ),
 .UNSPECIFIED., .F., .F.,
 ( 4, 4 ),
 ( 2.135345996541640089E-07, 0.0006888010880211291841 ),
 .UNSPECIFIED. ) ;
#3009=AXIS2_PLACEMENT_3D ( 'NONE', #6497, #8950, #2036 ) ;
#3010=VERTEX_POINT ( 'NONE', #5408 ) ;
#3017=DIRECTION ( 'NONE',  ( 0.000000000000000000, 0.000000000000000000, 1.000000000000000000 ) ) ;
#3021=DIRECTION ( 'NONE',  ( -1.000000000000000000, -0.000000000000000000, -0.000000000000000000 ) ) ;
#3032=CARTESIAN_POINT ( 'NONE',  ( 0.000000000000000000, 25.59481291497571220, 0.000000000000000000 ) ) ;
#3033=ORIENTED_EDGE ( 'NONE', *, *, #5415, .T. ) ;
#3034=B_SPLINE_CURVE_WITH_KNOTS ( 'NONE', 3,
 ( #5382, #9970, #11114, #11415 ),
 .UNSPECIFIED., .F., .F.,
 ( 4, 4 ),
 ( 2.135345996175604595E-07, 0.0006888010880210905865 ),
 .UNSPECIFIED. ) ;
#3036=EDGE_CURVE ( 'NONE', #4328, #4113, #10076, .T. ) ;
#3037=ORIENTED_EDGE ( 'NONE', *, *, #10499, .T. ) ;
#3039=CARTESIAN_POINT ( 'NONE',  ( 50.00050000000000239, 0.000000000000000000, 0.000000000000000000 ) ) ;
#3043=EDGE_LOOP ( 'NONE', ( #248, #14283, #9269, #1352 ) ) ;
#3046=FACE_OUTER_BOUND ( 'NONE', #4669, .T. ) ;
#3047=CARTESIAN_POINT ( 'NONE',  ( 2.765633920072235963, 22.71065055754452544, 9.836394144775786330 ) ) ;
#3050=CARTESIAN_POINT ( 'NONE',  ( 1.749999999999998002, -20.02152543075331081, -19.67366047555553266 ) ) ;
#3051=AXIS2_PLACEMENT_3D ( 'NONE', #4167, #9628, #4886 ) ;
#3052=CARTESIAN_POINT ( 'NONE',  ( 2.789999999999999147, 16.37294372382858398, 18.55949924794898465 ) ) ;
#3055=ADVANCED_FACE ( 'NONE', ( #166 ), #333, .T. ) ;
#3058=CARTESIAN_POINT ( 'NONE',  ( 2.789999999999999147, -23.17675759782035172, -7.772527002114682837 ) ) ;
#3061=DIRECTION ( 'NONE',  ( -1.000000000000000000, -0.000000000000000000, -0.000000000000000000 ) ) ;
#3062=EDGE_CURVE ( 'NONE', #11582, #4228, #68, .T. ) ;
#3063=TOROIDAL_SURFACE ( 'NONE', #6730, 24.12539914357697413, 8.000000000000000000 ) ;
#3065=EDGE_LOOP ( 'NONE', ( #3423, #10026, #12566, #13144, #8333, #3269 ) ) ;
#3076=CARTESIAN_POINT ( 'NONE',  ( 2.789999999999999147, -1.991882183130462503, 24.04302995059964942 ) ) ;
#3082=ORIENTED_EDGE ( 'NONE', *, *, #13303, .T. ) ;
#3083=CARTESIAN_POINT ( 'NONE',  ( 1.039999999999995373, 25.12109765559670649, -12.52377138324197681 ) ) ;
#3088=EDGE_CURVE ( 'NONE', #8921, #6027, #9671, .T. ) ;
#3089=( NAMED_UNIT ( * ) SI_UNIT ( $, .STERADIAN. ) SOLID_ANGLE_UNIT ( ) );
#3090=CIRCLE ( 'NONE', #7006, 24.12539914357697768 ) ;
#3099=CARTESIAN_POINT ( 'NONE',  ( -5.209999999999999964, 0.000000000000000000, 0.000000000000000000 ) ) ;
#3100=AXIS2_PLACEMENT_3D ( 'NONE', #5086, #10980, #12048 ) ;
#3102=CARTESIAN_POINT ( 'NONE',  ( 2.257825491203655055, -11.58891744060124473, 24.44564404695840665 ) ) ;
#3105=LINE ( 'NONE', #5648, #13811 ) ;
#3113=ORIENTED_EDGE ( 'NONE', *, *, #10497, .T. ) ;
#3114=CARTESIAN_POINT ( 'NONE',  ( 8.000000000000000000, 0.000000000000000000, 0.000000000000000000 ) ) ;
#3115=LINE ( 'NONE', #11325, #7987 ) ;
#3119=CIRCLE ( 'NONE', #8498, 2.524999999999998135 ) ;
#3122=ORIENTED_EDGE ( 'NONE', *, *, #14648, .T. ) ;
#3123=CARTESIAN_POINT ( 'NONE',  ( 1.749999999999998002, 24.89775460606851354, -12.96210679857759729 ) ) ;
#3129=EDGE_LOOP ( 'NONE', ( #8096, #6258, #6785, #2613, #8197, #2655 ) ) ;
#3130=CIRCLE ( 'NONE', #9752, 2.524999999999996803 ) ;
#3131=EDGE_LOOP ( 'NONE', ( #11039, #2236, #4649, #15148 ) ) ;
#3134=DIRECTION ( 'NONE',  ( 0.000000000000000000, 0.000000000000000000, 1.000000000000000000 ) ) ;
#3136=CIRCLE ( 'NONE', #2885, 28.06981291497571362 ) ;
#3137=CARTESIAN_POINT ( 'NONE',  ( 2.789999999999999147, 9.324097380959765147, -22.25075486061728824 ) ) ;
#3138=CARTESIAN_POINT ( 'NONE',  ( 0.07181525696555295102, -5.344212458769539431, 24.78695292654919768 ) ) ;
#3146=EDGE_LOOP ( 'NONE', ( #2363, #4011, #8226, #1875, #3971, #5105, #9866 ) ) ;
#3149=CARTESIAN_POINT ( 'NONE',  ( 2.790000000000000924, 0.000000000000000000, 0.000000000000000000 ) ) ;
#3155=CARTESIAN_POINT ( 'NONE',  ( 2.031033491000350466, -24.80232951178386713, 12.05173163741713083 ) ) ;
#3160=CARTESIAN_POINT ( 'NONE',  ( 2.765633920072235963, -5.391175441198450713, -24.15498966839968276 ) ) ;
#3161=CIRCLE ( 'NONE', #2413, 24.12539914357697413 ) ;
#3162=CARTESIAN_POINT ( 'NONE',  ( 0.1882238552569851786, -23.64332819722389090, 10.68696068830398360 ) ) ;
#3166=AXIS2_PLACEMENT_3D ( 'NONE', #8480, #5049, #14647 ) ;
#3176=CIRCLE ( 'NONE', #2675, 2.524999999999996803 ) ;
#3179=CARTESIAN_POINT ( 'NONE',  ( 1.749999999999998002, -12.96210679857804671, 24.89775460606827551 ) ) ;
#3184=ADVANCED_FACE ( 'NONE', ( #2160 ), #6846, .T. ) ;
#3188=CARTESIAN_POINT ( 'NONE',  ( 0.7592463941534238758, 3.797885586973211325, 27.31305418910211458 ) ) ;
#3190=CARTESIAN_POINT ( 'NONE',  ( 0.02436607992776194942, -5.391175441198450713, -24.15498966839968276 ) ) ;
#3191=DIRECTION ( 'NONE',  ( -1.000000000000000000, -0.000000000000000000, -0.000000000000000000 ) ) ;
#3193=ORIENTED_EDGE ( 'NONE', *, *, #7385, .F. ) ;
#3194=DIRECTION ( 'NONE',  ( 0.000000000000000000, 0.000000000000000000, 1.000000000000000000 ) ) ;
#3200=EDGE_CURVE ( 'NONE', #11548, #15218, #8496, .T. ) ;
#3203=CARTESIAN_POINT ( 'NONE',  ( 2.789999999999999147, -24.15498966839966855, 5.391175441198523544 ) ) ;
#3204=ORIENTED_EDGE ( 'NONE', *, *, #7686, .F. ) ;
#3205=CARTESIAN_POINT ( 'NONE',  ( 2.718184745196085661, 12.74223776959200727, 21.92234060054350309 ) ) ;
#3207=VERTEX_POINT ( 'NONE', #10225 ) ;
#3214=LINE ( 'NONE', #9275, #1336 ) ;
#3217=B_SPLINE_CURVE_WITH_KNOTS ( 'NONE', 3,
 ( #12126, #1838, #8604, #10986 ),
 .UNSPECIFIED., .F., .F.,
 ( 4, 4 ),
 ( 0.005258120783916782857, 0.005948386350302925507 ),
 .UNSPECIFIED. ) ;
#3227=CARTESIAN_POINT ( 'NONE',  ( 2.718131914667132776, -23.19485392143220182, 10.24630254990507083 ) ) ;
#3231=CARTESIAN_POINT ( 'NONE',  ( 0.02436607992776194942, -5.391175441198450713, -24.15498966839968276 ) ) ;
#3232=DIRECTION ( 'NONE',  ( 0.000000000000000000, 0.000000000000000000, 1.000000000000000000 ) ) ;
#3233=CARTESIAN_POINT ( 'NONE',  ( 0.1882238552569850676, 23.64332819722396195, -10.68696068830383084 ) ) ;
#3234=CARTESIAN_POINT ( 'NONE',  ( 2.071132347512118166, 24.19190980169967631, 12.96989951879416658 ) ) ;
#3240=B_SPLINE_CURVE_WITH_KNOTS ( 'NONE', 3,
 ( #13429, #6363, #1600, #14521, #9662, #14361 ),
 .UNSPECIFIED., .F., .F.,
 ( 4, 2, 4 ),
 ( 2.321268216997177022E-07, 0.001878622960950496190, 0.003757013795079292354 ),
 .UNSPECIFIED. ) ;
#3245=CARTESIAN_POINT ( 'NONE',  ( 0.02436607992776758727, 24.15498966839963302, 5.391175441198700291 ) ) ;
#3247=DIRECTION ( 'NONE',  ( -1.000000000000000000, -0.000000000000000000, 0.000000000000000000 ) ) ;
#3250=DIRECTION ( 'NONE',  ( -1.000000000000000000, -0.000000000000000000, -0.000000000000000000 ) ) ;
#3253=CARTESIAN_POINT ( 'NONE',  ( 0.7188676524878460095, -24.19190980169966210, 12.96989951879399428 ) ) ;
#3267=ORIENTED_EDGE ( 'NONE', *, *, #8626, .F. ) ;
#3269=ORIENTED_EDGE ( 'NONE', *, *, #8754, .F. ) ;
#3276=DIRECTION ( 'NONE',  ( 0.000000000000000000, 0.000000000000000000, 1.000000000000000000 ) ) ;
#3280=CARTESIAN_POINT ( 'NONE',  ( 2.790000000000000036, -15.96500990068111214, -18.34424029220128816 ) ) ;
#3281=EDGE_CURVE ( 'NONE', #8350, #929, #1537, .T. ) ;
#3282=ORIENTED_EDGE ( 'NONE', *, *, #12297, .F. ) ;
#3284=CARTESIAN_POINT ( 'NONE',  ( 0.000000000000000000, -9.324097380959319281, -22.25075486061748009 ) ) ;
#3288=CARTESIAN_POINT ( 'NONE',  ( 2.789999999999999147, -9.836394144775869819, 22.71065055754449347 ) ) ;
#3289=CARTESIAN_POINT ( 'NONE',  ( 2.262072625383134472, 4.996265754456739927, -26.57710921259756631 ) ) ;
#3293=FACE_OUTER_BOUND ( 'NONE', #3911, .T. ) ;
#3296=CIRCLE ( 'NONE', #9414, 24.12539914357697413 ) ;
#3297=CARTESIAN_POINT ( 'NONE',  ( 2.765633920072239516, 16.37294372382858398, 18.55949924794898465 ) ) ;
#3301=CARTESIAN_POINT ( 'NONE',  ( 2.765633920072239516, 21.30679549418631780, 12.59161484032919986 ) ) ;
#3303=VERTEX_POINT ( 'NONE', #12044 ) ;
#3307=ORIENTED_EDGE ( 'NONE', *, *, #9380, .T. ) ;
#3310=EDGE_LOOP ( 'NONE', ( #3692, #3204, #9881, #5251, #9880, #10633, #6463 ) ) ;
#3312=TOROIDAL_SURFACE ( 'NONE', #7236, 24.12539914357697768, 8.000000000000000000 ) ;
#3314=CIRCLE ( 'NONE', #11891, 24.12539914357697413 ) ;
#3315=DIRECTION ( 'NONE',  ( -1.000000000000000000, -0.000000000000000000, -0.000000000000000000 ) ) ;
#3321=CARTESIAN_POINT ( 'NONE',  ( 0.02436607992776368414, 18.55949924794916228, -16.37294372382838148 ) ) ;
#3322=AXIS2_PLACEMENT_3D ( 'NONE', #14871, #4342, #3194 ) ;
#3323=CIRCLE ( 'NONE', #7734, 2.524999999999995914 ) ;
#3324=CARTESIAN_POINT ( 'NONE',  ( 2.765633920072239516, 21.30679549418631780, 12.59161484032919986 ) ) ;
#3332=ORIENTED_EDGE ( 'NONE', *, *, #5735, .F. ) ;
#3335=ORIENTED_EDGE ( 'NONE', *, *, #1686, .F. ) ;
#3337=CARTESIAN_POINT ( 'NONE',  ( 2.783025342027734883, 23.92335783895644852, -5.408388659523843067 ) ) ;
#3339=B_SPLINE_CURVE_WITH_KNOTS ( 'NONE', 3,
 ( #10741, #14044, #2291, #198 ),
 .UNSPECIFIED., .F., .F.,
 ( 4, 4 ),
 ( 2.135345996700793610E-07, 0.0006888010880211471818 ),
 .UNSPECIFIED. ) ;
#3340=ORIENTED_EDGE ( 'NONE', *, *, #297, .F. ) ;
#3341=AXIS2_PLACEMENT_3D ( 'NONE', #9065, #5610, #8898 ) ;
#3345=VERTEX_POINT ( 'NONE', #4150 ) ;
#3348=CARTESIAN_POINT ( 'NONE',  ( 2.789999999999999147, -7.334849878007332791, -23.31896751603339979 ) ) ;
#3349=AXIS2_PLACEMENT_3D ( 'NONE', #12201, #6369, #2912 ) ;
#3357=CARTESIAN_POINT ( 'NONE',  ( 2.604434325169353137, -25.77772010606608077, 2.851997810081559503 ) ) ;
#3358=VECTOR ( 'NONE', #1037, 1000.000000000000000 ) ;
#3362=CARTESIAN_POINT ( 'NONE',  ( 0.7592463896980037319, 19.12676442129342647, 19.86438386685667368 ) ) ;
#3363=FACE_OUTER_BOUND ( 'NONE', #11153, .T. ) ;
#3366=VECTOR ( 'NONE', #10430, 1000.000000000000000 ) ;
#3369=CARTESIAN_POINT ( 'NONE',  ( 0.02436607992775544421, -22.71065055754445439, -9.836394144775947979 ) ) ;
#3373=VECTOR ( 'NONE', #12808, 1000.000000000000000 ) ;
#3382=EDGE_CURVE ( 'NONE', #5968, #13607, #6738, .T. ) ;
#3384=EDGE_LOOP ( 'NONE', ( #13328, #11974, #808, #11831, #14932, #8297 ) ) ;
#3385=CARTESIAN_POINT ( 'NONE',  ( 8.000000000000000000, 0.000000000000000000, 0.000000000000000000 ) ) ;
#3386=VECTOR ( 'NONE', #10740, 1000.000000000000000 ) ;
#3388=ADVANCED_FACE ( 'NONE', ( #8739 ), #4542, .T. ) ;
#3390=VERTEX_POINT ( 'NONE', #440 ) ;
#3391=CIRCLE ( 'NONE', #10264, 2.524999999999995914 ) ;
#3392=VERTEX_POINT ( 'NONE', #13516 ) ;
#3394=VERTEX_POINT ( 'NONE', #2914 ) ;
#3397=B_SPLINE_CURVE_WITH_KNOTS ( 'NONE', 3,
 ( #5910, #39, #322, #4752, #9422, #2446 ),
 .UNSPECIFIED., .F., .F.,
 ( 4, 2, 4 ),
 ( 2.132675795046084789E-07, 0.001878604073277003903, 0.003756994878974503470 ),
 .UNSPECIFIED. ) ;
#3398=AXIS2_PLACEMENT_3D ( 'NONE', #6412, #325, #13321 ) ;
#3403=VERTEX_POINT ( 'NONE', #2691 ) ;
#3410=VERTEX_POINT ( 'NONE', #2832 ) ;
#3412=EDGE_CURVE ( 'NONE', #269, #13647, #6561, .T. ) ;
#3415=CYLINDRICAL_SURFACE ( 'NONE', #1088, 13.19999999999999929 ) ;
#3416=CARTESIAN_POINT ( 'NONE',  ( 1.749999999999998002, 0.000000000000000000, 0.000000000000000000 ) ) ;
#3419=DIRECTION ( 'NONE',  ( -1.000000000000000000, -0.000000000000000000, 0.000000000000000000 ) ) ;
#3422=LINE ( 'NONE', #10635, #3358 ) ;
#3423=ORIENTED_EDGE ( 'NONE', *, *, #11, .F. ) ;
#3424=ORIENTED_EDGE ( 'NONE', *, *, #817, .T. ) ;
#3427=CARTESIAN_POINT ( 'NONE',  ( 2.765633920072235963, 21.30679549418649543, -12.59161484032888723 ) ) ;
#3428=CARTESIAN_POINT ( 'NONE',  ( -10.00000000000000000, 0.000000000000000000, 0.000000000000000000 ) ) ;
#3429=CYLINDRICAL_SURFACE ( 'NONE', #5543, 2.524999999999995914 ) ;
#3432=EDGE_CURVE ( 'NONE', #9629, #10133, #2715, .T. ) ;
#3434=DIRECTION ( 'NONE',  ( 0.000000000000000000, 0.000000000000000000, 1.000000000000000000 ) ) ;
#3438=CARTESIAN_POINT ( 'NONE',  ( -7.722669826818730404E-14, -20.65026423218563778, -12.51972477286604502 ) ) ;
#3443=ORIENTED_EDGE ( 'NONE', *, *, #11, .T. ) ;
#3446=B_SPLINE_CURVE_WITH_KNOTS ( 'NONE', 3,
 ( #11947, #14270, #3438, #13022 ),
 .UNSPECIFIED., .F., .F.,
 ( 4, 4 ),
 ( 0.0006045424356928436873, 0.0006887909409525051459 ),
 .UNSPECIFIED. ) ;
#3447=CARTESIAN_POINT ( 'NONE',  ( 1.749999999999998002, -4.633866840649122132, 27.68468304288257542 ) ) ;
#3450=PRODUCT_DEFINITION ( 'UNKNOWN', '', #569, #2861 ) ;
#3454=DIRECTION ( 'NONE',  ( -1.000000000000000000, 0.000000000000000000, 0.000000000000000000 ) ) ;
#3458=VERTEX_POINT ( 'NONE', #12433 ) ;
#3462=ORIENTED_EDGE ( 'NONE', *, *, #3631, .T. ) ;
#3467=EDGE_CURVE ( 'NONE', #6106, #3458, #821, .T. ) ;
#3468=CARTESIAN_POINT ( 'NONE',  ( 2.790000000000000480, -12.51294990530030837, 20.85230829256849105 ) ) ;
#3472=B_SPLINE_CURVE_WITH_KNOTS ( 'NONE', 3,
 ( #7267, #11939, #1427, #6118, #254, #12021 ),
 .UNSPECIFIED., .F., .F.,
 ( 4, 2, 4 ),
 ( 4.462636678151279571E-07, 0.001879885020955181143, 0.003759323778242547407 ),
 .UNSPECIFIED. ) ;
#3475=CARTESIAN_POINT ( 'NONE',  ( 0.000000000000000000, 0.000000000000000000, 0.000000000000000000 ) ) ;
#3486=EDGE_LOOP ( 'NONE', ( #6728, #10370, #984, #12353, #12284, #1331 ) ) ;
#3487=CYLINDRICAL_SURFACE ( 'NONE', #916, 13.19999999999999929 ) ;
#3490=AXIS2_PLACEMENT_3D ( 'NONE', #3039, #7727, #13640 ) ;
#3491=B_SPLINE_CURVE_WITH_KNOTS ( 'NONE', 3,
 ( #9647, #5140, #8719, #13413 ),
 .UNSPECIFIED., .F., .F.,
 ( 4, 4 ),
 ( 0.005258110598983623853, 0.005948376585272730464 ),
 .UNSPECIFIED. ) ;
#3498=CARTESIAN_POINT ( 'NONE',  ( 2.031033479673587827, -19.12621924769852555, -19.86422722021333342 ) ) ;
#3499=EDGE_CURVE ( 'NONE', #14244, #8705, #2134, .T. ) ;
#3504=CYLINDRICAL_SURFACE ( 'NONE', #7170, 13.19999999999999929 ) ;
#3505=CARTESIAN_POINT ( 'NONE',  ( 0.02436607992776325046, 16.37294372382858398, 18.55949924794898465 ) ) ;
#3506=CARTESIAN_POINT ( 'NONE',  ( 2.601776105308176046, -2.857713464478872201, 25.78859396478526733 ) ) ;
#3513=ADVANCED_FACE ( 'NONE', ( #3363 ), #1991, .F. ) ;
#3516=CARTESIAN_POINT ( 'NONE',  ( 2.257825459230520693, 4.993157874727810253, 26.58873630738054317 ) ) ;
#3519=LINE ( 'NONE', #122, #5871 ) ;
#3530=CARTESIAN_POINT ( 'NONE',  ( 1.749999999999998002, 12.52377138324224148, 25.12109765559658570 ) ) ;
#3532=DIRECTION ( 'NONE',  ( -1.000000000000000000, -0.000000000000000000, 0.000000000000000000 ) ) ;
#3533=AXIS2_PLACEMENT_3D ( 'NONE', #295, #11065, #6154 ) ;
#3535=CARTESIAN_POINT ( 'NONE',  ( 1.749999999999998002, 0.000000000000000000, 0.000000000000000000 ) ) ;
#3540=CIRCLE ( 'NONE', #12131, 28.06981291497571362 ) ;
#3543=ADVANCED_FACE ( 'NONE', ( #10130 ), #4519, .F. ) ;
#3544=AXIS2_PLACEMENT_3D ( 'NONE', #13528, #11436, #5401 ) ;
#3546=DIRECTION ( 'NONE',  ( -1.000000000000000000, -0.000000000000000000, -0.000000000000000000 ) ) ;
#3547=CARTESIAN_POINT ( 'NONE',  ( 2.601776144743011443, 23.64332819722380918, 10.68696068830415946 ) ) ;
#3548=EDGE_LOOP ( 'NONE', ( #4531, #12212, #1113, #2483 ) ) ;
#3554=VECTOR ( 'NONE', #4422, 1000.000000000000000 ) ;
#3557=ADVANCED_FACE ( 'NONE', ( #15213 ), #7048, .T. ) ;
#3558=EDGE_CURVE ( 'NONE', #567, #11124, #3446, .T. ) ;
#3565=EDGE_LOOP ( 'NONE', ( #8398, #13054, #920, #722, #4895, #4828 ) ) ;
#3571=EDGE_CURVE ( 'NONE', #7839, #8603, #1242, .T. ) ;
#3573=CARTESIAN_POINT ( 'NONE',  ( 2.765633920072239071, -16.37294372382844543, -18.55949924794910544 ) ) ;
#3575=LINE ( 'NONE', #4676, #13996 ) ;
#3576=B_SPLINE_CURVE_WITH_KNOTS ( 'NONE', 3,
 ( #12539, #9089, #938, #8004, #2016, #3179 ),
 .UNSPECIFIED., .F., .F.,
 ( 4, 2, 4 ),
 ( 2.032124546189621919E-07, 0.001878594002992309232, 0.003756984793529999193 ),
 .UNSPECIFIED. ) ;
#3579=CARTESIAN_POINT ( 'NONE',  ( 2.030753610301991419, 19.86438386685660618, 19.12676442129351173 ) ) ;
#3580=DIRECTION ( 'NONE',  ( 0.000000000000000000, 0.000000000000000000, 1.000000000000000000 ) ) ;
#3583=ORIENTED_EDGE ( 'NONE', *, *, #13023, .T. ) ;
#3587=DIRECTION ( 'NONE',  ( 0.000000000000000000, 0.000000000000000000, 1.000000000000000000 ) ) ;
#3600=AXIS2_PLACEMENT_3D ( 'NONE', #7549, #13371, #3936 ) ;
#3605=AXIS2_PLACEMENT_3D ( 'NONE', #10744, #2292, #9657 ) ;
#3608=ORIENTED_EDGE ( 'NONE', *, *, #7856, .F. ) ;
#3609=ORIENTED_EDGE ( 'NONE', *, *, #9159, .T. ) ;
#3611=CARTESIAN_POINT ( 'NONE',  ( 0.000000000000000000, 18.28042085475300382, -15.74360496233363804 ) ) ;
#3628=ORIENTED_EDGE ( 'NONE', *, *, #2041, .F. ) ;
#3631=EDGE_CURVE ( 'NONE', #9813, #6366, #10226, .T. ) ;
#3633=ADVANCED_FACE ( 'NONE', ( #6125 ), #13095, .F. ) ;
#3635=B_SPLINE_CURVE_WITH_KNOTS ( 'NONE', 3,
 ( #8551, #14320, #10928, #13310, #2786, #7481 ),
 .UNSPECIFIED., .F., .F.,
 ( 4, 2, 4 ),
 ( 2.132675795041204291E-07, 0.001878604073277003036, 0.003756994878974502169 ),
 .UNSPECIFIED. ) ;
#3637=CARTESIAN_POINT ( 'NONE',  ( 0.0003207540509378258692, 20.70663861606293921, -12.51925356660738053 ) ) ;
#3655=VECTOR ( 'NONE', #14978, 1000.000000000000000 ) ;
#3658=ORIENTED_EDGE ( 'NONE', *, *, #505, .F. ) ;
#3659=DIRECTION ( 'NONE',  ( -1.000000000000000000, -0.000000000000000000, -0.000000000000000000 ) ) ;
#3661=DIRECTION ( 'NONE',  ( -1.000000000000000000, -0.000000000000000000, 0.000000000000000000 ) ) ;
#3663=EDGE_CURVE ( 'NONE', #13730, #626, #6004, .T. ) ;
#3667=ORIENTED_EDGE ( 'NONE', *, *, #10596, .T. ) ;
#3669=CARTESIAN_POINT ( 'NONE',  ( 1.749999999999998002, -19.67366047555545094, 20.02152543075338187 ) ) ;
#3673=DIRECTION ( 'NONE',  ( 0.000000000000000000, -0.9510565162951523099, -0.3090169943749515591 ) ) ;
#3674=EDGE_LOOP ( 'NONE', ( #3766, #7349, #5852, #11321, #11991, #9247 ) ) ;
#3675=FACE_OUTER_BOUND ( 'NONE', #4958, .T. ) ;
#3678=ORIENTED_EDGE ( 'NONE', *, *, #13035, .T. ) ;
#3686=CARTESIAN_POINT ( 'NONE',  ( -7.664413047240269201E-14, 2.133839912090805147, 24.22524813288763568 ) ) ;
#3689=B_SPLINE_CURVE_WITH_KNOTS ( 'NONE', 3,
 ( #4833, #14122, #10659, #4918 ),
 .UNSPECIFIED., .F., .F.,
 ( 4, 4 ),
 ( 1.981826382900847025E-07, 0.0006887856082032273912 ),
 .UNSPECIFIED. ) ;
#3691=EDGE_CURVE ( 'NONE', #929, #6042, #7779, .T. ) ;
#3692=ORIENTED_EDGE ( 'NONE', *, *, #6049, .F. ) ;
#3695=CARTESIAN_POINT ( 'NONE',  ( 0.02436607992775717893, -9.836394144775869819, 22.71065055754449347 ) ) ;
#3698=CARTESIAN_POINT ( 'NONE',  ( 2.765633920072235963, 22.71065055754452544, 9.836394144775786330 ) ) ;
#3699=ORIENTED_EDGE ( 'NONE', *, *, #5310, .T. ) ;
#3705=EDGE_CURVE ( 'NONE', #4798, #8127, #148, .T. ) ;
#3711=B_SPLINE_CURVE_WITH_KNOTS ( 'NONE', 3,
 ( #10055, #11697, #10485, #4657 ),
 .UNSPECIFIED., .F., .F.,
 ( 4, 4 ),
 ( 0.005258214619651972732, 0.005948481662034169060 ),
 .UNSPECIFIED. ) ;
#3712=CARTESIAN_POINT ( 'NONE',  ( 0.02436607992775674525, 9.836394144776026138, -22.71065055754441531 ) ) ;
#3716=EDGE_CURVE ( 'NONE', #5643, #6579, #13714, .T. ) ;
#3721=CARTESIAN_POINT ( 'NONE',  ( -1.906188514513426096E-16, -24.22479935914659066, -2.133490293297270579 ) ) ;
#3723=CARTESIAN_POINT ( 'NONE',  ( 1.039999999999997593, 0.000000000000000000, 0.000000000000000000 ) ) ;
#3725=CARTESIAN_POINT ( 'NONE',  ( 2.789999999999999147, 25.59481291497571220, 0.000000000000000000 ) ) ;
#3726=LINE ( 'NONE', #11029, #10256 ) ;
#3727=ORIENTED_EDGE ( 'NONE', *, *, #1057, .F. ) ;
#3730=CYLINDRICAL_SURFACE ( 'NONE', #8311, 13.20000000000000284 ) ;
#3740=CARTESIAN_POINT ( 'NONE',  ( 2.790000000000000924, 4.898587196589412829E-16, -4.000000000000000000 ) ) ;
#3743=CARTESIAN_POINT ( 'NONE',  ( 0.7589665349472695111, -27.14933624560910630, 4.828387785247921116 ) ) ;
#3758=ORIENTED_EDGE ( 'NONE', *, *, #9652, .F. ) ;
#3766=ORIENTED_EDGE ( 'NONE', *, *, #9932, .F. ) ;
#3767=CARTESIAN_POINT ( 'NONE',  ( 0.000000000000000000, 12.52067188844351442, 20.62201879784919001 ) ) ;
#3772=EDGE_CURVE ( 'NONE', #7850, #8078, #9673, .T. ) ;
#3782=CIRCLE ( 'NONE', #4789, 2.524999999999996803 ) ;
#3783=ADVANCED_FACE ( 'NONE', ( #7508 ), #1665, .T. ) ;
#3784=CARTESIAN_POINT ( 'NONE',  ( 2.783068930044318545, 16.17493693894878604, 18.43696893154764282 ) ) ;
#3786=AXIS2_PLACEMENT_3D ( 'NONE', #1699, #1622, #375 ) ;
#3791=DIRECTION ( 'NONE',  ( -1.000000000000000000, 0.000000000000000000, 0.000000000000000000 ) ) ;
#3792=VERTEX_POINT ( 'NONE', #5509 ) ;
#3799=MECHANICAL_DESIGN_GEOMETRIC_PRESENTATION_REPRESENTATION('',(#15102),#616);
#3803=DIRECTION ( 'NONE',  ( 0.000000000000000000, 0.000000000000000000, 1.000000000000000000 ) ) ;
#3804=ORIENTED_EDGE ( 'NONE', *, *, #14274, .F. ) ;
#3806=CARTESIAN_POINT ( 'NONE',  ( 0.02436607992776238310, -2.336989772644097574, -24.63872515616085224 ) ) ;
#3809=CARTESIAN_POINT ( 'NONE',  ( 0.006974771092478231072, 9.686319561460942751, 22.53337530003406997 ) ) ;
#3811=ORIENTED_EDGE ( 'NONE', *, *, #4323, .T. ) ;
#3812=CIRCLE ( 'NONE', #6519, 28.06981291497571362 ) ;
#3817=CARTESIAN_POINT ( 'NONE',  ( 0.7589665089996505687, 12.05173163741758380, -24.80232951178364686 ) ) ;
#3825=CARTESIAN_POINT ( 'NONE',  ( 8.000000000000000000, 0.000000000000000000, 0.000000000000000000 ) ) ;
#3826=EDGE_CURVE ( 'NONE', #14563, #8616, #3130, .T. ) ;
#3830=CARTESIAN_POINT ( 'NONE',  ( 1.749999999999998002, 24.89775460606832524, 12.96210679857795256 ) ) ;
#3833=VECTOR ( 'NONE', #10303, 1000.000000000000000 ) ;
#3835=AXIS2_PLACEMENT_3D ( 'NONE', #13891, #12733, #6900 ) ;
#3840=ORIENTED_EDGE ( 'NONE', *, *, #11861, .T. ) ;
#3845=EDGE_CURVE ( 'NONE', #626, #3410, #492, .T. ) ;
#3846=FACE_OUTER_BOUND ( 'NONE', #12933, .T. ) ;
#3847=EDGE_CURVE ( 'NONE', #4705, #10796, #9481, .T. ) ;
#3848=AXIS2_PLACEMENT_3D ( 'NONE', #8269, #13972, #11649 ) ;
#3850=DIRECTION ( 'NONE',  ( 0.000000000000000000, 0.000000000000000000, 1.000000000000000000 ) ) ;
#3851=ADVANCED_FACE ( 'NONE', ( #4502 ), #7950, .F. ) ;
#3854=VECTOR ( 'NONE', #11897, 1000.000000000000000 ) ;
#3856=ADVANCED_FACE ( 'NONE', ( #2038 ), #8032, .F. ) ;
#3859=B_SPLINE_CURVE_WITH_KNOTS ( 'NONE', 3,
 ( #1165, #12828, #15078, #6648 ),
 .UNSPECIFIED., .F., .F.,
 ( 4, 4 ),
 ( 4.462636695580848051E-07, 0.0004963285629697519611 ),
 .UNSPECIFIED. ) ;
#3860=ORIENTED_EDGE ( 'NONE', *, *, #4513, .T. ) ;
#3861=VERTEX_POINT ( 'NONE', #14968 ) ;
#3863=CARTESIAN_POINT ( 'NONE',  ( 1.039999999999996927, -4.633866840649124796, 27.68468304288256832 ) ) ;
#3871=CARTESIAN_POINT ( 'NONE',  ( 0.5321745379877897975, 12.96514671151801323, -23.74442027961346113 ) ) ;
#3876=AXIS2_PLACEMENT_3D ( 'NONE', #3975, #1514, #1591 ) ;
#3879=ORIENTED_EDGE ( 'NONE', *, *, #10879, .T. ) ;
#3882=ORIENTED_EDGE ( 'NONE', *, *, #4195, .T. ) ;
#3885=AXIS2_PLACEMENT_3D ( 'NONE', #12740, #13675, #5467 ) ;
#3889=CARTESIAN_POINT ( 'NONE',  ( 2.765633920072241292, 18.55949924794916228, -16.37294372382838148 ) ) ;
#3892=ORIENTED_EDGE ( 'NONE', *, *, #9551, .F. ) ;
#3895=CARTESIAN_POINT ( 'NONE',  ( 2.789999999999999147, -14.18181402625756959, 19.91106274590508107 ) ) ;
#3897=ORIENTED_EDGE ( 'NONE', *, *, #8754, .T. ) ;
#3899=ORIENTED_EDGE ( 'NONE', *, *, #8713, .T. ) ;
#3902=AXIS2_PLACEMENT_3D ( 'NONE', #9807, #9725, #1430 ) ;
#3903=CARTESIAN_POINT ( 'NONE',  ( 0.7592463965288811512, -24.32906614999605921, -12.98165646470108925 ) ) ;
#3906=DIRECTION ( 'NONE',  ( 1.000000000000000000, 0.000000000000000000, 0.000000000000000000 ) ) ;
#3911=EDGE_LOOP ( 'NONE', ( #14581, #3667, #5796, #6423 ) ) ;
#3912=CARTESIAN_POINT ( 'NONE',  ( 1.960886852992497653, -24.44424927289185590, 12.96989951879399072 ) ) ;
#3914=EDGE_LOOP ( 'NONE', ( #1707, #2916, #11211, #3307 ) ) ;
#3915=CARTESIAN_POINT ( 'NONE',  ( 0.006931111373679591826, -22.53293026234497276, -9.685942809247297447 ) ) ;
#3917=EDGE_CURVE ( 'NONE', #269, #447, #12920, .T. ) ;
#3921=CARTESIAN_POINT ( 'NONE',  ( 2.789999999999999147, -15.04425356660744839, -20.70663861606288236 ) ) ;
#3924=ORIENTED_EDGE ( 'NONE', *, *, #14847, .T. ) ;
#3925=ORIENTED_EDGE ( 'NONE', *, *, #2802, .T. ) ;
#3929=EDGE_CURVE ( 'NONE', #5940, #12831, #7790, .T. ) ;
#3930=LINE ( 'NONE', #8606, #439 ) ;
#3931=DIRECTION ( 'NONE',  ( 0.000000000000000000, 0.000000000000000000, 1.000000000000000000 ) ) ;
#3936=DIRECTION ( 'NONE',  ( 0.000000000000000000, 0.000000000000000000, 1.000000000000000000 ) ) ;
#3942=DIRECTION ( 'NONE',  ( -1.000000000000000000, -0.000000000000000000, -0.000000000000000000 ) ) ;
#3949=ADVANCED_FACE ( 'NONE', ( #7106 ), #3487, .T. ) ;
#3954=CYLINDRICAL_SURFACE ( 'NONE', #14308, 2.524999999999995914 ) ;
#3962=CYLINDRICAL_SURFACE ( 'NONE', #8060, 2.524999999999995914 ) ;
#3963=CARTESIAN_POINT ( 'NONE',  ( 0.07181525696555239591, 24.78695292654921545, 5.344212458769448837 ) ) ;
#3965=B_SPLINE_CURVE_WITH_KNOTS ( 'NONE', 3,
 ( #7921, #6691, #771, #13683 ),
 .UNSPECIFIED., .F., .F.,
 ( 4, 4 ),
 ( 2.135345996173300665E-07, 0.0006888010880210822381 ),
 .UNSPECIFIED. ) ;
#3966=VERTEX_POINT ( 'NONE', #8176 ) ;
#3968=DIRECTION ( 'NONE',  ( 0.000000000000000000, 0.000000000000000000, 1.000000000000000000 ) ) ;
#3971=ORIENTED_EDGE ( 'NONE', *, *, #5646, .F. ) ;
#3974=CARTESIAN_POINT ( 'NONE',  ( 1.039999999999997149, -24.89775460606822577, -12.96210679857813730 ) ) ;
#3975=CARTESIAN_POINT ( 'NONE',  ( -5.209999999999999964, 0.000000000000000000, 0.000000000000000000 ) ) ;
#3977=DIRECTION ( 'NONE',  ( 0.000000000000000000, 0.000000000000000000, 1.000000000000000000 ) ) ;
#3978=CARTESIAN_POINT ( 'NONE',  ( 1.394999999999998685, 24.89775460606851354, -12.96210679857759374 ) ) ;
#3985=AXIS2_PLACEMENT_3D ( 'NONE', #11351, #10129, #4517 ) ;
#3987=CARTESIAN_POINT ( 'NONE',  ( 2.724444381390116021, -21.84113606038314259, 12.72236714503155142 ) ) ;
#3988=EDGE_CURVE ( 'NONE', #8704, #1423, #14168, .T. ) ;
#3994=ORIENTED_EDGE ( 'NONE', *, *, #6958, .T. ) ;
#3995=CARTESIAN_POINT ( 'NONE',  ( 2.783068888626320625, -9.685942809246897767, -22.53293026234513619 ) ) ;
#3999=FACE_OUTER_BOUND ( 'NONE', #2990, .T. ) ;
#4000=DIRECTION ( 'NONE',  ( -1.000000000000000000, 0.000000000000000000, -0.000000000000000000 ) ) ;
#4009=CARTESIAN_POINT ( 'NONE',  ( 2.789999999999999147, -2.336989772644440855, 24.63872515616082026 ) ) ;
#4011=ORIENTED_EDGE ( 'NONE', *, *, #11252, .F. ) ;
#4016=B_SPLINE_CURVE_WITH_KNOTS ( 'NONE', 3,
 ( #559, #10870, #5280, #8568, #3963, #14727 ),
 .UNSPECIFIED., .F., .F.,
 ( 4, 2, 4 ),
 ( 4.462636677693390501E-07, 0.001879885020955133004, 0.003759323778242496666 ),
 .UNSPECIFIED. ) ;
#4018=CARTESIAN_POINT ( 'NONE',  ( 2.783069004973550253, -23.92277630352791107, -5.408431875071696204 ) ) ;
#4022=FACE_OUTER_BOUND ( 'NONE', #8399, .T. ) ;
#4023=B_SPLINE_CURVE_WITH_KNOTS ( 'NONE', 3,
 ( #9012, #14860, #4018, #5492 ),
 .UNSPECIFIED., .F., .F.,
 ( 4, 4 ),
 ( 0.005258214619651960589, 0.005948481662034167325 ),
 .UNSPECIFIED. ) ;
#4028=CARTESIAN_POINT ( 'NONE',  ( 0.006931069955679173590, 18.43696893154758598, 16.17493693894884998 ) ) ;
#4031=EDGE_LOOP ( 'NONE', ( #4170, #1831, #14644, #4515 ) ) ;
#4034=CARTESIAN_POINT ( 'NONE',  ( 2.718131847775118182, 24.78765742476139522, 5.344160105508784397 ) ) ;
#4043=DIRECTION ( 'NONE',  ( 0.000000000000000000, 0.000000000000000000, 1.000000000000000000 ) ) ;
#4045=CARTESIAN_POINT ( 'NONE',  ( 0.02436607992775978102, 16.37294372382885044, -18.55949924794875017 ) ) ;
#4047=ORIENTED_EDGE ( 'NONE', *, *, #9107, .T. ) ;
#4051=EDGE_CURVE ( 'NONE', #14255, #14793, #301, .T. ) ;
#4053=CARTESIAN_POINT ( 'NONE',  ( 1.749999999999998002, 4.147968289691672084, -27.76164181293047406 ) ) ;
#4059=DIRECTION ( 'NONE',  ( -1.000000000000000000, 0.000000000000000000, 0.000000000000000000 ) ) ;
#4072=CARTESIAN_POINT ( 'NONE',  ( 2.789999999999999147, -24.34211360614294506, -7.909232158575071558 ) ) ;
#4074=CARTESIAN_POINT ( 'NONE',  ( 2.789999999999999147, -22.71065055754459650, 9.836394144775621129 ) ) ;
#4076=CARTESIAN_POINT ( 'NONE',  ( 1.749999999999998002, -12.96210679857767367, -24.89775460606847091 ) ) ;
#4079=FACE_OUTER_BOUND ( 'NONE', #8975, .T. ) ;
#4082=B_SPLINE_CURVE_WITH_KNOTS ( 'NONE', 3,
 ( #4966, #1730, #9720, #9639 ),
 .UNSPECIFIED., .F., .F.,
 ( 4, 4 ),
 ( 3.059063720746937335E-07, 0.0006888942284914199117 ),
 .UNSPECIFIED. ) ;
#4085=CARTESIAN_POINT ( 'NONE',  ( 2.765633920072235963, 24.63872515616082737, 2.336989772644355146 ) ) ;
#4088=ORIENTED_EDGE ( 'NONE', *, *, #13114, .T. ) ;
#4089=CARTESIAN_POINT ( 'NONE',  ( 2.789999999999999147, 23.17675759782041212, -7.772527002114516748 ) ) ;
#4098=CARTESIAN_POINT ( 'NONE',  ( 50.00050000000000239, 0.000000000000000000, 0.000000000000000000 ) ) ;
#4105=DIRECTION ( 'NONE',  ( -1.000000000000000000, -0.000000000000000000, -0.000000000000000000 ) ) ;
#4107=EDGE_LOOP ( 'NONE', ( #1038, #1645, #1867, #4644 ) ) ;
#4113=VERTEX_POINT ( 'NONE', #1642 ) ;
#4117=EDGE_CURVE ( 'NONE', #6654, #2553, #10578, .T. ) ;
#4119=CARTESIAN_POINT ( 'NONE',  ( 2.765633920072236851, 24.15498966839963302, 5.391175441198700291 ) ) ;
#4124=FACE_OUTER_BOUND ( 'NONE', #1478, .T. ) ;
#4125=CARTESIAN_POINT ( 'NONE',  ( 0.02436607992776325046, 16.37294372382858398, 18.55949924794898465 ) ) ;
#4130=VERTEX_POINT ( 'NONE', #9861 ) ;
#4132=VERTEX_POINT ( 'NONE', #14637 ) ;
#4134=ORIENTED_EDGE ( 'NONE', *, *, #9472, .F. ) ;
#4137=FACE_OUTER_BOUND ( 'NONE', #6773, .T. ) ;
#4138=ADVANCED_FACE ( 'NONE', ( #6330 ), #3954, .F. ) ;
#4149=CARTESIAN_POINT ( 'NONE',  ( 2.783068945535914995, 2.248820353272968919, 24.42321038836783131 ) ) ;
#4150=CARTESIAN_POINT ( 'NONE',  ( 0.000000000000000000, -1.991882183130475603, 24.04302995059966719 ) ) ;
#4151=ORIENTED_EDGE ( 'NONE', *, *, #10975, .T. ) ;
#4153=CARTESIAN_POINT ( 'NONE',  ( 2.789999999999999147, 2.680914349914567470E-13, -23.06981291497571362 ) ) ;
#4155=VERTEX_POINT ( 'NONE', #7564 ) ;
#4158=LINE ( 'NONE', #4074, #15170 ) ;
#4159=CARTESIAN_POINT ( 'NONE',  ( 2.601776096565022289, -12.84621645676828372, -22.54313264455027976 ) ) ;
#4160=DIRECTION ( 'NONE',  ( 0.000000000000000000, 0.000000000000000000, 1.000000000000000000 ) ) ;
#4162=CARTESIAN_POINT ( 'NONE',  ( 0.02436607992775761261, 22.71065055754452544, 9.836394144775786330 ) ) ;
#4163=AXIS2_PLACEMENT_3D ( 'NONE', #8340, #8777, #9573 ) ;
#4164=ORIENTED_EDGE ( 'NONE', *, *, #1444, .T. ) ;
#4165=B_SPLINE_CURVE_WITH_KNOTS ( 'NONE', 3,
 ( #10595, #10364, #4838, #12810 ),
 .UNSPECIFIED., .F., .F.,
 ( 4, 4 ),
 ( 0.0006045424356927869836, 0.0006887909409525213005 ),
 .UNSPECIFIED. ) ;
#4167=CARTESIAN_POINT ( 'NONE',  ( 0.000000000000000000, 7.909232158574813099, 24.34211360614303388 ) ) ;
#4170=ORIENTED_EDGE ( 'NONE', *, *, #6461, .T. ) ;
#4185=CARTESIAN_POINT ( 'NONE',  ( 0.07181525068722517668, 2.576941577947404305, 25.22524549359951251 ) ) ;
#4195=EDGE_CURVE ( 'NONE', #13780, #4420, #8913, .T. ) ;
#4196=CARTESIAN_POINT ( 'NONE',  ( 0.07186811453410638095, -16.91241718342012490, 18.89333555428548905 ) ) ;
#4198=DIRECTION ( 'NONE',  ( 0.000000000000000000, 0.000000000000000000, 1.000000000000000000 ) ) ;
#4199=EDGE_LOOP ( 'NONE', ( #6425, #13995, #11553, #3879 ) ) ;
#4203=DIRECTION ( 'NONE',  ( 1.000000000000000000, 0.000000000000000000, 0.000000000000000000 ) ) ;
#4205=EDGE_CURVE ( 'NONE', #11809, #11548, #14421, .T. ) ;
#4207=ORIENTED_EDGE ( 'NONE', *, *, #13839, .T. ) ;
#4212=CARTESIAN_POINT ( 'NONE',  ( 0.006974663525959075641, 12.53640742967783694, -21.08118142846890208 ) ) ;
#4226=CYLINDRICAL_SURFACE ( 'NONE', #3341, 13.19999999999999929 ) ;
#4227=ORIENTED_EDGE ( 'NONE', *, *, #3412, .T. ) ;
#4228=VERTEX_POINT ( 'NONE', #7637 ) ;
#4234=CIRCLE ( 'NONE', #11590, 24.12539914357697768 ) ;
#4235=CARTESIAN_POINT ( 'NONE',  ( 0.7592463834391182109, 24.80264696524898937, -12.05220173035413112 ) ) ;
#4239=DIRECTION ( 'NONE',  ( -1.000000000000000000, 0.000000000000000000, -0.000000000000000000 ) ) ;
#4244=CIRCLE ( 'NONE', #5714, 2.524999999999995914 ) ;
#4248=DIRECTION ( 'NONE',  ( 1.000000000000000000, -0.000000000000000000, -0.000000000000000000 ) ) ;
#4249=DIRECTION ( 'NONE',  ( -1.000000000000000000, -0.000000000000000000, -0.000000000000000000 ) ) ;
#4250=EDGE_CURVE ( 'NONE', #10187, #552, #11385, .T. ) ;
#4256=CARTESIAN_POINT ( 'NONE',  ( 0.7589665089996477931, -12.05173163741739906, 24.80232951178374279 ) ) ;
#4257=CARTESIAN_POINT ( 'NONE',  ( 0.4386599019957485579, -23.41653927703718097, 12.93238701107298283 ) ) ;
#4262=ORIENTED_EDGE ( 'NONE', *, *, #3631, .F. ) ;
#4264=CARTESIAN_POINT ( 'NONE',  ( 2.765633920072239516, 21.30679549418631780, 12.59161484032919986 ) ) ;
#4265=FACE_OUTER_BOUND ( 'NONE', #13894, .T. ) ;
#4266=EDGE_CURVE ( 'NONE', #2063, #11374, #3105, .T. ) ;
#4267=ORIENTED_EDGE ( 'NONE', *, *, #4323, .F. ) ;
#4268=CARTESIAN_POINT ( 'NONE',  ( 2.789999999999999147, 0.2301004812057544924, 24.44424927289185590 ) ) ;
#4273=ORIENTED_EDGE ( 'NONE', *, *, #1444, .F. ) ;
#4274=CARTESIAN_POINT ( 'NONE',  ( 2.257825462012206685, 12.96514671151767395, 23.74442027961364943 ) ) ;
#4280=CARTESIAN_POINT ( 'NONE',  ( 2.789999999999999147, -20.70663861606260170, -15.04425356660783031 ) ) ;
#4287=DIRECTION ( 'NONE',  ( -1.000000000000000000, 0.000000000000000000, -0.000000000000000000 ) ) ;
#4288=CYLINDRICAL_SURFACE ( 'NONE', #3985, 28.06981291497571362 ) ;
#4289=VECTOR ( 'NONE', #6980, 1000.000000000000000 ) ;
#4295=DIRECTION ( 'NONE',  ( -1.000000000000000000, -0.000000000000000000, 0.000000000000000000 ) ) ;
#4297=ORIENTED_EDGE ( 'NONE', *, *, #4778, .T. ) ;
#4299=DIRECTION ( 'NONE',  ( -1.000000000000000000, -0.000000000000000000, -0.000000000000000000 ) ) ;
#4304=CARTESIAN_POINT ( 'NONE',  ( 0.006931054464086492187, 24.42321038836783131, 2.248820353273056405 ) ) ;
#4306=EDGE_CURVE ( 'NONE', #6946, #7479, #7092, .T. ) ;
#4307=EDGE_CURVE ( 'NONE', #3792, #11100, #7670, .T. ) ;
#4316=FILL_AREA_STYLE ('',( #5630 ) ) ;
#4320=EDGE_LOOP ( 'NONE', ( #2354, #7794, #7842, #9153 ) ) ;
#4322=DIRECTION ( 'NONE',  ( 1.000000000000000000, 0.000000000000000000, 0.000000000000000000 ) ) ;
#4323=EDGE_CURVE ( 'NONE', #6024, #1104, #15018, .T. ) ;
#4324=CARTESIAN_POINT ( 'NONE',  ( 0.07186808533286581646, -23.19485392143207036, -10.24630254990540834 ) ) ;
#4326=DIRECTION ( 'NONE',  ( -1.000000000000000000, 0.000000000000000000, 0.000000000000000000 ) ) ;
#4328=VERTEX_POINT ( 'NONE', #1018 ) ;
#4337=CIRCLE ( 'NONE', #1633, 2.524999999999995914 ) ;
#4342=DIRECTION ( 'NONE',  ( -1.000000000000000000, -0.000000000000000000, -0.000000000000000000 ) ) ;
#4347=LINE ( 'NONE', #9034, #1858 ) ;
#4350=ORIENTED_EDGE ( 'NONE', *, *, #3062, .F. ) ;
#4352=DIRECTION ( 'NONE',  ( 0.000000000000000000, 0.3090169943749350723, 0.9510565162951576390 ) ) ;
#4355=AXIS2_PLACEMENT_3D ( 'NONE', #12633, #14880, #12564 ) ;
#4358=DIRECTION ( 'NONE',  ( -1.000000000000000000, -0.000000000000000000, -0.000000000000000000 ) ) ;
#4360=AXIS2_PLACEMENT_3D ( 'NONE', #11510, #5686, #13751 ) ;
#4361=CARTESIAN_POINT ( 'NONE',  ( 0.000000000000000000, 12.52067188844379864, -20.62201879784900882 ) ) ;
#4364=AXIS2_PLACEMENT_3D ( 'NONE', #10575, #7036, #11855 ) ;
#4370=LINE ( 'NONE', #673, #12233 ) ;
#4373=ORIENTED_EDGE ( 'NONE', *, *, #1854, .F. ) ;
#4387=CARTESIAN_POINT ( 'NONE',  ( -1.381028087215756681E-16, 24.22479935914660132, 2.133490293297101381 ) ) ;
#4391=CARTESIAN_POINT ( 'NONE',  ( 0.07186814640506919427, -12.74240566898967764, -21.92302674874977697 ) ) ;
#4392=CARTESIAN_POINT ( 'NONE',  ( 0.000000000000000000, 15.74360496233383522, 18.28042085475283329 ) ) ;
#4396=AXIS2_PLACEMENT_3D ( 'NONE', #11420, #895, #4448 ) ;
#4399=EDGE_CURVE ( 'NONE', #6867, #10187, #7639, .T. ) ;
#4404=DIRECTION ( 'NONE',  ( 0.000000000000000000, 0.8090169943749400128, 0.5877852522924831291 ) ) ;
#4406=DIRECTION ( 'NONE',  ( -1.000000000000000000, 0.000000000000000000, -0.000000000000000000 ) ) ;
#4410=TOROIDAL_SURFACE ( 'NONE', #4163, 24.12539914357697768, 8.000000000000000000 ) ;
#4414=CARTESIAN_POINT ( 'NONE',  ( 2.789999999999999147, 20.62201879784931435, -12.52067188844328882 ) ) ;
#4419=EDGE_CURVE ( 'NONE', #8921, #4328, #14615, .T. ) ;
#4420=VERTEX_POINT ( 'NONE', #839 ) ;
#4421=CARTESIAN_POINT ( 'NONE',  ( 1.394999999999998685, -27.68468304288255410, -4.633866840649221608 ) ) ;
#4422=DIRECTION ( 'NONE',  ( -1.000000000000000000, 0.000000000000000000, 0.000000000000000000 ) ) ;
#4424=ORIENTED_EDGE ( 'NONE', *, *, #5646, .T. ) ;
#4429=VERTEX_POINT ( 'NONE', #4392 ) ;
#4432=CARTESIAN_POINT ( 'NONE',  ( 2.765633920072238183, 2.336989772644269436, 24.63872515616083447 ) ) ;
#4433=VERTEX_POINT ( 'NONE', #15064 ) ;
#4442=CARTESIAN_POINT ( 'NONE',  ( 1.039999999999996927, -4.633866840649124796, 27.68468304288256832 ) ) ;
#4444=CARTESIAN_POINT ( 'NONE',  ( 2.783068945535915883, -2.248820353272798389, -24.42321038836784908 ) ) ;
#4446=CARTESIAN_POINT ( 'NONE',  ( 1.039999999999996261, 24.89775460606850999, -12.96210679857759018 ) ) ;
#4447=ORIENTED_EDGE ( 'NONE', *, *, #12943, .F. ) ;
#4448=DIRECTION ( 'NONE',  ( 0.000000000000000000, 0.000000000000000000, 1.000000000000000000 ) ) ;
#4449=CARTESIAN_POINT ( 'NONE',  ( -10.00000000000000000, 0.000000000000000000, 0.000000000000000000 ) ) ;
#4453=EDGE_CURVE ( 'NONE', #12548, #316, #2869, .T. ) ;
#4455=CARTESIAN_POINT ( 'NONE',  ( -7.841635642041319107E-14, -15.96555658743749717, -18.34439787333524663 ) ) ;
#4458=DIRECTION ( 'NONE',  ( -1.000000000000000000, -0.000000000000000000, -0.000000000000000000 ) ) ;
#4461=CARTESIAN_POINT ( 'NONE',  ( 2.783025306068356297, 16.17543236988015209, -18.43727551351014071 ) ) ;
#4464=CARTESIAN_POINT ( 'NONE',  ( 1.039999999999995373, -12.96210679857767900, -24.89775460606846380 ) ) ;
#4466=EDGE_CURVE ( 'NONE', #10187, #12893, #12396, .T. ) ;
#4467=ORIENTED_EDGE ( 'NONE', *, *, #4195, .F. ) ;
#4471=ORIENTED_EDGE ( 'NONE', *, *, #10432, .F. ) ;
#4473=EDGE_LOOP ( 'NONE', ( #9850, #4491, #14840, #13950, #2304, #14737 ) ) ;
#4475=DIRECTION ( 'NONE',  ( 0.000000000000000000, 0.000000000000000000, 1.000000000000000000 ) ) ;
#4476=AXIS2_PLACEMENT_3D ( 'NONE', #9130, #13812, #1990 ) ;
#4483=CARTESIAN_POINT ( 'NONE',  ( 0.7592463896980138349, 19.86438386685688684, -19.12676442129323107 ) ) ;
#4485=CARTESIAN_POINT ( 'NONE',  ( 2.783068961317272549, 21.08061549536614976, 12.53626894672835945 ) ) ;
#4491=ORIENTED_EDGE ( 'NONE', *, *, #10695, .F. ) ;
#4492=VERTEX_POINT ( 'NONE', #10073 ) ;
#4494=DIRECTION ( 'NONE',  ( -1.000000000000000000, -0.000000000000000000, -0.000000000000000000 ) ) ;
#4501=ORIENTED_EDGE ( 'NONE', *, *, #13692, .F. ) ;
#4502=FACE_OUTER_BOUND ( 'NONE', #7611, .T. ) ;
#4508=DIRECTION ( 'NONE',  ( -1.000000000000000000, -0.000000000000000000, -0.000000000000000000 ) ) ;
#4511=DIRECTION ( 'NONE',  ( -1.000000000000000000, 0.000000000000000000, 0.000000000000000000 ) ) ;
#4512=CARTESIAN_POINT ( 'NONE',  ( 2.765633920072235519, -18.55949924794880346, -16.37294372382878649 ) ) ;
#4513=EDGE_CURVE ( 'NONE', #6024, #7008, #4165, .T. ) ;
#4515=ORIENTED_EDGE ( 'NONE', *, *, #5177, .F. ) ;
#4517=DIRECTION ( 'NONE',  ( 0.000000000000000000, 0.000000000000000000, 1.000000000000000000 ) ) ;
#4518=B_SPLINE_CURVE_WITH_KNOTS ( 'NONE', 3,
 ( #9492, #9345, #6034, #7187 ),
 .UNSPECIFIED., .F., .F.,
 ( 4, 4 ),
 ( 3.059063720760159520E-07, 0.0006888942284914070097 ),
 .UNSPECIFIED. ) ;
#4519=CYLINDRICAL_SURFACE ( 'NONE', #12450, 2.524999999999995914 ) ;
#4520=ADVANCED_FACE ( 'NONE', ( #15144 ), #6199, .T. ) ;
#4522=VERTEX_POINT ( 'NONE', #5762 ) ;
#4529=DIRECTION ( 'NONE',  ( -1.000000000000000000, 0.000000000000000000, 0.000000000000000000 ) ) ;
#4530=DIRECTION ( 'NONE',  ( 0.000000000000000000, 0.000000000000000000, 1.000000000000000000 ) ) ;
#4531=ORIENTED_EDGE ( 'NONE', *, *, #10879, .F. ) ;
#4535=CARTESIAN_POINT ( 'NONE',  ( 1.749999999999998002, 4.633866840648922292, 27.68468304288260384 ) ) ;
#4536=CARTESIAN_POINT ( 'NONE',  ( 2.789999999999999147, -1.991882183130126549, -24.04302995059967429 ) ) ;
#4538=CIRCLE ( 'NONE', #13098, 28.06981291497571362 ) ;
#4539=ORIENTED_EDGE ( 'NONE', *, *, #7931, .F. ) ;
#4540=FACE_OUTER_BOUND ( 'NONE', #5889, .T. ) ;
#4542=TOROIDAL_SURFACE ( 'NONE', #8451, 24.12539914357697413, 8.000000000000000000 ) ;
#4544=ORIENTED_EDGE ( 'NONE', *, *, #817, .F. ) ;
#4546=( NAMED_UNIT ( * ) PLANE_ANGLE_UNIT ( ) SI_UNIT ( $, .RADIAN. ) );
#4552=AXIS2_PLACEMENT_3D ( 'NONE', #12611, #3250, #9011 ) ;
#4553=CARTESIAN_POINT ( 'NONE',  ( 0.1855654851361725199, -23.63475234378974577, -10.67816411292190004 ) ) ;
#4556=EDGE_CURVE ( 'NONE', #7436, #2289, #13556, .T. ) ;
#4558=ORIENTED_EDGE ( 'NONE', *, *, #11818, .F. ) ;
#4559=CARTESIAN_POINT ( 'NONE',  ( 1.039999999999997371, 25.12109765559653596, 12.52377138324232675 ) ) ;
#4561=VECTOR ( 'NONE', #705, 1000.000000000000000 ) ;
#4562=VECTOR ( 'NONE', #2712, 1000.000000000000000 ) ;
#4570=EDGE_CURVE ( 'NONE', #14075, #12114, #8891, .T. ) ;
#4572=ORIENTED_EDGE ( 'NONE', *, *, #4307, .T. ) ;
#4576=CARTESIAN_POINT ( 'NONE',  ( 2.765633920072235519, 24.15498966839970052, -5.391175441198366336 ) ) ;
#4586=EDGE_CURVE ( 'NONE', #5643, #5736, #8157, .T. ) ;
#4588=VERTEX_POINT ( 'NONE', #8203 ) ;
#4592=CARTESIAN_POINT ( 'NONE',  ( 2.789999999999999147, 16.37294372382885044, -18.55949924794875017 ) ) ;
#4597=CARTESIAN_POINT ( 'NONE',  ( -7.940452095251188120E-14, -18.34439787333518268, 15.96555658743757000 ) ) ;
#4598=AXIS2_PLACEMENT_3D ( 'NONE', #8034, #15196, #9340 ) ;
#4600=CARTESIAN_POINT ( 'NONE',  ( 2.790000000000000036, 22.37986894186685660, -9.514945144208509120 ) ) ;
#4607=EDGE_CURVE ( 'NONE', #9067, #4798, #10194, .T. ) ;
#4608=CARTESIAN_POINT ( 'NONE',  ( 2.789999999999999147, -20.70663861606282197, 15.04425356660753188 ) ) ;
#4609=CARTESIAN_POINT ( 'NONE',  ( 2.765633920072242180, 22.71065055754465689, -9.836394144775473691 ) ) ;
#4611=B_SPLINE_CURVE_WITH_KNOTS ( 'NONE', 3,
 ( #14193, #3579, #8266, #9578, #11863, #10647 ),
 .UNSPECIFIED., .F., .F.,
 ( 4, 2, 4 ),
 ( 4.462636793144857890E-07, 0.001879885123570645663, 0.003759323983461976531 ),
 .UNSPECIFIED. ) ;
#4614=AXIS2_PLACEMENT_3D ( 'NONE', #11514, #2224, #8984 ) ;
#4618=TOROIDAL_SURFACE ( 'NONE', #10732, 24.12539914357697768, 8.000000000000000000 ) ;
#4622=EDGE_CURVE ( 'NONE', #11374, #12104, #469, .T. ) ;
#4628=DIRECTION ( 'NONE',  ( -1.000000000000000000, -0.000000000000000000, -0.000000000000000000 ) ) ;
#4629=TOROIDAL_SURFACE ( 'NONE', #8046, 24.12539914357697768, 8.000000000000000000 ) ;
#4634=ORIENTED_EDGE ( 'NONE', *, *, #12683, .F. ) ;
#4637=CARTESIAN_POINT ( 'NONE',  ( 2.765633920072242624, 9.836394144775706394, 22.71065055754456097 ) ) ;
#4638=AXIS2_PLACEMENT_3D ( 'NONE', #8793, #3315, #642 ) ;
#4642=TOROIDAL_SURFACE ( 'NONE', #6343, 24.12539914357697768, 8.000000000000000000 ) ;
#4644=ORIENTED_EDGE ( 'NONE', *, *, #1583, .T. ) ;
#4645=DIRECTION ( 'NONE',  ( 1.000000000000000000, -0.000000000000000000, 0.000000000000000000 ) ) ;
#4646=CARTESIAN_POINT ( 'NONE',  ( 2.790000000000000036, 20.85230829256853013, 12.51294990530023732 ) ) ;
#4648=AXIS2_PLACEMENT_3D ( 'NONE', #4268, #10260, #14961 ) ;
#4649=ORIENTED_EDGE ( 'NONE', *, *, #1583, .F. ) ;
#4654=VERTEX_POINT ( 'NONE', #10663 ) ;
#4657=CARTESIAN_POINT ( 'NONE',  ( 0.02436607992776151574, 24.15498966839970052, -5.391175441198366336 ) ) ;
#4658=CARTESIAN_POINT ( 'NONE',  ( 0.006974674093432157128, -2.249040938978327908, -24.42374957165208116 ) ) ;
#4664=DIRECTION ( 'NONE',  ( 0.000000000000000000, 6.870191984066573782E-16, -1.000000000000000000 ) ) ;
#4669=EDGE_LOOP ( 'NONE', ( #13024, #1176, #12087, #4934 ) ) ;
#4674=CARTESIAN_POINT ( 'NONE',  ( -7.372183127218402931E-16, -20.85230829256862961, 12.51294990530008988 ) ) ;
#4675=FACE_OUTER_BOUND ( 'NONE', #13775, .T. ) ;
#4676=CARTESIAN_POINT ( 'NONE',  ( 1.394999999999999574, -12.52377138324206740, -25.12109765559666741 ) ) ;
#4679=DIRECTION ( 'NONE',  ( 1.000000000000000000, 0.000000000000000000, 0.000000000000000000 ) ) ;
#4680=DIRECTION ( 'NONE',  ( 0.000000000000000000, 0.000000000000000000, 1.000000000000000000 ) ) ;
#4681=CARTESIAN_POINT ( 'NONE',  ( -5.209999999999999964, 0.000000000000000000, 0.000000000000000000 ) ) ;
#4683=CARTESIAN_POINT ( 'NONE',  ( 1.749999999999998002, -4.147968289691484678, 27.76164181293050603 ) ) ;
#4690=CARTESIAN_POINT ( 'NONE',  ( 0.000000000000000000, 9.324097380959777581, -22.25075486061729535 ) ) ;
#4693=CARTESIAN_POINT ( 'NONE',  ( 0.000000000000000000, 0.000000000000000000, 0.000000000000000000 ) ) ;
#4694=DIRECTION ( 'NONE',  ( 0.000000000000000000, 0.000000000000000000, 1.000000000000000000 ) ) ;
#4698=EDGE_CURVE ( 'NONE', #10310, #952, #6283, .T. ) ;
#4702=CARTESIAN_POINT ( 'NONE',  ( 0.8958345380406140812, -24.59696699259434993, 12.96989951879399250 ) ) ;
#4703=VERTEX_POINT ( 'NONE', #6362 ) ;
#4705=VERTEX_POINT ( 'NONE', #9660 ) ;
#4706=ORIENTED_EDGE ( 'NONE', *, *, #6521, .F. ) ;
#4707=DIRECTION ( 'NONE',  ( 0.000000000000000000, 0.000000000000000000, 1.000000000000000000 ) ) ;
#4709=CARTESIAN_POINT ( 'NONE',  ( 1.394999999999999574, -4.633866840648735774, -27.68468304288263582 ) ) ;
#4713=CARTESIAN_POINT ( 'NONE',  ( 0.1855657389739082119, 5.253342437939721776, 25.39738473785002881 ) ) ;
#4721=EDGE_LOOP ( 'NONE', ( #13299, #1651, #10822, #9368 ) ) ;
#4723=FACE_OUTER_BOUND ( 'NONE', #3914, .T. ) ;
#4726=CARTESIAN_POINT ( 'NONE',  ( 1.039999999999994929, -25.12109765559662833, 12.52377138324214023 ) ) ;
#4728=CARTESIAN_POINT ( 'NONE',  ( 2.790000000000079527, 18.34439787333507255, 15.96555658743769079 ) ) ;
#4732=B_SPLINE_CURVE_WITH_KNOTS ( 'NONE', 3,
 ( #2138, #10135, #10288, #14907 ),
 .UNSPECIFIED., .F., .F.,
 ( 4, 4 ),
 ( 2.034713381942717888E-07, 0.0006887909409525252036 ),
 .UNSPECIFIED. ) ;
#4733=CARTESIAN_POINT ( 'NONE',  ( 2.789999999999999147, 14.55412442567617681, 19.64056340710880022 ) ) ;
#4734=ORIENTED_EDGE ( 'NONE', *, *, #4250, .T. ) ;
#4741=DIRECTION ( 'NONE',  ( 1.000000000000000000, 0.000000000000000000, 0.000000000000000000 ) ) ;
#4747=CARTESIAN_POINT ( 'NONE',  ( 2.789999999999999147, 15.04425356660760293, 20.70663861606276868 ) ) ;
#4752=CARTESIAN_POINT ( 'NONE',  ( 0.5279273381794625797, 26.82026385750178932, 3.461047254864356049 ) ) ;
#4753=ORIENTED_EDGE ( 'NONE', *, *, #5177, .T. ) ;
#4754=CYLINDRICAL_SURFACE ( 'NONE', #9018, 2.524999999999996358 ) ;
#4758=DIRECTION ( 'NONE',  ( -1.000000000000000000, -0.000000000000000000, -0.000000000000000000 ) ) ;
#4759=B_SPLINE_CURVE_WITH_KNOTS ( 'NONE', 3,
 ( #4442, #9124, #11568, #11343, #3138, #1046 ),
 .UNSPECIFIED., .F., .F.,
 ( 4, 2, 4 ),
 ( 4.462636682233640623E-07, 0.001879885020955585333, 0.003759323778242947261 ),
 .UNSPECIFIED. ) ;
#4760=DIRECTION ( 'NONE',  ( 0.000000000000000000, 0.000000000000000000, 1.000000000000000000 ) ) ;
#4763=ORIENTED_EDGE ( 'NONE', *, *, #7486, .F. ) ;
#4765=CARTESIAN_POINT ( 'NONE',  ( 1.749999999999998002, -27.76164181293054511, 4.147968289691195132 ) ) ;
#4772=ORIENTED_EDGE ( 'NONE', *, *, #5346, .T. ) ;
#4777=CARTESIAN_POINT ( 'NONE',  ( 8.000000000000000000, 0.000000000000000000, 0.000000000000000000 ) ) ;
#4778=EDGE_CURVE ( 'NONE', #5632, #11410, #268, .T. ) ;
#4779=EDGE_CURVE ( 'NONE', #2934, #7330, #3034, .T. ) ;
#4782=AXIS2_PLACEMENT_3D ( 'NONE', #8833, #5400, #6305 ) ;
#4784=CARTESIAN_POINT ( 'NONE',  ( 0.07186815222487989707, 5.344160105508701797, 24.78765742476140943 ) ) ;
#4786=VERTEX_POINT ( 'NONE', #12510 ) ;
#4789=AXIS2_PLACEMENT_3D ( 'NONE', #14280, #10661, #9514 ) ;
#4790=ADVANCED_FACE ( 'NONE', ( #10198 ), #1822, .F. ) ;
#4791=TOROIDAL_SURFACE ( 'NONE', #10668, 24.12539914357697413, 8.000000000000000000 ) ;
#4794=CARTESIAN_POINT ( 'NONE',  ( 2.765633920072238627, -21.30679549418621832, -12.59161484032935618 ) ) ;
#4795=CARTESIAN_POINT ( 'NONE',  ( 8.000000000000000000, 0.000000000000000000, 0.000000000000000000 ) ) ;
#4798=VERTEX_POINT ( 'NONE', #13508 ) ;
#4800=CARTESIAN_POINT ( 'NONE',  ( 2.789999999999999147, -22.25075486061731667, -9.324097380959683434 ) ) ;
#4801=CIRCLE ( 'NONE', #3322, 24.12539914357697768 ) ;
#4806=CARTESIAN_POINT ( 'NONE',  ( 1.394999999999999574, 4.147968289691677413, -27.76164181293047761 ) ) ;
#4809=ORIENTED_EDGE ( 'NONE', *, *, #622, .F. ) ;
#4811=LINE ( 'NONE', #9483, #5342 ) ;
#4813=VERTEX_POINT ( 'NONE', #11346 ) ;
#4816=DIRECTION ( 'NONE',  ( -1.000000000000000000, -0.000000000000000000, -0.000000000000000000 ) ) ;
#4819=PRODUCT_DEFINITION_SHAPE ( 'NONE', 'NONE',  #3450 ) ;
#4820=CARTESIAN_POINT ( 'NONE',  ( 2.031033471609898111, -27.31260702007178409, 3.797536611356223890 ) ) ;
#4821=AXIS2_PLACEMENT_3D ( 'NONE', #15098, #1405, #12775 ) ;
#4826=CARTESIAN_POINT ( 'NONE',  ( 2.783025228907522575, 22.53337530003403799, 9.686319561461028016 ) ) ;
#4828=ORIENTED_EDGE ( 'NONE', *, *, #10773, .F. ) ;
#4830=ORIENTED_EDGE ( 'NONE', *, *, #6135, .T. ) ;
#4831=DIRECTION ( 'NONE',  ( -1.000000000000000000, -0.000000000000000000, -0.000000000000000000 ) ) ;
#4832=AXIS2_PLACEMENT_3D ( 'NONE', #4608, #175, #2565 ) ;
#4833=CARTESIAN_POINT ( 'NONE',  ( 0.02436607992776585255, -5.391175441198789109, 24.15498966839961170 ) ) ;
#4834=DIRECTION ( 'NONE',  ( -1.000000000000000000, -0.000000000000000000, -0.000000000000000000 ) ) ;
#4838=CARTESIAN_POINT ( 'NONE',  ( 2.790000000000077307, 20.65026423218591844, -12.51972477286559027 ) ) ;
#4845=CARTESIAN_POINT ( 'NONE',  ( 2.563317066925346527E-16, -12.51294990530000817, -20.85230829256867935 ) ) ;
#4849=AXIS2_PLACEMENT_3D ( 'NONE', #8901, #4458, #10211 ) ;
#4850=CIRCLE ( 'NONE', #1904, 28.06981291497571007 ) ;
#4856=CARTESIAN_POINT ( 'NONE',  ( 1.039999999999997593, 0.000000000000000000, 0.000000000000000000 ) ) ;
#4861=CARTESIAN_POINT ( 'NONE',  ( 0.000000000000000000, -15.74360496233395956, 18.28042085475273026 ) ) ;
#4869=CIRCLE ( 'NONE', #3398, 24.12539914357697768 ) ;
#4870=B_SPLINE_CURVE_WITH_KNOTS ( 'NONE', 3,
 ( #6023, #6104, #8469, #2935, #7340, #12006 ),
 .UNSPECIFIED., .F., .F.,
 ( 4, 2, 4 ),
 ( 1.979325885387340151E-07, 0.001878588715165610589, 0.003756979497742682708 ),
 .UNSPECIFIED. ) ;
#4874=ORIENTED_EDGE ( 'NONE', *, *, #1394, .F. ) ;
#4882=DIRECTION ( 'NONE',  ( 0.000000000000000000, 0.9510565162951567508, -0.3090169943749379589 ) ) ;
#4883=EDGE_CURVE ( 'NONE', #7008, #4813, #10547, .T. ) ;
#4884=EDGE_CURVE ( 'NONE', #8456, #12081, #12575, .T. ) ;
#4886=DIRECTION ( 'NONE',  ( 0.000000000000000000, 0.000000000000000000, -1.000000000000000000 ) ) ;
#4891=FACE_OUTER_BOUND ( 'NONE', #6013, .T. ) ;
#4894=ADVANCED_FACE ( 'NONE', ( #13427 ), #12942, .F. ) ;
#4895=ORIENTED_EDGE ( 'NONE', *, *, #4586, .T. ) ;
#4897=CARTESIAN_POINT ( 'NONE',  ( 2.257825462012207574, 23.74442027961379864, -12.96514671151741638 ) ) ;
#4898=CARTESIAN_POINT ( 'NONE',  ( 0.006974657972266581039, -23.92335783895634194, -5.408388659524344000 ) ) ;
#4900=APPLICATION_CONTEXT ( 'automotive_design' ) ;
#4905=FACE_OUTER_BOUND ( 'NONE', #245, .T. ) ;
#4909=DIRECTION ( 'NONE',  ( -1.000000000000000000, -0.000000000000000000, -0.000000000000000000 ) ) ;
#4910=DIRECTION ( 'NONE',  ( 0.000000000000000000, 0.000000000000000000, -1.000000000000000000 ) ) ;
#4917=CARTESIAN_POINT ( 'NONE',  ( 2.765633920072234631, -21.30679549418640306, 12.59161484032904887 ) ) ;
#4918=CARTESIAN_POINT ( 'NONE',  ( 0.000000000000000000, -5.535312321042921369, 23.48180575137728354 ) ) ;
#4922=ORIENTED_EDGE ( 'NONE', *, *, #1394, .T. ) ;
#4923=CARTESIAN_POINT ( 'NONE',  ( 0.02436607992775891365, -24.63872515616080960, -2.336989772644527008 ) ) ;
#4924=LINE ( 'NONE', #13906, #2931 ) ;
#4934=ORIENTED_EDGE ( 'NONE', *, *, #11047, .T. ) ;
#4937=CARTESIAN_POINT ( 'NONE',  ( 2.790000000000076863, -23.69897269326681055, 5.456611084821764379 ) ) ;
#4940=CARTESIAN_POINT ( 'NONE',  ( 0.000000000000000000, 22.25075486061737351, 9.324097380959511128 ) ) ;
#4943=EDGE_CURVE ( 'NONE', #11143, #9391, #6880, .T. ) ;
#4948=DIRECTION ( 'NONE',  ( 0.000000000000000000, 0.000000000000000000, 1.000000000000000000 ) ) ;
#4950=ORIENTED_EDGE ( 'NONE', *, *, #10916, .F. ) ;
#4953=CARTESIAN_POINT ( 'NONE',  ( 2.789999999999999147, 12.59161484032912171, 21.30679549418635688 ) ) ;
#4958=EDGE_LOOP ( 'NONE', ( #704, #10566, #4164, #441, #12288, #10189, #8080, #996 ) ) ;
#4966=CARTESIAN_POINT ( 'NONE',  ( 2.765633920072235519, -9.836394144775869819, 22.71065055754449347 ) ) ;
#4972=CARTESIAN_POINT ( 'NONE',  ( 2.789999999999999147, -18.55949924794904504, 16.37294372382852004 ) ) ;
#4973=CARTESIAN_POINT ( 'NONE',  ( 8.000000000000000000, 0.000000000000000000, 0.000000000000000000 ) ) ;
#4981=ORIENTED_EDGE ( 'NONE', *, *, #15215, .T. ) ;
#4983=ORIENTED_EDGE ( 'NONE', *, *, #823, .F. ) ;
#4985=B_SPLINE_CURVE_WITH_KNOTS ( 'NONE', 3,
 ( #2734, #557, #7423, #12089, #11025, #10867 ),
 .UNSPECIFIED., .F., .F.,
 ( 4, 2, 4 ),
 ( 2.586195665736120714E-07, 0.001878649493629690539, 0.003757040367692807744 ),
 .UNSPECIFIED. ) ;
#4988=DIRECTION ( 'NONE',  ( -1.000000000000000000, -0.000000000000000000, -0.000000000000000000 ) ) ;
#4992=CARTESIAN_POINT ( 'NONE',  ( 0.07186815222488067423, -24.78765742476142719, 5.344160105508607650 ) ) ;
#4998=CARTESIAN_POINT ( 'NONE',  ( 2.790000000000077751, 12.51293083811798645, 20.85287692521934488 ) ) ;
#4999=EDGE_CURVE ( 'NONE', #11073, #6713, #9062, .T. ) ;
#5002=CARTESIAN_POINT ( 'NONE',  ( 2.601776091974071115, 25.40949241676360515, -5.251266773802107934 ) ) ;
#5004=ORIENTED_EDGE ( 'NONE', *, *, #11492, .F. ) ;
#5006=DIRECTION ( 'NONE',  ( -1.000000000000000000, 0.000000000000000000, -0.000000000000000000 ) ) ;
#5007=VERTEX_POINT ( 'NONE', #4512 ) ;
#5011=CARTESIAN_POINT ( 'NONE',  ( 2.262072769566602304, 11.57956866523218586, 24.43806413951680767 ) ) ;
#5013=CARTESIAN_POINT ( 'NONE',  ( 1.394999999999998685, 19.67366047555559661, -20.02152543075324331 ) ) ;
#5015=FACE_OUTER_BOUND ( 'NONE', #4473, .T. ) ;
#5017=B_SPLINE_CURVE_WITH_KNOTS ( 'NONE', 3,
 ( #5347, #10015, #6326, #11011, #6402, #474 ),
 .UNSPECIFIED., .F., .F.,
 ( 4, 2, 4 ),
 ( 4.462636731830560059E-07, 0.001879885066974964830, 0.003759323870276746679 ),
 .UNSPECIFIED. ) ;
#5022=ORIENTED_EDGE ( 'NONE', *, *, #13692, .T. ) ;
#5034=AXIS2_PLACEMENT_3D ( 'NONE', #6531, #5320, #4160 ) ;
#5039=CARTESIAN_POINT ( 'NONE',  ( 1.749999999999998002, 0.000000000000000000, 0.000000000000000000 ) ) ;
#5040=DIRECTION ( 'NONE',  ( 0.000000000000000000, 0.000000000000000000, 1.000000000000000000 ) ) ;
#5042=CARTESIAN_POINT ( 'NONE',  ( 0.02436607992776151574, 24.15498966839970052, -5.391175441198366336 ) ) ;
#5044=DIRECTION ( 'NONE',  ( 0.000000000000000000, 0.000000000000000000, 1.000000000000000000 ) ) ;
#5049=DIRECTION ( 'NONE',  ( -1.000000000000000000, -0.000000000000000000, -0.000000000000000000 ) ) ;
#5051=ADVANCED_FACE ( 'NONE', ( #4675 ), #12386, .T. ) ;
#5052=DIRECTION ( 'NONE',  ( -1.000000000000000000, 0.000000000000000000, 0.000000000000000000 ) ) ;
#5054=ORIENTED_EDGE ( 'NONE', *, *, #14433, .T. ) ;
#5061=VECTOR ( 'NONE', #4248, 1000.000000000000000 ) ;
#5065=ORIENTED_EDGE ( 'NONE', *, *, #14949, .F. ) ;
#5067=CARTESIAN_POINT ( 'NONE',  ( 0.006931054464084583991, -2.248820353273142558, 24.42321038836782776 ) ) ;
#5068=CARTESIAN_POINT ( 'NONE',  ( 2.789999999999999147, 20.70663861606272249, 15.04425356660767932 ) ) ;
#5075=CARTESIAN_POINT ( 'NONE',  ( 1.749999999999998002, 12.96210679857822257, -24.89775460606818669 ) ) ;
#5078=CARTESIAN_POINT ( 'NONE',  ( 0.000000000000000000, -22.25075486061732732, -9.324097380959701198 ) ) ;
#5085=CARTESIAN_POINT ( 'NONE',  ( 2.789999999999999147, -5.535312321042889394, 23.48180575137727999 ) ) ;
#5086=CARTESIAN_POINT ( 'NONE',  ( 1.039999999999997593, 0.000000000000000000, 0.000000000000000000 ) ) ;
#5088=ORIENTED_EDGE ( 'NONE', *, *, #9376, .T. ) ;
#5101=VECTOR ( 'NONE', #12315, 1000.000000000000000 ) ;
#5105=ORIENTED_EDGE ( 'NONE', *, *, #297, .T. ) ;
#5109=ORIENTED_EDGE ( 'NONE', *, *, #11056, .T. ) ;
#5110=CIRCLE ( 'NONE', #6080, 24.12539914357697413 ) ;
#5113=AXIS2_PLACEMENT_3D ( 'NONE', #7410, #475, #4882 ) ;
#5118=LINE ( 'NONE', #6103, #12369 ) ;
#5127=DIRECTION ( 'NONE',  ( -1.000000000000000000, 0.000000000000000000, 0.000000000000000000 ) ) ;
#5128=ORIENTED_EDGE ( 'NONE', *, *, #629, .T. ) ;
#5130=CARTESIAN_POINT ( 'NONE',  ( 2.765633920072235963, -16.37294372382871188, 18.55949924794887096 ) ) ;
#5133=ADVANCED_FACE ( 'NONE', ( #623 ), #4410, .T. ) ;
#5140=CARTESIAN_POINT ( 'NONE',  ( -2.179313406705571952E-17, -18.34424029220099683, -15.96500990068145853 ) ) ;
#5143=EDGE_CURVE ( 'NONE', #5459, #1104, #6692, .T. ) ;
#5146=AXIS2_PLACEMENT_3D ( 'NONE', #494, #9729, #14430 ) ;
#5151=CARTESIAN_POINT ( 'NONE',  ( 2.765633920072242624, -22.71065055754459650, 9.836394144775621129 ) ) ;
#5159=ORIENTED_EDGE ( 'NONE', *, *, #5870, .F. ) ;
#5162=CIRCLE ( 'NONE', #9324, 24.12539914357697768 ) ;
#5166=DIRECTION ( 'NONE',  ( 0.000000000000000000, 0.000000000000000000, 1.000000000000000000 ) ) ;
#5177=EDGE_CURVE ( 'NONE', #6579, #4492, #255, .T. ) ;
#5179=CARTESIAN_POINT ( 'NONE',  ( 2.789999999999999147, 2.680914349914567470E-13, -25.59481291497571220 ) ) ;
#5181=FACE_OUTER_BOUND ( 'NONE', #11108, .T. ) ;
#5187=ADVANCED_FACE ( 'NONE', ( #12307 ), #543, .F. ) ;
#5196=CARTESIAN_POINT ( 'NONE',  ( 1.394999999999999574, -19.67366047555515607, -20.02152543075367319 ) ) ;
#5197=CARTESIAN_POINT ( 'NONE',  ( 0.1855656748306449277, 2.851997810082009366, -25.77772010606602748 ) ) ;
#5200=DIRECTION ( 'NONE',  ( 0.000000000000000000, 0.000000000000000000, 1.000000000000000000 ) ) ;
#5202=VERTEX_POINT ( 'NONE', #12764 ) ;
#5203=ORIENTED_EDGE ( 'NONE', *, *, #8888, .T. ) ;
#5207=DIRECTION ( 'NONE',  ( 0.000000000000000000, 0.000000000000000000, 1.000000000000000000 ) ) ;
#5208=DIRECTION ( 'NONE',  ( 0.000000000000000000, 0.000000000000000000, 1.000000000000000000 ) ) ;
#5211=B_SPLINE_CURVE_WITH_KNOTS ( 'NONE', 3,
 ( #6157, #12225, #9911, #608 ),
 .UNSPECIFIED., .F., .F.,
 ( 4, 4 ),
 ( 2.135345996334758909E-07, 0.0006888010880211141137 ),
 .UNSPECIFIED. ) ;
#5221=DIRECTION ( 'NONE',  ( -1.000000000000000000, 0.000000000000000000, -0.000000000000000000 ) ) ;
#5227=DIRECTION ( 'NONE',  ( -1.000000000000000000, 0.000000000000000000, 0.000000000000000000 ) ) ;
#5229=CARTESIAN_POINT ( 'NONE',  ( 1.894165461959355756, 24.59696699259432151, 12.96989951879416303 ) ) ;
#5233=DIRECTION ( 'NONE',  ( -1.000000000000000000, -0.000000000000000000, -0.000000000000000000 ) ) ;
#5236=LINE ( 'NONE', #14603, #6312 ) ;
#5239=FACE_OUTER_BOUND ( 'NONE', #7350, .T. ) ;
#5240=DIRECTION ( 'NONE',  ( -1.000000000000000000, -0.000000000000000000, -0.000000000000000000 ) ) ;
#5242=EDGE_CURVE ( 'NONE', #11722, #10930, #8090, .T. ) ;
#5245=CARTESIAN_POINT ( 'NONE',  ( 0.000000000000000000, -7.909232158574647009, -24.34211360614308006 ) ) ;
#5247=EDGE_CURVE ( 'NONE', #6110, #7127, #3576, .T. ) ;
#5250=ORIENTED_EDGE ( 'NONE', *, *, #9934, .T. ) ;
#5251=ORIENTED_EDGE ( 'NONE', *, *, #12595, .F. ) ;
#5252=ORIENTED_EDGE ( 'NONE', *, *, #163, .F. ) ;
#5253=DIRECTION ( 'NONE',  ( -1.000000000000000000, 0.000000000000000000, -0.000000000000000000 ) ) ;
#5254=DIRECTION ( 'NONE',  ( 0.000000000000000000, 0.000000000000000000, -1.000000000000000000 ) ) ;
#5256=DIRECTION ( 'NONE',  ( -1.000000000000000000, 0.000000000000000000, 0.000000000000000000 ) ) ;
#5258=B_SPLINE_CURVE_WITH_KNOTS ( 'NONE', 3,
 ( #11570, #11791, #4597, #14107 ),
 .UNSPECIFIED., .F., .F.,
 ( 4, 4 ),
 ( 2.324263106244687463E-07, 0.0006888201370294697295 ),
 .UNSPECIFIED. ) ;
#5259=ORIENTED_EDGE ( 'NONE', *, *, #14729, .F. ) ;
#5263=EDGE_CURVE ( 'NONE', #13607, #11809, #859, .T. ) ;
#5275=ORIENTED_EDGE ( 'NONE', *, *, #13403, .T. ) ;
#5276=CARTESIAN_POINT ( 'NONE',  ( -5.435144416706554624E-16, -9.514945144208892813, 22.37986894186668962 ) ) ;
#5278=EDGE_CURVE ( 'NONE', #1971, #1373, #780, .T. ) ;
#5280=CARTESIAN_POINT ( 'NONE',  ( 0.5321745407694753460, 26.58873630738052185, 4.993157874727903511 ) ) ;
#5282=CARTESIAN_POINT ( 'NONE',  ( 2.718131885465892683, -18.89333555428565603, 16.91241718341992240 ) ) ;
#5285=CARTESIAN_POINT ( 'NONE',  ( 0.000000000000000000, 0.000000000000000000, 0.000000000000000000 ) ) ;
#5295=CARTESIAN_POINT ( 'NONE',  ( 1.039999999999997593, 0.000000000000000000, 0.000000000000000000 ) ) ;
#5306=CYLINDRICAL_SURFACE ( 'NONE', #14786, 13.19999999999999929 ) ;
#5307=AXIS2_PLACEMENT_3D ( 'NONE', #4795, #11912, #7164 ) ;
#5310=EDGE_CURVE ( 'NONE', #3792, #3345, #7365, .T. ) ;
#5311=LINE ( 'NONE', #12518, #5326 ) ;
#5319=CYLINDRICAL_SURFACE ( 'NONE', #7078, 13.19999999999999929 ) ;
#5320=DIRECTION ( 'NONE',  ( -1.000000000000000000, -0.000000000000000000, -0.000000000000000000 ) ) ;
#5326=VECTOR ( 'NONE', #4295, 1000.000000000000000 ) ;
#5329=ORIENTED_EDGE ( 'NONE', *, *, #3917, .T. ) ;
#5335=CARTESIAN_POINT ( 'NONE',  ( 1.998465710409312357E-16, 22.37986894186671805, 9.514945144208807548 ) ) ;
#5337=AXIS2_PLACEMENT_3D ( 'NONE', #3385, #8074, #2230 ) ;
#5342=VECTOR ( 'NONE', #2492, 1000.000000000000000 ) ;
#5346=EDGE_CURVE ( 'NONE', #7127, #13239, #14229, .T. ) ;
#5347=CARTESIAN_POINT ( 'NONE',  ( 1.039999999999996705, 27.76164181293051669, -4.147968289691385202 ) ) ;
#5352=DIRECTION ( 'NONE',  ( -1.000000000000000000, 0.000000000000000000, 0.000000000000000000 ) ) ;
#5360=ORIENTED_EDGE ( 'NONE', *, *, #9566, .F. ) ;
#5364=EDGE_CURVE ( 'NONE', #5007, #14821, #14070, .T. ) ;
#5368=ORIENTED_EDGE ( 'NONE', *, *, #14561, .T. ) ;
#5378=CARTESIAN_POINT ( 'NONE',  ( 2.789999999999999147, 24.44424927289185945, -0.2301004812058395077 ) ) ;
#5379=DIRECTION ( 'NONE',  ( -1.000000000000000000, 0.000000000000000000, 0.000000000000000000 ) ) ;
#5380=CARTESIAN_POINT ( 'NONE',  ( 2.031033471609899888, -3.797536611356125746, -27.31260702007179830 ) ) ;
#5382=CARTESIAN_POINT ( 'NONE',  ( 2.765633920072235963, 24.63872515616082737, 2.336989772644355146 ) ) ;
#5385=ORIENTED_EDGE ( 'NONE', *, *, #3558, .F. ) ;
#5386=CARTESIAN_POINT ( 'NONE',  ( 0.000000000000000000, -9.324097380959319281, -22.25075486061748009 ) ) ;
#5395=ORIENTED_EDGE ( 'NONE', *, *, #434, .F. ) ;
#5396=ORIENTED_EDGE ( 'NONE', *, *, #313, .T. ) ;
#5400=DIRECTION ( 'NONE',  ( -1.000000000000000000, 0.000000000000000000, -0.000000000000000000 ) ) ;
#5401=DIRECTION ( 'NONE',  ( 0.000000000000000000, 0.000000000000000000, 1.000000000000000000 ) ) ;
#5405=EDGE_CURVE ( 'NONE', #9117, #13730, #5162, .T. ) ;
#5408=CARTESIAN_POINT ( 'NONE',  ( 2.765633920072235963, 21.30679549418649543, -12.59161484032888723 ) ) ;
#5409=ORIENTED_EDGE ( 'NONE', *, *, #12161, .F. ) ;
#5413=AXIS2_PLACEMENT_3D ( 'NONE', #1471, #6155, #10839 ) ;
#5415=EDGE_CURVE ( 'NONE', #807, #6110, #12902, .T. ) ;
#5418=DIRECTION ( 'NONE',  ( -1.000000000000000000, -0.000000000000000000, 0.000000000000000000 ) ) ;
#5419=EDGE_LOOP ( 'NONE', ( #6375, #9137, #9506, #6662, #12173, #120, #9828, #13316 ) ) ;
#5420=CARTESIAN_POINT ( 'NONE',  ( 2.765633920072235519, -9.836394144775869819, 22.71065055754449347 ) ) ;
#5421=CARTESIAN_POINT ( 'NONE',  ( 0.006930995026450773554, -23.92277630352799278, 5.408431875071351591 ) ) ;
#5428=ORIENTED_EDGE ( 'NONE', *, *, #1210, .T. ) ;
#5433=EDGE_CURVE ( 'NONE', #9763, #2063, #2474, .T. ) ;
#5438=VERTEX_POINT ( 'NONE', #14231 ) ;
#5439=CARTESIAN_POINT ( 'NONE',  ( 0.7589665203264078785, 19.12621924769895898, -19.86422722021291776 ) ) ;
#5441=ORIENTED_EDGE ( 'NONE', *, *, #14955, .T. ) ;
#5445=CARTESIAN_POINT ( 'NONE',  ( 2.765633920072235963, -5.391175441198450713, -24.15498966839968276 ) ) ;
#5452=DIRECTION ( 'NONE',  ( -1.000000000000000000, 0.000000000000000000, 0.000000000000000000 ) ) ;
#5455=DIRECTION ( 'NONE',  ( -1.000000000000000000, 0.000000000000000000, -0.000000000000000000 ) ) ;
#5456=EDGE_CURVE ( 'NONE', #10374, #11429, #13464, .T. ) ;
#5459=VERTEX_POINT ( 'NONE', #9845 ) ;
#5460=ADVANCED_FACE ( 'NONE', ( #5015 ), #9907, .T. ) ;
#5462=FACE_OUTER_BOUND ( 'NONE', #3486, .T. ) ;
#5467=DIRECTION ( 'NONE',  ( 0.000000000000000000, 0.000000000000000000, 1.000000000000000000 ) ) ;
#5468=DIRECTION ( 'NONE',  ( -1.000000000000000000, -0.000000000000000000, -0.000000000000000000 ) ) ;
#5471=CIRCLE ( 'NONE', #14038, 2.524999999999998135 ) ;
#5472=CARTESIAN_POINT ( 'NONE',  ( 1.039999999999995373, 25.12109765559670649, -12.52377138324197681 ) ) ;
#5473=CARTESIAN_POINT ( 'NONE',  ( 0.07186815222488118771, 24.78765742476146272, -5.344160105508446001 ) ) ;
#5474=ORIENTED_EDGE ( 'NONE', *, *, #4943, .T. ) ;
#5476=DIRECTION ( 'NONE',  ( 0.000000000000000000, 0.000000000000000000, 1.000000000000000000 ) ) ;
#5480=AXIS2_PLACEMENT_3D ( 'NONE', #1891, #14966, #11181 ) ;
#5482=VERTEX_POINT ( 'NONE', #4162 ) ;
#5491=CARTESIAN_POINT ( 'NONE',  ( 0.000000000000000000, -23.48180575137727288, -5.535312321042949790 ) ) ;
#5492=CARTESIAN_POINT ( 'NONE',  ( 2.765633920072239516, -24.15498966839958683, -5.391175441198872598 ) ) ;
#5501=CARTESIAN_POINT ( 'NONE',  ( 0.7589665203264103210, -19.12621924769880977, 19.86422722021305631 ) ) ;
#5503=B_SPLINE_CURVE_WITH_KNOTS ( 'NONE', 3,
 ( #3637, #9260, #6877, #2488 ),
 .UNSPECIFIED., .F., .F.,
 ( 4, 4 ),
 ( 0.005342776758202955750, 0.005948405594583417583 ),
 .UNSPECIFIED. ) ;
#5504=DIRECTION ( 'NONE',  ( -1.000000000000000000, 0.000000000000000000, -0.000000000000000000 ) ) ;
#5505=ORIENTED_EDGE ( 'NONE', *, *, #12994, .F. ) ;
#5506=CARTESIAN_POINT ( 'NONE',  ( 0.7589665203264061022, 19.86422722021312026, 19.12621924769873161 ) ) ;
#5509=CARTESIAN_POINT ( 'NONE',  ( 0.000000000000000000, -5.535312321042921369, 23.48180575137728354 ) ) ;
#5510=ADVANCED_FACE ( 'NONE', ( #4079 ), #14611, .F. ) ;
#5514=EDGE_CURVE ( 'NONE', #8417, #910, #6494, .T. ) ;
#5520=DIRECTION ( 'NONE',  ( -1.000000000000000000, 0.000000000000000000, -0.000000000000000000 ) ) ;
#5522=DIRECTION ( 'NONE',  ( 1.000000000000000000, 0.000000000000000000, 0.000000000000000000 ) ) ;
#5523=CARTESIAN_POINT ( 'NONE',  ( 0.02436607992776021470, 21.30679549418649543, -12.59161484032888723 ) ) ;
#5524=EDGE_CURVE ( 'NONE', #4654, #12548, #13450, .T. ) ;
#5525=VERTEX_POINT ( 'NONE', #7546 ) ;
#5527=DIRECTION ( 'NONE',  ( 1.000000000000000000, 0.000000000000000000, 0.000000000000000000 ) ) ;
#5530=AXIS2_PLACEMENT_3D ( 'NONE', #15086, #15171, #7866 ) ;
#5532=CIRCLE ( 'NONE', #5769, 24.12539914357697413 ) ;
#5536=ORIENTED_EDGE ( 'NONE', *, *, #12554, .T. ) ;
#5538=LINE ( 'NONE', #986, #8522 ) ;
#5539=ORIENTED_EDGE ( 'NONE', *, *, #622, .T. ) ;
#5540=DIRECTION ( 'NONE',  ( 0.000000000000000000, 0.000000000000000000, 1.000000000000000000 ) ) ;
#5542=CARTESIAN_POINT ( 'NONE',  ( 1.749999999999998002, 20.02152543075346003, 19.67366047555537634 ) ) ;
#5543=AXIS2_PLACEMENT_3D ( 'NONE', #748, #14815, #14976 ) ;
#5547=CARTESIAN_POINT ( 'NONE',  ( 0.1855657389739081564, 25.39738473785008210, -5.253342437939463316 ) ) ;
#5549=ORIENTED_EDGE ( 'NONE', *, *, #589, .F. ) ;
#5554=SURFACE_STYLE_USAGE ( .BOTH. , #701 ) ;
#5555=AXIS2_PLACEMENT_3D ( 'NONE', #4089, #8769, #6545 ) ;
#5559=CARTESIAN_POINT ( 'NONE',  ( 2.257825467309738432, 26.83036154824994313, 3.467596033028380376 ) ) ;
#5560=DIRECTION ( 'NONE',  ( 0.000000000000000000, 0.000000000000000000, -1.000000000000000000 ) ) ;
#5561=CARTESIAN_POINT ( 'NONE',  ( 1.039999999999996927, 4.633866840649313090, -27.68468304288253634 ) ) ;
#5568=EDGE_CURVE ( 'NONE', #8616, #7008, #11762, .T. ) ;
#5570=EDGE_LOOP ( 'NONE', ( #3462, #2938, #1531, #5109, #1897, #712, #9801, #2271 ) ) ;
#5572=VECTOR ( 'NONE', #7977, 1000.000000000000000 ) ;
#5573=CARTESIAN_POINT ( 'NONE',  ( 0.1882239080259267838, -25.40949241676349146, -5.251266773802644394 ) ) ;
#5579=ORIENTED_EDGE ( 'NONE', *, *, #2673, .T. ) ;
#5581=AXIS2_PLACEMENT_3D ( 'NONE', #9611, #2476, #8375 ) ;
#5584=ORIENTED_EDGE ( 'NONE', *, *, #9700, .T. ) ;
#5585=LINE ( 'NONE', #3203, #2270 ) ;
#5589=CARTESIAN_POINT ( 'NONE',  ( 0.1855655959470668692, 17.45907811351482763, -19.17825124759758282 ) ) ;
#5595=EDGE_CURVE ( 'NONE', #9825, #4705, #467, .T. ) ;
#5602=CIRCLE ( 'NONE', #14179, 28.06981291497571007 ) ;
#5610=DIRECTION ( 'NONE',  ( -1.000000000000000000, -0.000000000000000000, 0.000000000000000000 ) ) ;
#5611=VERTEX_POINT ( 'NONE', #10144 ) ;
#5613=EDGE_LOOP ( 'NONE', ( #13417, #7390, #11918, #7017, #13337, #1941, #2852 ) ) ;
#5614=DIRECTION ( 'NONE',  ( -1.000000000000000000, 0.000000000000000000, -0.000000000000000000 ) ) ;
#5616=EDGE_CURVE ( 'NONE', #8705, #3394, #1962, .T. ) ;
#5617=ORIENTED_EDGE ( 'NONE', *, *, #5524, .F. ) ;
#5621=CARTESIAN_POINT ( 'NONE',  ( 0.5279273620711166792, -12.96450951081199499, -23.73240184472509995 ) ) ;
#5622=CARTESIAN_POINT ( 'NONE',  ( 2.783069004973551142, 5.408431875071779693, -23.92277630352788975 ) ) ;
#5626=VECTOR ( 'NONE', #1120, 1000.000000000000000 ) ;
#5630=FILL_AREA_STYLE_COLOUR ( '', #9484 ) ;
#5632=VERTEX_POINT ( 'NONE', #4536 ) ;
#5639=VECTOR ( 'NONE', #14577, 1000.000000000000000 ) ;
#5643=VERTEX_POINT ( 'NONE', #13758 ) ;
#5644=CARTESIAN_POINT ( 'NONE',  ( 0.07186808533286681566, 23.19485392143213431, 10.24630254990524314 ) ) ;
#5646=EDGE_CURVE ( 'NONE', #1055, #15005, #9118, .T. ) ;
#5648=CARTESIAN_POINT ( 'NONE',  ( 1.394999999999999574, 4.633866840648922292, 27.68468304288260384 ) ) ;
#5649=EDGE_CURVE ( 'NONE', #1849, #5700, #1221, .T. ) ;
#5652=LINE ( 'NONE', #5794, #1607 ) ;
#5654=ORIENTED_EDGE ( 'NONE', *, *, #3088, .T. ) ;
#5659=ORIENTED_EDGE ( 'NONE', *, *, #5735, .T. ) ;
#5660=LINE ( 'NONE', #4806, #12213 ) ;
#5665=EDGE_LOOP ( 'NONE', ( #1498, #11549, #13230, #1950, #72, #11784 ) ) ;
#5667=DIRECTION ( 'NONE',  ( 0.000000000000000000, 0.000000000000000000, 1.000000000000000000 ) ) ;
#5671=B_SPLINE_CURVE_WITH_KNOTS ( 'NONE', 3,
 ( #15116, #12786, #8039, #2272 ),
 .UNSPECIFIED., .F., .F.,
 ( 4, 4 ),
 ( 2.034713381942770033E-07, 0.0006887909409525396235 ),
 .UNSPECIFIED. ) ;
#5674=CARTESIAN_POINT ( 'NONE',  ( 2.262072661820534236, -26.82026385750180353, 3.461047254864169975 ) ) ;
#5677=CARTESIAN_POINT ( 'NONE',  ( 2.789999999999999147, 18.28042085475278355, 15.74360496233388140 ) ) ;
#5682=CARTESIAN_POINT ( 'NONE',  ( 1.039999999999997593, 0.000000000000000000, 0.000000000000000000 ) ) ;
#5683=DIRECTION ( 'NONE',  ( 0.000000000000000000, 0.000000000000000000, 1.000000000000000000 ) ) ;
#5686=DIRECTION ( 'NONE',  ( -1.000000000000000000, -0.000000000000000000, 0.000000000000000000 ) ) ;
#5687=CARTESIAN_POINT ( 'NONE',  ( 2.765633920072235075, 24.63872515616082737, -2.336989772644355590 ) ) ;
#5690=CARTESIAN_POINT ( 'NONE',  ( 2.789679245949062913, -20.70663861606260525, -12.51925356660783528 ) ) ;
#5691=CARTESIAN_POINT ( 'NONE',  ( 2.789999999999999147, -7.909232158574988958, 24.34211360614297348 ) ) ;
#5694=EDGE_LOOP ( 'NONE', ( #14539, #8274, #9256, #3628, #6627, #13216 ) ) ;
#5696=B_SPLINE_CURVE_WITH_KNOTS ( 'NONE', 3,
 ( #11699, #5804, #4728, #6949 ),
 .UNSPECIFIED., .F., .F.,
 ( 4, 4 ),
 ( 2.324263106257895883E-07, 0.0006888201370294903293 ),
 .UNSPECIFIED. ) ;
#5697=CARTESIAN_POINT ( 'NONE',  ( -10.00000000000000000, 0.000000000000000000, 0.000000000000000000 ) ) ;
#5700=VERTEX_POINT ( 'NONE', #12451 ) ;
#5701=ORIENTED_EDGE ( 'NONE', *, *, #2041, .T. ) ;
#5703=CARTESIAN_POINT ( 'NONE',  ( 0.000000000000000000, 0.000000000000000000, 0.000000000000000000 ) ) ;
#5707=CARTESIAN_POINT ( 'NONE',  ( 1.749999999999998002, 0.000000000000000000, 0.000000000000000000 ) ) ;
#5710=EDGE_LOOP ( 'NONE', ( #8346, #2385, #8381, #11179 ) ) ;
#5714=AXIS2_PLACEMENT_3D ( 'NONE', #879, #12331, #10262 ) ;
#5716=ORIENTED_EDGE ( 'NONE', *, *, #10856, .T. ) ;
#5722=DIRECTION ( 'NONE',  ( -1.000000000000000000, -0.000000000000000000, -0.000000000000000000 ) ) ;
#5727=LINE ( 'NONE', #9471, #15206 ) ;
#5734=VERTEX_POINT ( 'NONE', #9518 ) ;
#5735=EDGE_CURVE ( 'NONE', #10191, #7336, #13690, .T. ) ;
#5736=VERTEX_POINT ( 'NONE', #10448 ) ;
#5739=DIRECTION ( 'NONE',  ( -1.000000000000000000, 0.000000000000000000, 0.000000000000000000 ) ) ;
#5744=VERTEX_POINT ( 'NONE', #10530 ) ;
#5745=CYLINDRICAL_SURFACE ( 'NONE', #7343, 28.06981291497571362 ) ;
#5747=CARTESIAN_POINT ( 'NONE',  ( 1.039999999999996705, 19.67366047555530173, 20.02152543075352398 ) ) ;
#5750=CARTESIAN_POINT ( 'NONE',  ( 2.789999999999999147, -19.64056340710864745, -14.55412442567638287 ) ) ;
#5755=ORIENTED_EDGE ( 'NONE', *, *, #10306, .T. ) ;
#5756=DIRECTION ( 'NONE',  ( 0.000000000000000000, 0.000000000000000000, 1.000000000000000000 ) ) ;
#5758=ORIENTED_EDGE ( 'NONE', *, *, #6245, .T. ) ;
#5760=DIRECTION ( 'NONE',  ( -1.000000000000000000, -0.000000000000000000, -0.000000000000000000 ) ) ;
#5762=CARTESIAN_POINT ( 'NONE',  ( 1.039999999999995373, 12.96210679857822434, -24.89775460606817958 ) ) ;
#5763=B_SPLINE_CURVE_WITH_KNOTS ( 'NONE', 3,
 ( #12318, #11167, #638, #5573, #9389, #11390 ),
 .UNSPECIFIED., .F., .F.,
 ( 4, 2, 4 ),
 ( 4.462636678184503380E-07, 0.001879885020955184395, 0.003759323778242550443 ),
 .UNSPECIFIED. ) ;
#5766=CIRCLE ( 'NONE', #8448, 24.12539914357697768 ) ;
#5767=VERTEX_POINT ( 'NONE', #15145 ) ;
#5768=DIRECTION ( 'NONE',  ( 0.000000000000000000, 0.000000000000000000, 1.000000000000000000 ) ) ;
#5769=AXIS2_PLACEMENT_3D ( 'NONE', #7684, #11216, #3232 ) ;
#5785=DIRECTION ( 'NONE',  ( -1.000000000000000000, -0.000000000000000000, -0.000000000000000000 ) ) ;
#5789=CIRCLE ( 'NONE', #7249, 28.06981291497571007 ) ;
#5794=CARTESIAN_POINT ( 'NONE',  ( 1.394999999999998685, 24.89775460606832524, 12.96210679857795256 ) ) ;
#5796=ORIENTED_EDGE ( 'NONE', *, *, #13281, .T. ) ;
#5798=ADVANCED_FACE ( 'NONE', ( #3675 ), #8359, .F. ) ;
#5800=B_SPLINE_CURVE_WITH_KNOTS ( 'NONE', 3,
 ( #7555, #12305, #7698, #13300 ),
 .UNSPECIFIED., .F., .F.,
 ( 4, 4 ),
 ( 2.034713381942717623E-07, 0.0006887909409525284563 ),
 .UNSPECIFIED. ) ;
#5803=CARTESIAN_POINT ( 'NONE',  ( 0.02436607992776238310, -2.336989772644097574, -24.63872515616085224 ) ) ;
#5804=CARTESIAN_POINT ( 'NONE',  ( 2.783025306068356741, 18.43727551351032190, 16.17543236987995314 ) ) ;
#5806=CARTESIAN_POINT ( 'NONE',  ( 2.765633920072238183, -5.391175441198789109, 24.15498966839961170 ) ) ;
#5812=ORIENTED_EDGE ( 'NONE', *, *, #8796, .F. ) ;
#5815=CARTESIAN_POINT ( 'NONE',  ( 0.07181524296601660140, -16.91181672897718968, -18.89296398180210446 ) ) ;
#5829=DIRECTION ( 'NONE',  ( -1.000000000000000000, 0.000000000000000000, 0.000000000000000000 ) ) ;
#5834=ORIENTED_EDGE ( 'NONE', *, *, #4250, .F. ) ;
#5835=ORIENTED_EDGE ( 'NONE', *, *, #7099, .F. ) ;
#5843=CARTESIAN_POINT ( 'NONE',  ( 1.394999999999999574, -12.96210679857767900, -24.89775460606846380 ) ) ;
#5844=CARTESIAN_POINT ( 'NONE',  ( 0.000000000000000000, 23.48180575137729775, 5.535312321042836103 ) ) ;
#5851=VECTOR ( 'NONE', #6614, 1000.000000000000000 ) ;
#5852=ORIENTED_EDGE ( 'NONE', *, *, #5999, .T. ) ;
#5855=ORIENTED_EDGE ( 'NONE', *, *, #3571, .T. ) ;
#5857=VERTEX_POINT ( 'NONE', #11115 ) ;
#5862=CARTESIAN_POINT ( 'NONE',  ( 2.789999999999999147, -15.74360496233368245, -18.28042085475295409 ) ) ;
#5867=AXIS2_PLACEMENT_3D ( 'NONE', #7120, #4679, #1206 ) ;
#5869=DIRECTION ( 'NONE',  ( 0.000000000000000000, 0.8090169943749400128, 0.5877852522924831291 ) ) ;
#5870=EDGE_CURVE ( 'NONE', #13727, #12150, #13273, .T. ) ;
#5871=VECTOR ( 'NONE', #3454, 1000.000000000000000 ) ;
#5880=ORIENTED_EDGE ( 'NONE', *, *, #15083, .F. ) ;
#5884=CARTESIAN_POINT ( 'NONE',  ( 0.000000000000000000, 24.04302995059966719, 1.991882183130389228 ) ) ;
#5885=B_SPLINE_CURVE_WITH_KNOTS ( 'NONE', 3,
 ( #4576, #3337, #5947, #8027 ),
 .UNSPECIFIED., .F., .F.,
 ( 4, 4 ),
 ( 1.981826382900813409E-07, 0.0006887856082032195850 ),
 .UNSPECIFIED. ) ;
#5889=EDGE_LOOP ( 'NONE', ( #13203, #9342, #2599, #12409, #781, #11600 ) ) ;
#5893=DIRECTION ( 'NONE',  ( 0.000000000000000000, 0.000000000000000000, 1.000000000000000000 ) ) ;
#5896=DIRECTION ( 'NONE',  ( 0.000000000000000000, 0.000000000000000000, 1.000000000000000000 ) ) ;
#5905=ADVANCED_FACE ( 'NONE', ( #431 ), #277, .T. ) ;
#5908=ORIENTED_EDGE ( 'NONE', *, *, #12475, .F. ) ;
#5910=CARTESIAN_POINT ( 'NONE',  ( 0.02436607992775978102, 24.63872515616082737, 2.336989772644355146 ) ) ;
#5915=DIRECTION ( 'NONE',  ( 0.000000000000000000, 0.000000000000000000, 1.000000000000000000 ) ) ;
#5916=DIRECTION ( 'NONE',  ( -1.000000000000000000, -0.000000000000000000, -0.000000000000000000 ) ) ;
#5917=CARTESIAN_POINT ( 'NONE',  ( 0.5279273381794601372, -26.82026385750175734, -3.461047254864539457 ) ) ;
#5920=EDGE_CURVE ( 'NONE', #14821, #6969, #3240, .T. ) ;
#5926=ORIENTED_EDGE ( 'NONE', *, *, #2132, .T. ) ;
#5928=ORIENTED_EDGE ( 'NONE', *, *, #14613, .F. ) ;
#5930=FACE_OUTER_BOUND ( 'NONE', #8748, .T. ) ;
#5933=LINE ( 'NONE', #5013, #2319 ) ;
#5939=CARTESIAN_POINT ( 'NONE',  ( 2.789999999999999147, 9.836394144775706394, 22.71065055754456097 ) ) ;
#5940=VERTEX_POINT ( 'NONE', #13111 ) ;
#5942=FACE_OUTER_BOUND ( 'NONE', #10804, .T. ) ;
#5947=CARTESIAN_POINT ( 'NONE',  ( 2.790000000000077307, 23.69897269326684963, -5.456611084821608948 ) ) ;
#5950=DIRECTION ( 'NONE',  ( 0.000000000000000000, 0.000000000000000000, 1.000000000000000000 ) ) ;
#5951=CARTESIAN_POINT ( 'NONE',  ( 2.030753610301984313, -19.86438386685646762, -19.12676442129367516 ) ) ;
#5952=ORIENTED_EDGE ( 'NONE', *, *, #1290, .F. ) ;
#5954=B_SPLINE_CURVE_WITH_KNOTS ( 'NONE', 3,
 ( #9699, #9546, #14239, #3547, #2634, #3698 ),
 .UNSPECIFIED., .F., .F.,
 ( 4, 2, 4 ),
 ( 4.462636882235905044E-07, 0.001879885203074807597, 0.003759324142461391294 ),
 .UNSPECIFIED. ) ;
#5955=ORIENTED_EDGE ( 'NONE', *, *, #9652, .T. ) ;
#5959=FACE_OUTER_BOUND ( 'NONE', #11800, .T. ) ;
#5968=VERTEX_POINT ( 'NONE', #3912 ) ;
#5983=ORIENTED_EDGE ( 'NONE', *, *, #5433, .F. ) ;
#5990=EDGE_LOOP ( 'NONE', ( #9704, #14716, #1978, #8144, #8296, #9390, #12535 ) ) ;
#5992=ORIENTED_EDGE ( 'NONE', *, *, #12297, .T. ) ;
#5999=EDGE_CURVE ( 'NONE', #14273, #11143, #13495, .T. ) ;
#6004=B_SPLINE_CURVE_WITH_KNOTS ( 'NONE', 3,
 ( #2358, #15130, #11796, #9286 ),
 .UNSPECIFIED., .F., .F.,
 ( 4, 4 ),
 ( 0.005258110598983630792, 0.005948376585272738271 ),
 .UNSPECIFIED. ) ;
#6008=CIRCLE ( 'NONE', #14609, 2.524999999999996358 ) ;
#6013=EDGE_LOOP ( 'NONE', ( #4207, #3899, #11599, #7553 ) ) ;
#6014=ORIENTED_EDGE ( 'NONE', *, *, #9193, .T. ) ;
#6017=ORIENTED_EDGE ( 'NONE', *, *, #795, .T. ) ;
#6020=CARTESIAN_POINT ( 'NONE',  ( 2.765633920072242624, -22.71065055754459650, 9.836394144775621129 ) ) ;
#6023=CARTESIAN_POINT ( 'NONE',  ( 2.765633920072239516, -24.15498966839958683, -5.391175441198872598 ) ) ;
#6024=VERTEX_POINT ( 'NONE', #892 ) ;
#6027=VERTEX_POINT ( 'NONE', #13656 ) ;
#6029=VECTOR ( 'NONE', #9918, 1000.000000000000000 ) ;
#6034=CARTESIAN_POINT ( 'NONE',  ( 2.790000000000076419, 9.515416771311512534, -22.38018801136466251 ) ) ;
#6035=CARTESIAN_POINT ( 'NONE',  ( 0.000000000000000000, -7.909232158574647009, -24.34211360614308006 ) ) ;
#6038=ADVANCED_FACE ( 'NONE', ( #9127 ), #6817, .T. ) ;
#6040=B_SPLINE_CURVE_WITH_KNOTS ( 'NONE', 3,
 ( #1652, #5276, #14939, #8002 ),
 .UNSPECIFIED., .F., .F.,
 ( 4, 4 ),
 ( 0.005258105385878676132, 0.005948373736081387537 ),
 .UNSPECIFIED. ) ;
#6042=VERTEX_POINT ( 'NONE', #816 ) ;
#6044=DIRECTION ( 'NONE',  ( -1.000000000000000000, 0.000000000000000000, -0.000000000000000000 ) ) ;
#6045=DIRECTION ( 'NONE',  ( 1.000000000000000000, 0.000000000000000000, 0.000000000000000000 ) ) ;
#6048=ORIENTED_EDGE ( 'NONE', *, *, #364, .T. ) ;
#6049=EDGE_CURVE ( 'NONE', #852, #7933, #7259, .T. ) ;
#6051=ORIENTED_EDGE ( 'NONE', *, *, #4622, .T. ) ;
#6064=VERTEX_POINT ( 'NONE', #13578 ) ;
#6067=ORIENTED_EDGE ( 'NONE', *, *, #6769, .F. ) ;
#6068=CIRCLE ( 'NONE', #8029, 2.524999999999995470 ) ;
#6072=ORIENTED_EDGE ( 'NONE', *, *, #6135, .F. ) ;
#6073=ORIENTED_EDGE ( 'NONE', *, *, #7802, .T. ) ;
#6076=LINE ( 'NONE', #7392, #12458 ) ;
#6077=LINE ( 'NONE', #4709, #8290 ) ;
#6080=AXIS2_PLACEMENT_3D ( 'NONE', #2064, #6754, #908 ) ;
#6081=CARTESIAN_POINT ( 'NONE',  ( 2.765633920072241292, 18.55949924794916228, -16.37294372382838148 ) ) ;
#6088=EDGE_CURVE ( 'NONE', #4492, #368, #5258, .T. ) ;
#6092=LINE ( 'NONE', #5939, #4562 ) ;
#6093=ORIENTED_EDGE ( 'NONE', *, *, #5310, .F. ) ;
#6102=EDGE_CURVE ( 'NONE', #14952, #14366, #3575, .T. ) ;
#6103=CARTESIAN_POINT ( 'NONE',  ( 2.789999999999999147, 2.680914349914567470E-13, -23.06981291497571362 ) ) ;
#6104=CARTESIAN_POINT ( 'NONE',  ( 2.718131847775120402, -24.78765742476134548, -5.344160105508965586 ) ) ;
#6106=VERTEX_POINT ( 'NONE', #1048 ) ;
#6108=EDGE_CURVE ( 'NONE', #7234, #1971, #10012, .T. ) ;
#6110=VERTEX_POINT ( 'NONE', #6963 ) ;
#6111=CARTESIAN_POINT ( 'NONE',  ( 2.789999999999999147, -18.28042085475266276, -15.74360496233401996 ) ) ;
#6114=CARTESIAN_POINT ( 'NONE',  ( 0.006974674093433583938, -24.42374957165207405, 2.249040938978413173 ) ) ;
#6118=CARTESIAN_POINT ( 'NONE',  ( 0.1882239080259273667, 5.251266773802727883, -25.40949241676348080 ) ) ;
#6121=VERTEX_POINT ( 'NONE', #13017 ) ;
#6125=FACE_OUTER_BOUND ( 'NONE', #5665, .T. ) ;
#6132=LINE ( 'NONE', #5843, #3373 ) ;
#6135=EDGE_CURVE ( 'NONE', #11582, #7330, #12017, .T. ) ;
#6137=ORIENTED_EDGE ( 'NONE', *, *, #3281, .F. ) ;
#6139=CARTESIAN_POINT ( 'NONE',  ( 0.02436607992776021470, 21.30679549418649543, -12.59161484032888723 ) ) ;
#6140=VERTEX_POINT ( 'NONE', #2352 ) ;
#6148=ORIENTED_EDGE ( 'NONE', *, *, #10018, .T. ) ;
#6154=DIRECTION ( 'NONE',  ( 0.000000000000000000, 0.000000000000000000, -1.000000000000000000 ) ) ;
#6155=DIRECTION ( 'NONE',  ( -1.000000000000000000, -0.000000000000000000, -0.000000000000000000 ) ) ;
#6157=CARTESIAN_POINT ( 'NONE',  ( 2.765633920072236407, -2.336989772644440855, 24.63872515616082026 ) ) ;
#6164=ORIENTED_EDGE ( 'NONE', *, *, #15118, .F. ) ;
#6166=DIRECTION ( 'NONE',  ( 0.000000000000000000, 0.000000000000000000, 1.000000000000000000 ) ) ;
#6175=EDGE_LOOP ( 'NONE', ( #14093, #5755, #1584, #13044 ) ) ;
#6176=CARTESIAN_POINT ( 'NONE',  ( 2.601776105308176934, 2.857713464479052057, -25.78859396478524957 ) ) ;
#6178=ORIENTED_EDGE ( 'NONE', *, *, #15096, .T. ) ;
#6184=FACE_OUTER_BOUND ( 'NONE', #5570, .T. ) ;
#6186=AXIS2_PLACEMENT_3D ( 'NONE', #14899, #12580, #11200 ) ;
#6187=DIRECTION ( 'NONE',  ( 0.000000000000000000, 0.000000000000000000, 1.000000000000000000 ) ) ;
#6192=ORIENTED_EDGE ( 'NONE', *, *, #14537, .F. ) ;
#6194=B_SPLINE_CURVE_WITH_KNOTS ( 'NONE', 3,
 ( #8238, #7096, #13063, #4800 ),
 .UNSPECIFIED., .F., .F.,
 ( 4, 4 ),
 ( 3.059063720760159520E-07, 0.0006888942284914164422 ),
 .UNSPECIFIED. ) ;
#6196=DIRECTION ( 'NONE',  ( 0.000000000000000000, 0.000000000000000000, 1.000000000000000000 ) ) ;
#6199=TOROIDAL_SURFACE ( 'NONE', #2768, 24.12539914357697768, 8.000000000000000000 ) ;
#6205=CARTESIAN_POINT ( 'NONE',  ( 0.000000000000000000, -1.991882183130475603, 24.04302995059966719 ) ) ;
#6207=DIRECTION ( 'NONE',  ( 0.000000000000000000, 0.000000000000000000, 1.000000000000000000 ) ) ;
#6209=CARTESIAN_POINT ( 'NONE',  ( 1.394999999999999574, 19.67366047555530528, 20.02152543075352753 ) ) ;
#6213=CARTESIAN_POINT ( 'NONE',  ( 1.039999999999997593, 0.000000000000000000, 0.000000000000000000 ) ) ;
#6214=ORIENTED_EDGE ( 'NONE', *, *, #5364, .F. ) ;
#6215=CARTESIAN_POINT ( 'NONE',  ( 1.949486339718610296E-19, -22.37986894186666831, -9.514945144208986960 ) ) ;
#6218=VERTEX_POINT ( 'NONE', #2576 ) ;
#6225=CARTESIAN_POINT ( 'NONE',  ( 2.262072706628479590, 18.56460150496938155, 19.66369668717039332 ) ) ;
#6228=ADVANCED_FACE ( 'NONE', ( #7271 ), #1663, .T. ) ;
#6232=ORIENTED_EDGE ( 'NONE', *, *, #4778, .F. ) ;
#6238=CIRCLE ( 'NONE', #3051, 2.524999999999995914 ) ;
#6239=EDGE_CURVE ( 'NONE', #4813, #10374, #14836, .T. ) ;
#6242=ORIENTED_EDGE ( 'NONE', *, *, #13206, .F. ) ;
#6243=B_SPLINE_CURVE_WITH_KNOTS ( 'NONE', 3,
 ( #14362, #6287, #8426, #14590, #13112, #2601 ),
 .UNSPECIFIED., .F., .F.,
 ( 4, 2, 4 ),
 ( 4.462636882206429356E-07, 0.001879885203074806513, 0.003759324142461392161 ),
 .UNSPECIFIED. ) ;
#6244=DIRECTION ( 'NONE',  ( 0.000000000000000000, 0.000000000000000000, 1.000000000000000000 ) ) ;
#6245=EDGE_CURVE ( 'NONE', #383, #10848, #3726, .T. ) ;
#6248=CARTESIAN_POINT ( 'NONE',  ( 1.039999999999995373, 12.96210679857822434, -24.89775460606817958 ) ) ;
#6252=DIRECTION ( 'NONE',  ( -1.000000000000000000, -0.000000000000000000, -0.000000000000000000 ) ) ;
#6253=CARTESIAN_POINT ( 'NONE',  ( 0.02436607992776064838, 12.59161484032912171, 21.30679549418635688 ) ) ;
#6258=ORIENTED_EDGE ( 'NONE', *, *, #10613, .F. ) ;
#6264=ADVANCED_FACE ( 'NONE', ( #12171 ), #9542, .T. ) ;
#6269=LINE ( 'NONE', #9811, #13473 ) ;
#6270=TOROIDAL_SURFACE ( 'NONE', #13129, 24.12539914357697768, 8.000000000000000000 ) ;
#6271=EDGE_CURVE ( 'NONE', #4588, #567, #7323, .T. ) ;
#6274=ORIENTED_EDGE ( 'NONE', *, *, #3412, .F. ) ;
#6275=EDGE_CURVE ( 'NONE', #11370, #11374, #458, .T. ) ;
#6278=FACE_OUTER_BOUND ( 'NONE', #3384, .T. ) ;
#6280=CARTESIAN_POINT ( 'NONE',  ( 2.765633920072239516, -2.336989772644097574, -24.63872515616085224 ) ) ;
#6283=LINE ( 'NONE', #6209, #7434 ) ;
#6285=ORIENTED_EDGE ( 'NONE', *, *, #12595, .T. ) ;
#6287=CARTESIAN_POINT ( 'NONE',  ( 0.7592463834391192101, -12.05220173035421993, -24.80264696524895385 ) ) ;
#6291=ADVANCED_FACE ( 'NONE', ( #4905 ), #12094, .T. ) ;
#6297=DIRECTION ( 'NONE',  ( -1.000000000000000000, -0.000000000000000000, -0.000000000000000000 ) ) ;
#6299=ORIENTED_EDGE ( 'NONE', *, *, #711, .T. ) ;
#6303=CARTESIAN_POINT ( 'NONE',  ( 0.06555561860988173839, 21.84113606038307509, 12.72236714503170596 ) ) ;
#6305=DIRECTION ( 'NONE',  ( 0.000000000000000000, 0.000000000000000000, 1.000000000000000000 ) ) ;
#6309=CARTESIAN_POINT ( 'NONE',  ( 2.031033479673586939, 19.86422722021340093, -19.12621924769845805 ) ) ;
#6311=CARTESIAN_POINT ( 'NONE',  ( 0.02436607992776064838, 5.391175441198615914, 24.15498966839965078 ) ) ;
#6312=VECTOR ( 'NONE', #4529, 1000.000000000000000 ) ;
#6316=EDGE_LOOP ( 'NONE', ( #7044, #12568, #2325, #10438 ) ) ;
#6317=CARTESIAN_POINT ( 'NONE',  ( 1.394999999999998685, 12.96210679857822434, -24.89775460606818314 ) ) ;
#6318=CARTESIAN_POINT ( 'NONE',  ( 2.789679245949062913, -20.70663861606260525, -12.51925356660783528 ) ) ;
#6320=CIRCLE ( 'NONE', #9273, 24.12539914357697413 ) ;
#6321=VECTOR ( 'NONE', #12861, 1000.000000000000000 ) ;
#6322=VECTOR ( 'NONE', #5379, 1000.000000000000000 ) ;
#6324=FACE_OUTER_BOUND ( 'NONE', #10392, .T. ) ;
#6326=CARTESIAN_POINT ( 'NONE',  ( 0.5321745326902588280, 26.83036154824994668, -3.467596033028380376 ) ) ;
#6330=FACE_OUTER_BOUND ( 'NONE', #13215, .T. ) ;
#6335=DIRECTION ( 'NONE',  ( -1.000000000000000000, -0.000000000000000000, -0.000000000000000000 ) ) ;
#6339=CARTESIAN_POINT ( 'NONE',  ( 2.789999999999999147, -9.324097380959603498, 22.25075486061734864 ) ) ;
#6340=LINE ( 'NONE', #8566, #10758 ) ;
#6343=AXIS2_PLACEMENT_3D ( 'NONE', #3114, #15164, #9235 ) ;
#6349=CARTESIAN_POINT ( 'NONE',  ( 2.789999999999999147, 0.2301004812061083760, -24.44424927289185234 ) ) ;
#6359=CARTESIAN_POINT ( 'NONE',  ( 2.262072661820536013, -3.461047254864073164, -26.82026385750182129 ) ) ;
#6360=CARTESIAN_POINT ( 'NONE',  ( 1.749999999999998002, -4.633866840648726004, -27.68468304288263582 ) ) ;
#6362=CARTESIAN_POINT ( 'NONE',  ( 1.749999999999998002, -20.02152543075360214, 19.67366047555523068 ) ) ;
#6363=CARTESIAN_POINT ( 'NONE',  ( 0.07186811453410632544, -18.89333555428542155, -16.91241718342019951 ) ) ;
#6364=CARTESIAN_POINT ( 'NONE',  ( 2.031033467310408014, 12.98167595241057626, -24.32849926382737138 ) ) ;
#6366=VERTEX_POINT ( 'NONE', #13790 ) ;
#6367=LINE ( 'NONE', #9665, #14698 ) ;
#6368=ADVANCED_FACE ( 'NONE', ( #733 ), #12258, .T. ) ;
#6369=DIRECTION ( 'NONE',  ( -1.000000000000000000, -0.000000000000000000, -0.000000000000000000 ) ) ;
#6373=CARTESIAN_POINT ( 'NONE',  ( 0.000000000000000000, 4.898587196589412829E-16, -4.000000000000000000 ) ) ;
#6375=ORIENTED_EDGE ( 'NONE', *, *, #4779, .T. ) ;
#6378=CARTESIAN_POINT ( 'NONE',  ( 0.8291131470075423504, 24.44424927289185945, 12.96989951879416125 ) ) ;
#6380=CYLINDRICAL_SURFACE ( 'NONE', #4782, 2.524999999999995914 ) ;
#6381=EDGE_CURVE ( 'NONE', #13727, #7471, #9061, .T. ) ;
#6390=B_SPLINE_CURVE_WITH_KNOTS ( 'NONE', 3,
 ( #8977, #10208, #4455, #7752 ),
 .UNSPECIFIED., .F., .F.,
 ( 4, 4 ),
 ( 2.324263106244697256E-07, 0.0006888201370294697295 ),
 .UNSPECIFIED. ) ;
#6397=CARTESIAN_POINT ( 'NONE',  ( 2.789999999999999147, 5.535312321043049266, -23.48180575137724446 ) ) ;
#6398=VERTEX_POINT ( 'NONE', #12492 ) ;
#6402=CARTESIAN_POINT ( 'NONE',  ( 0.07181525068722525995, 25.22524549359950541, -2.576941577947494011 ) ) ;
#6407=ORIENTED_EDGE ( 'NONE', *, *, #7370, .F. ) ;
#6412=CARTESIAN_POINT ( 'NONE',  ( 0.000000000000000000, 0.000000000000000000, 0.000000000000000000 ) ) ;
#6418=FACE_OUTER_BOUND ( 'NONE', #3065, .T. ) ;
#6420=CARTESIAN_POINT ( 'NONE',  ( 0.02436607992776455150, 21.30679549418631780, 12.59161484032919986 ) ) ;
#6422=ORIENTED_EDGE ( 'NONE', *, *, #11479, .T. ) ;
#6423=ORIENTED_EDGE ( 'NONE', *, *, #6271, .T. ) ;
#6425=ORIENTED_EDGE ( 'NONE', *, *, #13988, .T. ) ;
#6426=CARTESIAN_POINT ( 'NONE',  ( 2.718131864678288601, 2.577209017047007666, 25.22589920183362722 ) ) ;
#6427=FACE_OUTER_BOUND ( 'NONE', #9120, .T. ) ;
#6428=ADVANCED_FACE ( 'NONE', ( #14730 ), #875, .T. ) ;
#6429=FACE_OUTER_BOUND ( 'NONE', #11783, .T. ) ;
#6435=CARTESIAN_POINT ( 'NONE',  ( 2.783025336474041822, 12.53640742967753141, 21.08118142846907972 ) ) ;
#6442=B_SPLINE_CURVE_WITH_KNOTS ( 'NONE', 3,
 ( #3427, #8256, #12937, #8115 ),
 .UNSPECIFIED., .F., .F.,
 ( 4, 4 ),
 ( 2.034713381942717888E-07, 0.0006045424356927869836 ),
 .UNSPECIFIED. ) ;
#6443=ORIENTED_EDGE ( 'NONE', *, *, #13563, .F. ) ;
#6453=CARTESIAN_POINT ( 'NONE',  ( 0.000000000000000000, 5.535312321043032391, -23.48180575137725867 ) ) ;
#6461=EDGE_CURVE ( 'NONE', #6579, #4703, #8388, .T. ) ;
#6463=ORIENTED_EDGE ( 'NONE', *, *, #8243, .T. ) ;
#6465=CYLINDRICAL_SURFACE ( 'NONE', #5555, 13.19999999999999929 ) ;
#6466=EDGE_CURVE ( 'NONE', #4703, #9629, #8279, .T. ) ;
#6470=CARTESIAN_POINT ( 'NONE',  ( 0.07181524296601550506, -18.89296398180203695, 16.91181672897726784 ) ) ;
#6477=CARTESIAN_POINT ( 'NONE',  ( 2.789999999999999147, -20.70663861606260170, -12.51925356660783528 ) ) ;
#6478=VECTOR ( 'NONE', #13069, 1000.000000000000000 ) ;
#6481=CARTESIAN_POINT ( 'NONE',  ( 2.789999999999999147, 23.31896751603331808, 7.334849878007589474 ) ) ;
#6489=AXIS2_PLACEMENT_3D ( 'NONE', #11435, #912, #9300 ) ;
#6490=EDGE_CURVE ( 'NONE', #2553, #13780, #5660, .T. ) ;
#6494=B_SPLINE_CURVE_WITH_KNOTS ( 'NONE', 3,
 ( #13292, #13225, #2772, #7465, #13529, #13368 ),
 .UNSPECIFIED., .F., .F.,
 ( 4, 2, 4 ),
 ( 2.586195665736120714E-07, 0.001878649493629692274, 0.003757040367692811213 ),
 .UNSPECIFIED. ) ;
#6496=CARTESIAN_POINT ( 'NONE',  ( 1.749999999999998002, 12.52377138324259143, -25.12109765559640451 ) ) ;
#6497=CARTESIAN_POINT ( 'NONE',  ( 2.789999999999999147, -8.936381166381891568E-14, 25.59481291497571220 ) ) ;
#6499=DIRECTION ( 'NONE',  ( -1.000000000000000000, -0.000000000000000000, -0.000000000000000000 ) ) ;
#6508=CYLINDRICAL_SURFACE ( 'NONE', #1403, 13.19999999999999929 ) ;
#6519=AXIS2_PLACEMENT_3D ( 'NONE', #8869, #13565, #10183 ) ;
#6520=CARTESIAN_POINT ( 'NONE',  ( 0.000000000000000000, 0.000000000000000000, 0.000000000000000000 ) ) ;
#6521=EDGE_CURVE ( 'NONE', #11429, #10552, #5727, .T. ) ;
#6526=VERTEX_POINT ( 'NONE', #13945 ) ;
#6528=VECTOR ( 'NONE', #1715, 1000.000000000000000 ) ;
#6531=CARTESIAN_POINT ( 'NONE',  ( 1.039999999999997593, 0.000000000000000000, 0.000000000000000000 ) ) ;
#6545=DIRECTION ( 'NONE',  ( 0.000000000000000000, 0.000000000000000000, 1.000000000000000000 ) ) ;
#6547=CIRCLE ( 'NONE', #3600, 24.12539914357697413 ) ;
#6553=CIRCLE ( 'NONE', #15155, 2.524999999999996358 ) ;
#6554=FACE_OUTER_BOUND ( 'NONE', #5613, .T. ) ;
#6557=FACE_OUTER_BOUND ( 'NONE', #11286, .T. ) ;
#6560=CARTESIAN_POINT ( 'NONE',  ( 0.1855654851361731306, -10.67816411292181655, 23.63475234378979195 ) ) ;
#6561=CIRCLE ( 'NONE', #13173, 24.12539914357697768 ) ;
#6571=FACE_OUTER_BOUND ( 'NONE', #7119, .T. ) ;
#6579=VERTEX_POINT ( 'NONE', #11622 ) ;
#6585=CARTESIAN_POINT ( 'NONE',  ( 0.02436607992775978102, 16.37294372382885044, -18.55949924794875017 ) ) ;
#6586=CARTESIAN_POINT ( 'NONE',  ( 1.749999999999998002, -27.76164181293049182, -4.147968289691579713 ) ) ;
#6587=EDGE_LOOP ( 'NONE', ( #13188, #13570, #10897, #14956 ) ) ;
#6588=EDGE_CURVE ( 'NONE', #2490, #1743, #12800, .T. ) ;
#6589=ORIENTED_EDGE ( 'NONE', *, *, #11158, .F. ) ;
#6595=DIRECTION ( 'NONE',  ( 0.000000000000000000, 1.374038396813314756E-15, -1.000000000000000000 ) ) ;
#6603=CARTESIAN_POINT ( 'NONE',  ( 0.006974771092478172958, -9.686319561460797090, -22.53337530003413747 ) ) ;
#6614=DIRECTION ( 'NONE',  ( -1.000000000000000000, 0.000000000000000000, 0.000000000000000000 ) ) ;
#6615=CARTESIAN_POINT ( 'NONE',  ( 2.604434261026088215, -5.253342437939904741, 25.39738473784999684 ) ) ;
#6618=B_SPLINE_CURVE_WITH_KNOTS ( 'NONE', 3,
 ( #12663, #12591, #990, #3231 ),
 .UNSPECIFIED., .F., .F.,
 ( 4, 4 ),
 ( 0.005258214619651984008, 0.005948481662034168192 ),
 .UNSPECIFIED. ) ;
#6627=ORIENTED_EDGE ( 'NONE', *, *, #8327, .T. ) ;
#6629=ORIENTED_EDGE ( 'NONE', *, *, #10695, .T. ) ;
#6633=CARTESIAN_POINT ( 'NONE',  ( 0.7592463896980057303, -19.86438386685674473, 19.12676442129336252 ) ) ;
#6639=DIRECTION ( 'NONE',  ( 0.000000000000000000, -0.8090169943749444537, -0.5877852522924771339 ) ) ;
#6648=CARTESIAN_POINT ( 'NONE',  ( 1.960886852992497653, -24.44424927289185590, 12.96989951879399072 ) ) ;
#6649=EDGE_CURVE ( 'NONE', #1940, #14933, #14087, .T. ) ;
#6651=CYLINDRICAL_SURFACE ( 'NONE', #7743, 28.06981291497571362 ) ;
#6654=VERTEX_POINT ( 'NONE', #1487 ) ;
#6656=CYLINDRICAL_SURFACE ( 'NONE', #3490, 4.000000000000000000 ) ;
#6660=ORIENTED_EDGE ( 'NONE', *, *, #7614, .F. ) ;
#6661=EDGE_CURVE ( 'NONE', #10903, #6696, #13723, .T. ) ;
#6662=ORIENTED_EDGE ( 'NONE', *, *, #9473, .T. ) ;
#6663=CARTESIAN_POINT ( 'NONE',  ( 2.789999999999999147, 0.000000000000000000, 0.000000000000000000 ) ) ;
#6664=CARTESIAN_POINT ( 'NONE',  ( 1.749999999999998002, 12.52377138324224148, 25.12109765559658570 ) ) ;
#6667=CARTESIAN_POINT ( 'NONE',  ( 1.039999999999996039, 24.89775460606832169, 12.96210679857795256 ) ) ;
#6674=FACE_OUTER_BOUND ( 'NONE', #1135, .T. ) ;
#6678=CARTESIAN_POINT ( 'NONE',  ( 2.789999999999999147, 12.52067188844381107, -20.62201879784899461 ) ) ;
#6681=CYLINDRICAL_SURFACE ( 'NONE', #11702, 13.19999999999999929 ) ;
#6684=CARTESIAN_POINT ( 'NONE',  ( 2.718131847775119514, -5.344160105508880321, 24.78765742476137035 ) ) ;
#6691=CARTESIAN_POINT ( 'NONE',  ( 0.006974674093433516284, 24.42374957165205629, -2.249040938978583259 ) ) ;
#6692=B_SPLINE_CURVE_WITH_KNOTS ( 'NONE', 3,
 ( #1501, #13542, #13015, #14189 ),
 .UNSPECIFIED., .F., .F.,
 ( 4, 4 ),
 ( 0.005258139959819257275, 0.005342776758202955750 ),
 .UNSPECIFIED. ) ;
#6696=VERTEX_POINT ( 'NONE', #9626 ) ;
#6703=CARTESIAN_POINT ( 'NONE',  ( 0.1855654851361731306, 23.63475234378982748, 10.67816411292173306 ) ) ;
#6704=DIRECTION ( 'NONE',  ( -1.000000000000000000, -0.000000000000000000, -0.000000000000000000 ) ) ;
#6706=EDGE_CURVE ( 'NONE', #2360, #11849, #3635, .T. ) ;
#6707=B_SPLINE_CURVE_WITH_KNOTS ( 'NONE', 3,
 ( #2758, #14451, #4149, #13515 ),
 .UNSPECIFIED., .F., .F.,
 ( 4, 4 ),
 ( 0.005258120783916788929, 0.005948386350302939385 ),
 .UNSPECIFIED. ) ;
#6711=DIRECTION ( 'NONE',  ( -1.000000000000000000, 0.000000000000000000, -0.000000000000000000 ) ) ;
#6713=VERTEX_POINT ( 'NONE', #8389 ) ;
#6723=CARTESIAN_POINT ( 'NONE',  ( 2.789999999999999147, -15.04425356660744839, -20.70663861606288236 ) ) ;
#6728=ORIENTED_EDGE ( 'NONE', *, *, #146, .F. ) ;
#6730=AXIS2_PLACEMENT_3D ( 'NONE', #12218, #524, #2995 ) ;
#6731=CYLINDRICAL_SURFACE ( 'NONE', #7579, 13.19999999999999929 ) ;
#6737=CARTESIAN_POINT ( 'NONE',  ( 2.789999999999999147, -1.991882183130126549, -24.04302995059967429 ) ) ;
#6738=B_SPLINE_CURVE_WITH_KNOTS ( 'NONE', 3,
 ( #7382, #512, #1609, #14678, #3987, #14453 ),
 .UNSPECIFIED., .F., .F.,
 ( 4, 2, 4 ),
 ( 0.0004963285629697519611, 0.002127826186449857486, 0.003759323809929962686 ),
 .UNSPECIFIED. ) ;
#6740=ADVANCED_FACE ( 'NONE', ( #7867 ), #10016, .T. ) ;
#6745=DIRECTION ( 'NONE',  ( -1.000000000000000000, -0.000000000000000000, 0.000000000000000000 ) ) ;
#6746=ADVANCED_FACE ( 'NONE', ( #6557 ), #13939, .T. ) ;
#6753=ORIENTED_EDGE ( 'NONE', *, *, #9193, .F. ) ;
#6754=DIRECTION ( 'NONE',  ( -1.000000000000000000, -0.000000000000000000, -0.000000000000000000 ) ) ;
#6755=DIRECTION ( 'NONE',  ( -1.000000000000000000, -0.000000000000000000, -0.000000000000000000 ) ) ;
#6756=ORIENTED_EDGE ( 'NONE', *, *, #7871, .T. ) ;
#6762=CARTESIAN_POINT ( 'NONE',  ( 0.07181523211953064201, -23.19431517146941246, 10.24584646439529756 ) ) ;
#6769=EDGE_CURVE ( 'NONE', #15033, #3207, #11869, .T. ) ;
#6773=EDGE_LOOP ( 'NONE', ( #1762, #6589, #11999, #9585, #14175, #6942 ) ) ;
#6774=ORIENTED_EDGE ( 'NONE', *, *, #313, .F. ) ;
#6782=DIRECTION ( 'NONE',  ( 0.000000000000000000, 6.870191984066572599E-15, -1.000000000000000000 ) ) ;
#6785=ORIENTED_EDGE ( 'NONE', *, *, #13114, .F. ) ;
#6791=( GEOMETRIC_REPRESENTATION_CONTEXT ( 3 ) GLOBAL_UNCERTAINTY_ASSIGNED_CONTEXT ( ( #14552 ) ) GLOBAL_UNIT_ASSIGNED_CONTEXT ( ( #10078, #4546, #10307 ) ) REPRESENTATION_CONTEXT ( 'NONE', 'WORKASPACE' ) );
#6799=CARTESIAN_POINT ( 'NONE',  ( 0.07186811453410689443, 18.89333555428554590, 16.91241718342006450 ) ) ;
#6800=FACE_OUTER_BOUND ( 'NONE', #10357, .T. ) ;
#6803=AXIS2_PLACEMENT_3D ( 'NONE', #1065, #7984, #12662 ) ;
#6804=CARTESIAN_POINT ( 'NONE',  ( 2.765633920072235963, -24.63872515616080960, -2.336989772644527008 ) ) ;
#6816=AXIS2_PLACEMENT_3D ( 'NONE', #1869, #6704, #11384 ) ;
#6817=CYLINDRICAL_SURFACE ( 'NONE', #11766, 28.06981291497571362 ) ;
#6819=CARTESIAN_POINT ( 'NONE',  ( 1.749999999999998002, 12.96210679857822257, -24.89775460606818669 ) ) ;
#6822=ORIENTED_EDGE ( 'NONE', *, *, #13303, .F. ) ;
#6824=LINE ( 'NONE', #3288, #5572 ) ;
#6826=B_SPLINE_CURVE_WITH_KNOTS ( 'NONE', 3,
 ( #6205, #350, #5067, #2973 ),
 .UNSPECIFIED., .F., .F.,
 ( 4, 4 ),
 ( 0.005258120783916793266, 0.005948386350302923772 ),
 .UNSPECIFIED. ) ;
#6831=DIRECTION ( 'NONE',  ( 0.000000000000000000, 0.000000000000000000, 1.000000000000000000 ) ) ;
#6835=DIRECTION ( 'NONE',  ( 0.000000000000000000, 0.000000000000000000, 1.000000000000000000 ) ) ;
#6839=EDGE_CURVE ( 'NONE', #1110, #6106, #4023, .T. ) ;
#6842=EDGE_LOOP ( 'NONE', ( #1005, #10153, #3267, #10389, #10841, #3113 ) ) ;
#6844=AXIS2_PLACEMENT_3D ( 'NONE', #15075, #9317, #5560 ) ;
#6846=CYLINDRICAL_SURFACE ( 'NONE', #1832, 28.06981291497571362 ) ;
#6847=ORIENTED_EDGE ( 'NONE', *, *, #11904, .T. ) ;
#6850=ORIENTED_EDGE ( 'NONE', *, *, #5433, .T. ) ;
#6853=DIRECTION ( 'NONE',  ( -1.000000000000000000, -0.000000000000000000, -0.000000000000000000 ) ) ;
#6859=ADVANCED_FACE ( 'NONE', ( #14556 ), #15184, .T. ) ;
#6861=ORIENTED_EDGE ( 'NONE', *, *, #6588, .T. ) ;
#6862=FACE_OUTER_BOUND ( 'NONE', #9528, .T. ) ;
#6863=DIRECTION ( 'NONE',  ( 0.000000000000000000, 1.374038396813314756E-15, -1.000000000000000000 ) ) ;
#6867=VERTEX_POINT ( 'NONE', #13040 ) ;
#6877=CARTESIAN_POINT ( 'NONE',  ( 0.009068833172775131110, 21.10834851580723992, -12.54305517365597922 ) ) ;
#6879=VERTEX_POINT ( 'NONE', #14288 ) ;
#6880=B_SPLINE_CURVE_WITH_KNOTS ( 'NONE', 3,
 ( #8119, #10643, #12645, #2434, #3498, #15122 ),
 .UNSPECIFIED., .F., .F.,
 ( 4, 2, 4 ),
 ( 2.321268216997094965E-07, 0.001878622960950495756, 0.003757013795079291486 ),
 .UNSPECIFIED. ) ;
#6887=DIRECTION ( 'NONE',  ( 0.000000000000000000, 0.5877852522924805756, -0.8090169943749421222 ) ) ;
#6888=CARTESIAN_POINT ( 'NONE',  ( 0.000000000000000000, -9.324097380959594616, 22.25075486061734509 ) ) ;
#6890=DIRECTION ( 'NONE',  ( 0.000000000000000000, 0.000000000000000000, 1.000000000000000000 ) ) ;
#6898=ORIENTED_EDGE ( 'NONE', *, *, #9712, .F. ) ;
#6899=EDGE_CURVE ( 'NONE', #9813, #5482, #11815, .T. ) ;
#6900=DIRECTION ( 'NONE',  ( 0.000000000000000000, 1.776356839400252831E-15, -1.000000000000000000 ) ) ;
#6901=CARTESIAN_POINT ( 'NONE',  ( 2.765633920072235519, 18.55949924794892780, 16.37294372382865504 ) ) ;
#6924=ORIENTED_EDGE ( 'NONE', *, *, #13746, .F. ) ;
#6932=CARTESIAN_POINT ( 'NONE',  ( 2.790000000000000480, 9.514945144208736494, 22.37986894186676423 ) ) ;
#6934=VECTOR ( 'NONE', #13475, 1000.000000000000000 ) ;
#6942=ORIENTED_EDGE ( 'NONE', *, *, #15112, .F. ) ;
#6946=VERTEX_POINT ( 'NONE', #12691 ) ;
#6947=CARTESIAN_POINT ( 'NONE',  ( 1.039999999999996705, 19.67366047555530173, 20.02152543075352398 ) ) ;
#6949=CARTESIAN_POINT ( 'NONE',  ( 2.789999999999999147, 18.28042085475278355, 15.74360496233388140 ) ) ;
#6953=CARTESIAN_POINT ( 'NONE',  ( 2.765633920072235519, -18.55949924794880346, -16.37294372382878649 ) ) ;
#6956=CARTESIAN_POINT ( 'NONE',  ( 1.749999999999998002, 24.89775460606851354, -12.96210679857759729 ) ) ;
#6957=DIRECTION ( 'NONE',  ( -1.000000000000000000, -0.000000000000000000, 0.000000000000000000 ) ) ;
#6958=EDGE_CURVE ( 'NONE', #368, #1565, #10009, .T. ) ;
#6959=B_SPLINE_CURVE_WITH_KNOTS ( 'NONE', 3,
 ( #8343, #4600, #8051, #13019 ),
 .UNSPECIFIED., .F., .F.,
 ( 4, 4 ),
 ( 0.005258105385878691744, 0.005948373736081389272 ),
 .UNSPECIFIED. ) ;
#6961=CARTESIAN_POINT ( 'NONE',  ( 0.000000000000000000, -20.62201879784923264, 12.52067188844344336 ) ) ;
#6963=CARTESIAN_POINT ( 'NONE',  ( 2.765633920072239071, -12.59161484032927092, 21.30679549418627161 ) ) ;
#6965=CARTESIAN_POINT ( 'NONE',  ( 2.789999999999999147, -20.62201879784921843, 12.52067188844344336 ) ) ;
#6969=VERTEX_POINT ( 'NONE', #9437 ) ;
#6970=EDGE_CURVE ( 'NONE', #11124, #5767, #3391, .T. ) ;
#6973=CIRCLE ( 'NONE', #7710, 2.524999999999994582 ) ;
#6976=DIRECTION ( 'NONE',  ( -1.000000000000000000, -0.000000000000000000, 0.000000000000000000 ) ) ;
#6977=DIRECTION ( 'NONE',  ( 0.000000000000000000, 0.000000000000000000, 1.000000000000000000 ) ) ;
#6980=DIRECTION ( 'NONE',  ( -1.000000000000000000, 0.000000000000000000, 0.000000000000000000 ) ) ;
#6983=CARTESIAN_POINT ( 'NONE',  ( 2.765633920072237295, 12.59161484032912171, 21.30679549418635688 ) ) ;
#6985=EDGE_CURVE ( 'NONE', #10552, #7184, #10412, .T. ) ;
#6996=DIRECTION ( 'NONE',  ( -1.000000000000000000, -0.000000000000000000, -0.000000000000000000 ) ) ;
#7001=FACE_OUTER_BOUND ( 'NONE', #3310, .T. ) ;
#7006=AXIS2_PLACEMENT_3D ( 'NONE', #5703, #6853, #4475 ) ;
#7008=VERTEX_POINT ( 'NONE', #4414 ) ;
#7009=LINE ( 'NONE', #4421, #10476 ) ;
#7014=DIRECTION ( 'NONE',  ( 0.000000000000000000, 0.000000000000000000, 1.000000000000000000 ) ) ;
#7017=ORIENTED_EDGE ( 'NONE', *, *, #6649, .F. ) ;
#7022=FACE_OUTER_BOUND ( 'NONE', #10230, .T. ) ;
#7027=MECHANICAL_DESIGN_GEOMETRIC_PRESENTATION_REPRESENTATION('',(#11447),#6791);
#7028=VERTEX_POINT ( 'NONE', #7527 ) ;
#7029=ORIENTED_EDGE ( 'NONE', *, *, #4466, .T. ) ;
#7031=CARTESIAN_POINT ( 'NONE',  ( 2.765633920072235963, 21.30679549418649543, -12.59161484032888723 ) ) ;
#7036=DIRECTION ( 'NONE',  ( -1.000000000000000000, -0.000000000000000000, -0.000000000000000000 ) ) ;
#7044=ORIENTED_EDGE ( 'NONE', *, *, #8116, .F. ) ;
#7046=FACE_OUTER_BOUND ( 'NONE', #13818, .T. ) ;
#7048=CYLINDRICAL_SURFACE ( 'NONE', #3848, 28.06981291497571362 ) ;
#7062=CARTESIAN_POINT ( 'NONE',  ( 2.765633920072234631, 5.391175441198615914, 24.15498966839965078 ) ) ;
#7065=EDGE_LOOP ( 'NONE', ( #11486, #1029, #11322, #2010 ) ) ;
#7066=CARTESIAN_POINT ( 'NONE',  ( 2.789999999999999147, -22.25075486061744812, 9.324097380959361914 ) ) ;
#7067=AXIS2_PLACEMENT_3D ( 'NONE', #10545, #11979, #10688 ) ;
#7071=AXIS2_PLACEMENT_3D ( 'NONE', #13388, #2866, #7562 ) ;
#7073=EDGE_LOOP ( 'NONE', ( #14548, #607, #13745, #4950 ) ) ;
#7074=ORIENTED_EDGE ( 'NONE', *, *, #11618, .T. ) ;
#7075=B_SPLINE_CURVE_WITH_KNOTS ( 'NONE', 3,
 ( #14934, #11377, #5559, #2168, #14851, #13771 ),
 .UNSPECIFIED., .F., .F.,
 ( 4, 2, 4 ),
 ( 4.462636731831954487E-07, 0.001879885066974966781, 0.003759323870276750149 ),
 .UNSPECIFIED. ) ;
#7078=AXIS2_PLACEMENT_3D ( 'NONE', #13446, #14465, #1765 ) ;
#7089=AXIS2_PLACEMENT_3D ( 'NONE', #7964, #96, #6890 ) ;
#7091=CYLINDRICAL_SURFACE ( 'NONE', #10190, 13.19999999999999929 ) ;
#7092=B_SPLINE_CURVE_WITH_KNOTS ( 'NONE', 3,
 ( #9098, #3188, #7870, #633, #4185, #8855 ),
 .UNSPECIFIED., .F., .F.,
 ( 4, 2, 4 ),
 ( 4.462636732176736601E-07, 0.001879885066974997356, 0.003759323870276777037 ),
 .UNSPECIFIED. ) ;
#7096=CARTESIAN_POINT ( 'NONE',  ( 2.783025228907520798, -22.53337530003396338, -9.686319561461189664 ) ) ;
#7098=DIRECTION ( 'NONE',  ( -1.000000000000000000, -0.000000000000000000, 0.000000000000000000 ) ) ;
#7099=EDGE_CURVE ( 'NONE', #1547, #12081, #9681, .T. ) ;
#7100=DIRECTION ( 'NONE',  ( 1.000000000000000000, -0.000000000000000000, 0.000000000000000000 ) ) ;
#7101=B_SPLINE_CURVE_WITH_KNOTS ( 'NONE', 3,
 ( #2205, #4212, #8882, #4361 ),
 .UNSPECIFIED., .F., .F.,
 ( 4, 4 ),
 ( 2.034713381942769504E-07, 0.0006887909409525124101 ),
 .UNSPECIFIED. ) ;
#7103=CARTESIAN_POINT ( 'NONE',  ( 0.5321745087963408727, 11.58891744060107065, 24.44564404695848836 ) ) ;
#7106=FACE_OUTER_BOUND ( 'NONE', #8073, .T. ) ;
#7111=ORIENTED_EDGE ( 'NONE', *, *, #11225, .F. ) ;
#7115=DIRECTION ( 'NONE',  ( -1.000000000000000000, -0.000000000000000000, -0.000000000000000000 ) ) ;
#7117=DIRECTION ( 'NONE',  ( 0.000000000000000000, -0.9510565162951544194, 0.3090169943749446757 ) ) ;
#7119=EDGE_LOOP ( 'NONE', ( #12491, #14376, #12585, #4544, #13382, #1740 ) ) ;
#7120=CARTESIAN_POINT ( 'NONE',  ( 0.000000000000000000, 0.000000000000000000, 0.000000000000000000 ) ) ;
#7122=CARTESIAN_POINT ( 'NONE',  ( 1.039999999999997149, -27.68468304288261805, 4.633866840648821039 ) ) ;
#7127=VERTEX_POINT ( 'NONE', #2829 ) ;
#7132=DIRECTION ( 'NONE',  ( 0.000000000000000000, 0.000000000000000000, 1.000000000000000000 ) ) ;
#7138=EDGE_CURVE ( 'NONE', #14234, #12512, #6367, .T. ) ;
#7139=ORIENTED_EDGE ( 'NONE', *, *, #5405, .T. ) ;
#7141=CARTESIAN_POINT ( 'NONE',  ( 0.000000000000000000, 22.25075486061751207, -9.324097380959241121 ) ) ;
#7149=VERTEX_POINT ( 'NONE', #11118 ) ;
#7155=LINE ( 'NONE', #9534, #9434 ) ;
#7164=DIRECTION ( 'NONE',  ( 0.000000000000000000, 0.000000000000000000, 1.000000000000000000 ) ) ;
#7170=AXIS2_PLACEMENT_3D ( 'NONE', #2507, #9352, #4680 ) ;
#7176=B_SPLINE_CURVE_WITH_KNOTS ( 'NONE', 3,
 ( #13959, #4898, #10574, #8401 ),
 .UNSPECIFIED., .F., .F.,
 ( 4, 4 ),
 ( 1.981826382900849143E-07, 0.0006887856082032019125 ),
 .UNSPECIFIED. ) ;
#7182=AXIS2_PLACEMENT_3D ( 'NONE', #2226, #4758, #10528 ) ;
#7184=VERTEX_POINT ( 'NONE', #1910 ) ;
#7185=CARTESIAN_POINT ( 'NONE',  ( 0.02436607992776411782, -16.37294372382844543, -18.55949924794910544 ) ) ;
#7187=CARTESIAN_POINT ( 'NONE',  ( 2.789999999999999147, 9.324097380959765147, -22.25075486061728824 ) ) ;
#7189=DIRECTION ( 'NONE',  ( -1.000000000000000000, 0.000000000000000000, 0.000000000000000000 ) ) ;
#7190=DIRECTION ( 'NONE',  ( -1.000000000000000000, -0.000000000000000000, -0.000000000000000000 ) ) ;
#7194=CARTESIAN_POINT ( 'NONE',  ( 0.7592463965288823724, -12.98165646470099155, 24.32906614999610895 ) ) ;
#7195=CARTESIAN_POINT ( 'NONE',  ( 0.07181524296601451973, 16.91181672897733534, 18.89296398180198011 ) ) ;
#7198=ORIENTED_EDGE ( 'NONE', *, *, #6649, .T. ) ;
#7204=CARTESIAN_POINT ( 'NONE',  ( 2.765633920072235963, -16.37294372382871188, 18.55949924794887096 ) ) ;
#7208=DIRECTION ( 'NONE',  ( -1.000000000000000000, 0.000000000000000000, 0.000000000000000000 ) ) ;
#7209=CARTESIAN_POINT ( 'NONE',  ( 8.000000000000000000, 0.000000000000000000, 0.000000000000000000 ) ) ;
#7220=AXIS2_PLACEMENT_3D ( 'NONE', #2686, #583, #9594 ) ;
#7223=ORIENTED_EDGE ( 'NONE', *, *, #5242, .F. ) ;
#7225=CARTESIAN_POINT ( 'NONE',  ( 2.765633920072233742, -24.15498966839966855, 5.391175441198523544 ) ) ;
#7227=CARTESIAN_POINT ( 'NONE',  ( 2.765633920072241292, 18.55949924794916228, -16.37294372382838148 ) ) ;
#7233=EDGE_CURVE ( 'NONE', #3010, #852, #4370, .T. ) ;
#7234=VERTEX_POINT ( 'NONE', #9056 ) ;
#7236=AXIS2_PLACEMENT_3D ( 'NONE', #2431, #11716, #5896 ) ;
#7237=CIRCLE ( 'NONE', #4552, 24.12539914357697768 ) ;
#7241=VERTEX_POINT ( 'NONE', #5386 ) ;
#7243=CARTESIAN_POINT ( 'NONE',  ( 2.789999999999999147, 7.334849878007844382, -23.31896751603323992 ) ) ;
#7244=ORIENTED_EDGE ( 'NONE', *, *, #13068, .T. ) ;
#7249=AXIS2_PLACEMENT_3D ( 'NONE', #13380, #3942, #384 ) ;
#7259=B_SPLINE_CURVE_WITH_KNOTS ( 'NONE', 3,
 ( #5523, #2050, #10122, #9053, #9973, #4446 ),
 .UNSPECIFIED., .F., .F.,
 ( 4, 2, 4 ),
 ( 2.032124546189838441E-07, 0.001878594002992310316, 0.003756984793530001362 ),
 .UNSPECIFIED. ) ;
#7260=CARTESIAN_POINT ( 'NONE',  ( 1.039999999999996705, 27.76164181293051669, -4.147968289691385202 ) ) ;
#7261=TOROIDAL_SURFACE ( 'NONE', #15125, 24.12539914357697413, 8.000000000000000000 ) ;
#7265=CARTESIAN_POINT ( 'NONE',  ( 1.394999999999999574, 12.52377138324259676, -25.12109765559640451 ) ) ;
#7266=CYLINDRICAL_SURFACE ( 'NONE', #8774, 28.06981291497571362 ) ;
#7267=CARTESIAN_POINT ( 'NONE',  ( 1.039999999999996927, 4.633866840649313090, -27.68468304288253634 ) ) ;
#7270=EDGE_CURVE ( 'NONE', #3390, #2825, #8076, .T. ) ;
#7271=FACE_OUTER_BOUND ( 'NONE', #906, .T. ) ;
#7273=CARTESIAN_POINT ( 'NONE',  ( 2.790000000000000924, 0.000000000000000000, 4.000000000000000000 ) ) ;
#7277=ORIENTED_EDGE ( 'NONE', *, *, #11338, .T. ) ;
#7278=VERTEX_POINT ( 'NONE', #6819 ) ;
#7281=CYLINDRICAL_SURFACE ( 'NONE', #2393, 13.20000000000000284 ) ;
#7284=DIRECTION ( 'NONE',  ( 0.000000000000000000, 0.000000000000000000, 1.000000000000000000 ) ) ;
#7285=AXIS2_PLACEMENT_3D ( 'NONE', #9797, #13074, #10793 ) ;
#7293=ORIENTED_EDGE ( 'NONE', *, *, #8775, .F. ) ;
#7296=DIRECTION ( 'NONE',  ( -1.000000000000000000, -0.000000000000000000, -0.000000000000000000 ) ) ;
#7301=CIRCLE ( 'NONE', #9264, 28.06981291497571362 ) ;
#7304=ORIENTED_EDGE ( 'NONE', *, *, #9473, .F. ) ;
#7306=ORIENTED_EDGE ( 'NONE', *, *, #5247, .F. ) ;
#7310=ADVANCED_FACE ( 'NONE', ( #10511 ), #9351, .T. ) ;
#7311=ADVANCED_FACE ( 'NONE', ( #2437, #2211 ), #1130, .F. ) ;
#7323=B_SPLINE_CURVE_WITH_KNOTS ( 'NONE', 3,
 ( #2737, #9576, #10728, #10803 ),
 .UNSPECIFIED., .F., .F.,
 ( 4, 4 ),
 ( 2.034713381942770033E-07, 0.0006045424356928436873 ),
 .UNSPECIFIED. ) ;
#7324=TOROIDAL_SURFACE ( 'NONE', #7067, 24.12539914357697413, 8.000000000000000000 ) ;
#7326=VERTEX_POINT ( 'NONE', #6965 ) ;
#7327=CARTESIAN_POINT ( 'NONE',  ( -10.00000000000000000, 0.000000000000000000, 0.000000000000000000 ) ) ;
#7330=VERTEX_POINT ( 'NONE', #12867 ) ;
#7332=CIRCLE ( 'NONE', #1431, 2.524999999999995914 ) ;
#7333=B_SPLINE_CURVE_WITH_KNOTS ( 'NONE', 3,
 ( #8400, #6114, #8706, #13400 ),
 .UNSPECIFIED., .F., .F.,
 ( 4, 4 ),
 ( 2.135345996175579449E-07, 0.0006888010880210803950 ),
 .UNSPECIFIED. ) ;
#7336=VERTEX_POINT ( 'NONE', #9413 ) ;
#7339=CARTESIAN_POINT ( 'NONE',  ( 0.02436607992776541887, 12.59161484032942901, -21.30679549418617924 ) ) ;
#7340=CARTESIAN_POINT ( 'NONE',  ( 2.031033465052725084, -27.14933624560904946, -4.828387785248313691 ) ) ;
#7341=VECTOR ( 'NONE', #14143, 1000.000000000000000 ) ;
#7343=AXIS2_PLACEMENT_3D ( 'NONE', #12794, #3659, #2506 ) ;
#7344=CARTESIAN_POINT ( 'NONE',  ( 2.030753605846574494, 3.797885586973597682, -27.31305418910206129 ) ) ;
#7348=B_SPLINE_CURVE_WITH_KNOTS ( 'NONE', 3,
 ( #8658, #7447, #13274, #11964 ),
 .UNSPECIFIED., .F., .F.,
 ( 4, 4 ),
 ( 2.324263106244698315E-07, 0.0006888201370294677779 ),
 .UNSPECIFIED. ) ;
#7349=ORIENTED_EDGE ( 'NONE', *, *, #612, .T. ) ;
#7350=EDGE_LOOP ( 'NONE', ( #13693, #12874, #8130, #11051 ) ) ;
#7351=CARTESIAN_POINT ( 'NONE',  ( 2.789679245949062913, -20.70663861606260525, -12.51925356660783528 ) ) ;
#7352=CARTESIAN_POINT ( 'NONE',  ( 2.789999999999999147, 24.34211360614300190, 7.909232158574900140 ) ) ;
#7353=CARTESIAN_POINT ( 'NONE',  ( 0.000000000000000000, 0.000000000000000000, 0.000000000000000000 ) ) ;
#7354=CARTESIAN_POINT ( 'NONE',  ( 2.262072625383131363, 26.57710921259761960, 4.996265754456460151 ) ) ;
#7364=ORIENTED_EDGE ( 'NONE', *, *, #12758, .T. ) ;
#7365=CIRCLE ( 'NONE', #730, 24.12539914357697768 ) ;
#7369=CARTESIAN_POINT ( 'NONE',  ( 2.789999999999999147, 5.391175441198615914, 24.15498966839965078 ) ) ;
#7370=EDGE_CURVE ( 'NONE', #8417, #5700, #14109, .T. ) ;
#7371=CARTESIAN_POINT ( 'NONE',  ( 2.765633920072236851, -22.71065055754445439, -9.836394144775947979 ) ) ;
#7381=CARTESIAN_POINT ( 'NONE',  ( 2.030753602223784871, 27.14986936243581184, -4.828194074574073902 ) ) ;
#7382=CARTESIAN_POINT ( 'NONE',  ( 1.960886852992497653, -24.44424927289185590, 12.96989951879399072 ) ) ;
#7385=EDGE_CURVE ( 'NONE', #8382, #12063, #4611, .T. ) ;
#7390=ORIENTED_EDGE ( 'NONE', *, *, #14242, .F. ) ;
#7391=CARTESIAN_POINT ( 'NONE',  ( 2.789999999999999147, -9.324097380959294412, -22.25075486061747654 ) ) ;
#7392=CARTESIAN_POINT ( 'NONE',  ( 1.394999999999998685, -27.76164181293049182, -4.147968289691579713 ) ) ;
#7397=ORIENTED_EDGE ( 'NONE', *, *, #13281, .F. ) ;
#7399=EDGE_CURVE ( 'NONE', #8616, #8417, #6959, .T. ) ;
#7405=ADVANCED_FACE ( 'NONE', ( #1050 ), #5745, .T. ) ;
#7410=CARTESIAN_POINT ( 'NONE',  ( 2.789999999999999147, -7.909232158574647009, -24.34211360614308006 ) ) ;
#7423=CARTESIAN_POINT ( 'NONE',  ( 2.604434514863827488, -10.67816411292148793, -23.63475234378993761 ) ) ;
#7430=DIRECTION ( 'NONE',  ( -1.000000000000000000, -0.000000000000000000, -0.000000000000000000 ) ) ;
#7432=FACE_OUTER_BOUND ( 'NONE', #10182, .T. ) ;
#7434=VECTOR ( 'NONE', #10818, 1000.000000000000000 ) ;
#7436=VERTEX_POINT ( 'NONE', #12096 ) ;
#7438=ORIENTED_EDGE ( 'NONE', *, *, #4586, .F. ) ;
#7439=DIRECTION ( 'NONE',  ( 0.000000000000000000, 0.000000000000000000, 1.000000000000000000 ) ) ;
#7440=CARTESIAN_POINT ( 'NONE',  ( 2.604434325169353581, -2.851997810081467577, -25.77772010606609498 ) ) ;
#7447=CARTESIAN_POINT ( 'NONE',  ( 0.006974693931641778172, 18.43727551351055283, -16.17543236987968669 ) ) ;
#7448=ORIENTED_EDGE ( 'NONE', *, *, #14334, .T. ) ;
#7451=CARTESIAN_POINT ( 'NONE',  ( 2.030753610301984313, -19.12676442129359700, 19.86438386685654578 ) ) ;
#7453=B_SPLINE_CURVE_WITH_KNOTS ( 'NONE', 3,
 ( #10583, #7194, #8190, #12868, #1207, #11573 ),
 .UNSPECIFIED., .F., .F.,
 ( 4, 2, 4 ),
 ( 4.462636695653741059E-07, 0.001879885036799761782, 0.003759323809929957915 ),
 .UNSPECIFIED. ) ;
#7461=CARTESIAN_POINT ( 'NONE',  ( 2.604434404052933694, 17.45907811351455408, 19.17825124759784572 ) ) ;
#7462=CARTESIAN_POINT ( 'NONE',  ( 0.000000000000000000, 20.70663861606293210, -15.04425356660737556 ) ) ;
#7464=DIRECTION ( 'NONE',  ( 0.000000000000000000, 0.000000000000000000, 1.000000000000000000 ) ) ;
#7465=CARTESIAN_POINT ( 'NONE',  ( 2.262072769566603636, 24.43806413951692136, -11.57956866523193185 ) ) ;
#7466=EDGE_CURVE ( 'NONE', #6526, #4130, #7824, .T. ) ;
#7468=DIRECTION ( 'NONE',  ( -1.000000000000000000, -0.000000000000000000, -0.000000000000000000 ) ) ;
#7469=AXIS2_PLACEMENT_3D ( 'NONE', #3825, #9827, #7524 ) ;
#7471=VERTEX_POINT ( 'NONE', #7273 ) ;
#7472=LINE ( 'NONE', #6317, #14380 ) ;
#7474=CARTESIAN_POINT ( 'NONE',  ( 1.039999999999997593, 0.000000000000000000, 0.000000000000000000 ) ) ;
#7476=CIRCLE ( 'NONE', #8685, 28.06981291497571007 ) ;
#7479=VERTEX_POINT ( 'NONE', #7582 ) ;
#7481=CARTESIAN_POINT ( 'NONE',  ( 1.039999999999998925, -4.147968289691484678, 27.76164181293050248 ) ) ;
#7486=EDGE_CURVE ( 'NONE', #12123, #3403, #13211, .T. ) ;
#7487=B_SPLINE_CURVE_WITH_KNOTS ( 'NONE', 3,
 ( #6280, #9885, #7440, #6359, #5380, #14441 ),
 .UNSPECIFIED., .F., .F.,
 ( 4, 2, 4 ),
 ( 2.132675795048140697E-07, 0.001878604073277005205, 0.003756994878974505639 ),
 .UNSPECIFIED. ) ;
#7495=ORIENTED_EDGE ( 'NONE', *, *, #14425, .T. ) ;
#7497=CIRCLE ( 'NONE', #603, 2.524999999999995914 ) ;
#7499=ADVANCED_FACE ( 'NONE', ( #14341 ), #11101, .T. ) ;
#7502=CARTESIAN_POINT ( 'NONE',  ( 1.749999999999998002, 27.68468304288259318, 4.633866840649019103 ) ) ;
#7508=FACE_OUTER_BOUND ( 'NONE', #7065, .T. ) ;
#7514=EDGE_LOOP ( 'NONE', ( #10606, #773, #10542, #8889, #7913, #11469 ) ) ;
#7524=DIRECTION ( 'NONE',  ( 0.000000000000000000, 0.000000000000000000, 1.000000000000000000 ) ) ;
#7525=ADVANCED_FACE ( 'NONE', ( #6418 ), #1935, .T. ) ;
#7527=CARTESIAN_POINT ( 'NONE',  ( 0.02436607992776194942, -5.391175441198450713, -24.15498966839968276 ) ) ;
#7535=ORIENTED_EDGE ( 'NONE', *, *, #12170, .F. ) ;
#7536=TOROIDAL_SURFACE ( 'NONE', #4598, 24.12539914357697768, 8.000000000000000000 ) ;
#7540=B_SPLINE_CURVE_WITH_KNOTS ( 'NONE', 3,
 ( #551, #13315, #9938, #3712 ),
 .UNSPECIFIED., .F., .F.,
 ( 4, 4 ),
 ( 0.005258105385878707357, 0.005948373736081385803 ),
 .UNSPECIFIED. ) ;
#7541=FACE_OUTER_BOUND ( 'NONE', #4320, .T. ) ;
#7543=FACE_OUTER_BOUND ( 'NONE', #10850, .T. ) ;
#7545=B_SPLINE_CURVE_WITH_KNOTS ( 'NONE', 3,
 ( #5690, #11515, #11657, #12741 ),
 .UNSPECIFIED., .F., .F.,
 ( 4, 4 ),
 ( 0.005342776758202895035, 0.005948405594583416715 ),
 .UNSPECIFIED. ) ;
#7546=CARTESIAN_POINT ( 'NONE',  ( 2.789999999999999147, -23.48180575137734039, 5.535312321042630934 ) ) ;
#7549=CARTESIAN_POINT ( 'NONE',  ( 2.789999999999999147, 0.000000000000000000, 0.000000000000000000 ) ) ;
#7553=ORIENTED_EDGE ( 'NONE', *, *, #8532, .F. ) ;
#7555=CARTESIAN_POINT ( 'NONE',  ( 2.765633920072235075, -12.59161484032896361, -21.30679549418645280 ) ) ;
#7559=CYLINDRICAL_SURFACE ( 'NONE', #2100, 4.000000000000000000 ) ;
#7561=CARTESIAN_POINT ( 'NONE',  ( 1.749999999999998002, -12.52377138324241734, 25.12109765559649688 ) ) ;
#7562=DIRECTION ( 'NONE',  ( 0.000000000000000000, 0.000000000000000000, 1.000000000000000000 ) ) ;
#7564=CARTESIAN_POINT ( 'NONE',  ( 1.749999999999998002, 27.68468304288259318, 4.633866840649019103 ) ) ;
#7566=CARTESIAN_POINT ( 'NONE',  ( 0.1855657168891856057, 12.84444904262024956, 22.53097606932990260 ) ) ;
#7568=VERTEX_POINT ( 'NONE', #13725 ) ;
#7570=ADVANCED_FACE ( 'NONE', ( #4124 ), #1190, .T. ) ;
#7573=VERTEX_POINT ( 'NONE', #3123 ) ;
#7575=CLOSED_SHELL ( 'NONE', ( #2722, #7649, #2317, #2833, #3856, #11418, #3633, #9994, #7970, #11632, #11713, #8222, #8160, #6264, #14278, #2707, #10563, #521, #11797, #1666, #7525, #917, #12100, #1195, #3388, #13369, #9708, #5460, #6746, #1291, #2279, #8307, #11449, #7405, #11162, #3557, #15165, #6038, #3184, #12820, #12345, #5051, #10783, #7699, #8140, #6740, #13486, #9428, #9848, #2178, #5133, #13774, #9635, #1870, #10217, #3055, #6228, #4520, #10706, #1467, #7570, #6859, #848, #11156, #8789, #787, #9150, #11409, #10323, #164, #14166, #7311, #11284, #13595, #5187, #10515, #9840, #12859, #3543, #11982, #8878, #4138, #2154, #6428, #4790, #10952, #11066, #5510, #2343, #6291, #1103, #10320, #10580, #12153, #3783, #3949, #13517, #12090, #9913, #3513, #1016, #14420, #13642, #14490, #12476, #11086, #930, #560, #4894, #7499, #345, #811, #6368, #14937, #3851, #10868, #8402, #645, #147, #9773, #5798, #13674, #1511, #2250, #12607, #5905, #306, #11603, #13873, #7310, #13007, #10124, #11731 ) ) ;
#7579=AXIS2_PLACEMENT_3D ( 'NONE', #3348, #8040, #12717 ) ;
#7581=ORIENTED_EDGE ( 'NONE', *, *, #9111, .T. ) ;
#7582=CARTESIAN_POINT ( 'NONE',  ( 0.02436607992776281678, 2.336989772644269436, 24.63872515616083447 ) ) ;
#7583=CARTESIAN_POINT ( 'NONE',  ( 1.039999999999995595, 4.147968289691676524, -27.76164181293047051 ) ) ;
#7585=EDGE_CURVE ( 'NONE', #12816, #7568, #10992, .T. ) ;
#7588=ORIENTED_EDGE ( 'NONE', *, *, #7792, .T. ) ;
#7592=CARTESIAN_POINT ( 'NONE',  ( 0.5321745379877909077, -23.74442027961350377, -12.96514671151793507 ) ) ;
#7593=AXIS2_PLACEMENT_3D ( 'NONE', #14671, #668, #14748 ) ;
#7594=FACE_OUTER_BOUND ( 'NONE', #13061, .T. ) ;
#7595=CARTESIAN_POINT ( 'NONE',  ( 0.02436607992776151574, -18.55949924794880346, -16.37294372382878649 ) ) ;
#7599=FACE_OUTER_BOUND ( 'NONE', #2166, .T. ) ;
#7608=ORIENTED_EDGE ( 'NONE', *, *, #8713, .F. ) ;
#7611=EDGE_LOOP ( 'NONE', ( #11819, #10038, #3925, #10587, #14591, #4572, #10111, #461 ) ) ;
#7614=EDGE_CURVE ( 'NONE', #1974, #4433, #732, .T. ) ;
#7615=CARTESIAN_POINT ( 'NONE',  ( 2.030753603471112889, -12.98165646470063983, -24.32906614999630790 ) ) ;
#7616=CARTESIAN_POINT ( 'NONE',  ( 2.789999999999999147, 7.772527002114753003, -23.17675759782032685 ) ) ;
#7618=DIRECTION ( 'NONE',  ( 1.000000000000000000, -0.000000000000000000, -0.000000000000000000 ) ) ;
#7629=EDGE_CURVE ( 'NONE', #9391, #14971, #3812, .T. ) ;
#7637=CARTESIAN_POINT ( 'NONE',  ( 2.765633920072236851, 24.15498966839963302, 5.391175441198700291 ) ) ;
#7639=B_SPLINE_CURVE_WITH_KNOTS ( 'NONE', 3,
 ( #15173, #4646, #4485, #3324 ),
 .UNSPECIFIED., .F., .F.,
 ( 4, 4 ),
 ( 0.005258139959819225183, 0.005948405594583413246 ),
 .UNSPECIFIED. ) ;
#7640=LINE ( 'NONE', #6477, #5101 ) ;
#7641=ORIENTED_EDGE ( 'NONE', *, *, #7871, .F. ) ;
#7649=ADVANCED_FACE ( 'NONE', ( #7809 ), #12630, .T. ) ;
#7651=EDGE_CURVE ( 'NONE', #13868, #7028, #4347, .T. ) ;
#7652=EDGE_LOOP ( 'NONE', ( #3443, #14878, #5659, #6014 ) ) ;
#7654=CARTESIAN_POINT ( 'NONE',  ( -7.816002369513581784E-14, 15.96555658743763217, 18.34439787333512939 ) ) ;
#7655=ORIENTED_EDGE ( 'NONE', *, *, #2240, .F. ) ;
#7658=CIRCLE ( 'NONE', #6186, 28.06981291497571007 ) ;
#7660=CARTESIAN_POINT ( 'NONE',  ( 1.039999999999996705, -19.67366047555515252, -20.02152543075367319 ) ) ;
#7661=CARTESIAN_POINT ( 'NONE',  ( 1.039999999999999147, 12.52377138324259676, -25.12109765559640095 ) ) ;
#7663=FACE_OUTER_BOUND ( 'NONE', #5710, .T. ) ;
#7667=CARTESIAN_POINT ( 'NONE',  ( 2.765633920072235519, -9.836394144775869819, 22.71065055754449347 ) ) ;
#7668=ORIENTED_EDGE ( 'NONE', *, *, #12045, .F. ) ;
#7670=CIRCLE ( 'NONE', #1039, 2.524999999999995914 ) ;
#7671=CARTESIAN_POINT ( 'NONE',  ( 1.749999999999998002, 27.68468304288265358, -4.633866840648635410 ) ) ;
#7676=CARTESIAN_POINT ( 'NONE',  ( 2.765633920072234631, 5.391175441198615914, 24.15498966839965078 ) ) ;
#7677=CARTESIAN_POINT ( 'NONE',  ( 2.789999999999999147, 24.44424927289184879, 0.2301004812061933913 ) ) ;
#7678=EDGE_LOOP ( 'NONE', ( #14908, #11756, #4922, #286 ) ) ;
#7679=ORIENTED_EDGE ( 'NONE', *, *, #3088, .F. ) ;
#7682=CARTESIAN_POINT ( 'NONE',  ( 0.000000000000000000, 1.991882183130641248, -24.04302995059964942 ) ) ;
#7683=CYLINDRICAL_SURFACE ( 'NONE', #10654, 13.19999999999999929 ) ;
#7684=CARTESIAN_POINT ( 'NONE',  ( 2.789999999999999147, 0.000000000000000000, 0.000000000000000000 ) ) ;
#7686=EDGE_CURVE ( 'NONE', #1104, #852, #5503, .T. ) ;
#7688=CARTESIAN_POINT ( 'NONE',  ( 2.171938186095908829, 23.93436800624300886, 12.96259772325185544 ) ) ;
#7689=ORIENTED_EDGE ( 'NONE', *, *, #13679, .T. ) ;
#7690=CARTESIAN_POINT ( 'NONE',  ( 0.000000000000000000, -22.25075486061745167, 9.324097380959385006 ) ) ;
#7694=ORIENTED_EDGE ( 'NONE', *, *, #4779, .F. ) ;
#7698=CARTESIAN_POINT ( 'NONE',  ( 2.790000000000076863, -12.51293083811783191, -20.85287692521943015 ) ) ;
#7699=ADVANCED_FACE ( 'NONE', ( #8173 ), #12846, .T. ) ;
#7700=CARTESIAN_POINT ( 'NONE',  ( 2.765633920072234631, 16.37294372382885044, -18.55949924794875017 ) ) ;
#7705=CARTESIAN_POINT ( 'NONE',  ( 2.601776144743012775, -10.68696068830424473, 23.64332819722378076 ) ) ;
#7710=AXIS2_PLACEMENT_3D ( 'NONE', #11242, #8782, #6639 ) ;
#7719=CARTESIAN_POINT ( 'NONE',  ( 1.039999999999996483, -19.67366047555544384, 20.02152543075338897 ) ) ;
#7726=CARTESIAN_POINT ( 'NONE',  ( 2.257825491203657275, 11.58891744060141882, -24.44564404695831783 ) ) ;
#7727=DIRECTION ( 'NONE',  ( -1.000000000000000000, 0.000000000000000000, 0.000000000000000000 ) ) ;
#7733=TOROIDAL_SURFACE ( 'NONE', #1102, 24.12539914357697413, 8.000000000000000000 ) ;
#7734=AXIS2_PLACEMENT_3D ( 'NONE', #13613, #9852, #5254 ) ;
#7743=AXIS2_PLACEMENT_3D ( 'NONE', #9174, #5722, #10394 ) ;
#7744=ORIENTED_EDGE ( 'NONE', *, *, #14074, .F. ) ;
#7747=DIRECTION ( 'NONE',  ( 0.000000000000000000, 0.000000000000000000, 1.000000000000000000 ) ) ;
#7752=CARTESIAN_POINT ( 'NONE',  ( 0.000000000000000000, -15.74360496233370021, -18.28042085475294698 ) ) ;
#7753=ORIENTED_EDGE ( 'NONE', *, *, #3036, .T. ) ;
#7754=ORIENTED_EDGE ( 'NONE', *, *, #804, .F. ) ;
#7755=CYLINDRICAL_SURFACE ( 'NONE', #4360, 2.524999999999995914 ) ;
#7756=CIRCLE ( 'NONE', #3100, 28.06981291497571007 ) ;
#7761=CARTESIAN_POINT ( 'NONE',  ( 2.789999999999999147, 7.909232158575156824, -24.34211360614291664 ) ) ;
#7764=CARTESIAN_POINT ( 'NONE',  ( 2.351340098004231383, 23.41653927703715965, 12.93238701107315514 ) ) ;
#7765=ORIENTED_EDGE ( 'NONE', *, *, #11989, .F. ) ;
#7770=ORIENTED_EDGE ( 'NONE', *, *, #10029, .F. ) ;
#7779=CIRCLE ( 'NONE', #1150, 2.524999999999995914 ) ;
#7780=CIRCLE ( 'NONE', #8258, 2.524999999999995914 ) ;
#7788=EDGE_CURVE ( 'NONE', #12063, #2289, #5696, .T. ) ;
#7790=CIRCLE ( 'NONE', #10246, 24.12539914357697413 ) ;
#7791=CARTESIAN_POINT ( 'NONE',  ( 0.02436607992775934733, -21.30679549418640306, 12.59161484032904887 ) ) ;
#7792=EDGE_CURVE ( 'NONE', #9957, #7850, #10828, .T. ) ;
#7793=CIRCLE ( 'NONE', #10490, 24.12539914357697768 ) ;
#7794=ORIENTED_EDGE ( 'NONE', *, *, #5278, .T. ) ;
#7800=ORIENTED_EDGE ( 'NONE', *, *, #13476, .T. ) ;
#7802=EDGE_CURVE ( 'NONE', #4654, #14563, #5885, .T. ) ;
#7804=DIRECTION ( 'NONE',  ( 1.000000000000000000, 0.000000000000000000, -0.000000000000000000 ) ) ;
#7809=FACE_OUTER_BOUND ( 'NONE', #10570, .T. ) ;
#7819=AXIS2_PLACEMENT_3D ( 'NONE', #12590, #5760, #5540 ) ;
#7824=CIRCLE ( 'NONE', #9785, 24.12539914357697768 ) ;
#7838=ORIENTED_EDGE ( 'NONE', *, *, #331, .F. ) ;
#7839=VERTEX_POINT ( 'NONE', #1255 ) ;
#7842=ORIENTED_EDGE ( 'NONE', *, *, #13746, .T. ) ;
#7845=CARTESIAN_POINT ( 'NONE',  ( 2.789999999999999147, -5.535312321042557215, -23.48180575137735815 ) ) ;
#7850=VERTEX_POINT ( 'NONE', #14172 ) ;
#7851=DIRECTION ( 'NONE',  ( 0.000000000000000000, 0.000000000000000000, 1.000000000000000000 ) ) ;
#7854=VERTEX_POINT ( 'NONE', #396 ) ;
#7856=EDGE_CURVE ( 'NONE', #12188, #12123, #5118, .T. ) ;
#7865=ORIENTED_EDGE ( 'NONE', *, *, #6521, .T. ) ;
#7866=DIRECTION ( 'NONE',  ( 0.000000000000000000, 0.000000000000000000, 1.000000000000000000 ) ) ;
#7867=FACE_OUTER_BOUND ( 'NONE', #6587, .T. ) ;
#7870=CARTESIAN_POINT ( 'NONE',  ( 0.5321745326902584949, 3.467596033028283564, 26.83036154824995023 ) ) ;
#7871=EDGE_CURVE ( 'NONE', #11410, #2490, #2788, .T. ) ;
#7874=CARTESIAN_POINT ( 'NONE',  ( 1.749999999999998002, -4.147968289691086774, -27.76164181293056288 ) ) ;
#7889=ORIENTED_EDGE ( 'NONE', *, *, #8825, .F. ) ;
#7893=DIRECTION ( 'NONE',  ( -1.000000000000000000, 0.000000000000000000, 0.000000000000000000 ) ) ;
#7896=CARTESIAN_POINT ( 'NONE',  ( 1.749999999999998002, -12.52377138324206030, -25.12109765559667096 ) ) ;
#7898=DIRECTION ( 'NONE',  ( 0.000000000000000000, 0.5877852522924629231, 0.8090169943749548898 ) ) ;
#7903=CARTESIAN_POINT ( 'NONE',  ( 1.394999999999999574, -20.02152543075359858, 19.67366047555523778 ) ) ;
#7910=ORIENTED_EDGE ( 'NONE', *, *, #2258, .F. ) ;
#7912=CARTESIAN_POINT ( 'NONE',  ( 1.039999999999997593, 0.000000000000000000, 0.000000000000000000 ) ) ;
#7913=ORIENTED_EDGE ( 'NONE', *, *, #13560, .F. ) ;
#7914=CARTESIAN_POINT ( 'NONE',  ( 2.789999999999999147, 7.909232158575156824, -21.81711360614291806 ) ) ;
#7918=CARTESIAN_POINT ( 'NONE',  ( 0.07181523211953112773, 23.19431517146946931, -10.24584646439514657 ) ) ;
#7921=CARTESIAN_POINT ( 'NONE',  ( 0.02436607992776628623, 24.63872515616082737, -2.336989772644355590 ) ) ;
#7922=CARTESIAN_POINT ( 'NONE',  ( 2.765633920072236851, 24.15498966839963302, 5.391175441198700291 ) ) ;
#7926=ORIENTED_EDGE ( 'NONE', *, *, #8626, .T. ) ;
#7929=CARTESIAN_POINT ( 'NONE',  ( 1.039999999999996927, -25.12109765559644714, -12.52377138324250438 ) ) ;
#7931=EDGE_CURVE ( 'NONE', #9391, #5611, #12155, .T. ) ;
#7933=VERTEX_POINT ( 'NONE', #9627 ) ;
#7939=CARTESIAN_POINT ( 'NONE',  ( 2.789999999999999147, 22.25075486061751207, -9.324097380959219805 ) ) ;
#7940=ORIENTED_EDGE ( 'NONE', *, *, #11422, .F. ) ;
#7945=EDGE_CURVE ( 'NONE', #7436, #14511, #13837, .T. ) ;
#7950=CYLINDRICAL_SURFACE ( 'NONE', #4355, 2.524999999999995914 ) ;
#7951=AXIS2_PLACEMENT_3D ( 'NONE', #6213, #10892, #9747 ) ;
#7954=EDGE_CURVE ( 'NONE', #4522, #11822, #12167, .T. ) ;
#7964=CARTESIAN_POINT ( 'NONE',  ( 2.789999999999999147, -20.70663861606282197, 15.04425356660753188 ) ) ;
#7969=B_SPLINE_CURVE_WITH_KNOTS ( 'NONE', 3,
 ( #1162, #9680, #59, #2537, #10544, #8300 ),
 .UNSPECIFIED., .F., .F.,
 ( 4, 2, 4 ),
 ( 4.462636678113234028E-07, 0.001879885020955180275, 0.003759323778242549142 ),
 .UNSPECIFIED. ) ;
#7970=ADVANCED_FACE ( 'NONE', ( #4022 ), #8696, .F. ) ;
#7972=CARTESIAN_POINT ( 'NONE',  ( 2.601776121706764311, -17.47009390565504816, 19.18368891937484477 ) ) ;
#7975=ORIENTED_EDGE ( 'NONE', *, *, #804, .T. ) ;
#7976=EDGE_CURVE ( 'NONE', #5736, #807, #6973, .T. ) ;
#7977=DIRECTION ( 'NONE',  ( -1.000000000000000000, 0.000000000000000000, 0.000000000000000000 ) ) ;
#7979=ORIENTED_EDGE ( 'NONE', *, *, #6706, .F. ) ;
#7982=CARTESIAN_POINT ( 'NONE',  ( -10.00000000000000000, 0.000000000000000000, 0.000000000000000000 ) ) ;
#7984=DIRECTION ( 'NONE',  ( 1.000000000000000000, 0.000000000000000000, 0.000000000000000000 ) ) ;
#7987=VECTOR ( 'NONE', #7804, 1000.000000000000000 ) ;
#7989=CIRCLE ( 'NONE', #10687, 24.12539914357697768 ) ;
#7992=ORIENTED_EDGE ( 'NONE', *, *, #4307, .F. ) ;
#7993=DIRECTION ( 'NONE',  ( 0.000000000000000000, 0.000000000000000000, -1.000000000000000000 ) ) ;
#8002=CARTESIAN_POINT ( 'NONE',  ( 0.02436607992775717893, -9.836394144775869819, 22.71065055754449347 ) ) ;
#8004=CARTESIAN_POINT ( 'NONE',  ( 2.262072637928882468, -12.96450951081233605, 23.73240184472491876 ) ) ;
#8009=CARTESIAN_POINT ( 'NONE',  ( 2.789999999999999147, 22.71065055754452544, 9.836394144775786330 ) ) ;
#8020=DIRECTION ( 'NONE',  ( 0.000000000000000000, 0.000000000000000000, 1.000000000000000000 ) ) ;
#8022=AXIS2_PLACEMENT_3D ( 'NONE', #9730, #13262, #12180 ) ;
#8023=DIRECTION ( 'NONE',  ( -1.000000000000000000, -0.000000000000000000, -0.000000000000000000 ) ) ;
#8027=CARTESIAN_POINT ( 'NONE',  ( 2.789999999999999147, 23.48180575137737947, -5.535312321042476391 ) ) ;
#8029=AXIS2_PLACEMENT_3D ( 'NONE', #4072, #9987, #14689 ) ;
#8030=EDGE_LOOP ( 'NONE', ( #14632, #12462, #73, #1292, #7975, #8407 ) ) ;
#8031=CIRCLE ( 'NONE', #13925, 2.524999999999997691 ) ;
#8032=CYLINDRICAL_SURFACE ( 'NONE', #2388, 2.524999999999995914 ) ;
#8034=CARTESIAN_POINT ( 'NONE',  ( 8.000000000000000000, 0.000000000000000000, 0.000000000000000000 ) ) ;
#8038=EDGE_LOOP ( 'NONE', ( #2813, #12996, #2436, #11499, #12412, #10738, #11838, #702, #12781, #12205, #15157, #10074, #597, #7438, #174, #11612, #10781, #10721, #1960, #3658, #12776, #12227, #5065, #1898, #2783, #8662, #7754, #5549, #2944, #9995, #13057, #9618, #7679, #9263, #9025, #1812, #13457, #6242, #10605, #11055, #8342, #14079, #4501, #7889, #6072 ) ) ;
#8039=CARTESIAN_POINT ( 'NONE',  ( -7.810937420967753123E-14, 20.85287692521929159, 12.51293083811806461 ) ) ;
#8040=DIRECTION ( 'NONE',  ( -1.000000000000000000, -0.000000000000000000, 0.000000000000000000 ) ) ;
#8041=AXIS2_PLACEMENT_3D ( 'NONE', #5378, #7893, #13732 ) ;
#8042=CARTESIAN_POINT ( 'NONE',  ( 0.000000000000000000, -23.48180575137736170, 5.535312321042622052 ) ) ;
#8046=AXIS2_PLACEMENT_3D ( 'NONE', #8583, #13192, #8728 ) ;
#8051=CARTESIAN_POINT ( 'NONE',  ( 2.783068888626321513, 22.53293026234517171, -9.685942809246819607 ) ) ;
#8052=EDGE_CURVE ( 'NONE', #5611, #6969, #7476, .T. ) ;
#8058=FACE_OUTER_BOUND ( 'NONE', #1481, .T. ) ;
#8060=AXIS2_PLACEMENT_3D ( 'NONE', #7352, #8637, #13254 ) ;
#8062=CARTESIAN_POINT ( 'NONE',  ( 2.262072769566604524, -24.43806413951684320, 11.57956866523208461 ) ) ;
#8063=CARTESIAN_POINT ( 'NONE',  ( 1.749999999999998002, -4.633866840649122132, 27.68468304288257542 ) ) ;
#8072=EDGE_CURVE ( 'NONE', #12913, #2534, #11285, .T. ) ;
#8073=EDGE_LOOP ( 'NONE', ( #5474, #659, #10560, #2403 ) ) ;
#8074=DIRECTION ( 'NONE',  ( -1.000000000000000000, -0.000000000000000000, -0.000000000000000000 ) ) ;
#8076=CIRCLE ( 'NONE', #4396, 28.06981291497571362 ) ;
#8077=DIRECTION ( 'NONE',  ( 0.000000000000000000, 0.000000000000000000, 1.000000000000000000 ) ) ;
#8078=VERTEX_POINT ( 'NONE', #549 ) ;
#8080=ORIENTED_EDGE ( 'NONE', *, *, #1667, .T. ) ;
#8087=CARTESIAN_POINT ( 'NONE',  ( 2.789999999999999147, -19.91106274590503844, -14.18181402625762821 ) ) ;
#8090=LINE ( 'NONE', #709, #13242 ) ;
#8091=EDGE_LOOP ( 'NONE', ( #8470, #9520, #9677, #13561, #14686, #9289 ) ) ;
#8096=ORIENTED_EDGE ( 'NONE', *, *, #12758, .F. ) ;
#8098=LINE ( 'NONE', #9169, #10917 ) ;
#8101=CARTESIAN_POINT ( 'NONE',  ( 2.789999999999999147, 7.334849878007507762, 23.31896751603335005 ) ) ;
#8104=FACE_OUTER_BOUND ( 'NONE', #11973, .T. ) ;
#8107=CARTESIAN_POINT ( 'NONE',  ( -10.00000000000000000, 0.000000000000000000, 0.000000000000000000 ) ) ;
#8108=CARTESIAN_POINT ( 'NONE',  ( 2.789999999999999147, -20.70663861606260170, -15.04425356660783031 ) ) ;
#8111=DIRECTION ( 'NONE',  ( -1.000000000000000000, 0.000000000000000000, 0.000000000000000000 ) ) ;
#8115=CARTESIAN_POINT ( 'NONE',  ( 2.789679245949058917, 20.70663861606308487, -12.51925356660738053 ) ) ;
#8116=EDGE_CURVE ( 'NONE', #11849, #7839, #221, .T. ) ;
#8118=FACE_OUTER_BOUND ( 'NONE', #9083, .T. ) ;
#8119=CARTESIAN_POINT ( 'NONE',  ( 2.765633920072239071, -16.37294372382844543, -18.55949924794910544 ) ) ;
#8120=EDGE_CURVE ( 'NONE', #6398, #3345, #10898, .T. ) ;
#8123=CARTESIAN_POINT ( 'NONE',  ( 2.789999999999999147, 22.71065055754465689, -9.836394144775473691 ) ) ;
#8127=VERTEX_POINT ( 'NONE', #4940 ) ;
#8130=ORIENTED_EDGE ( 'NONE', *, *, #8615, .T. ) ;
#8134=FACE_OUTER_BOUND ( 'NONE', #3146, .T. ) ;
#8138=ORIENTED_EDGE ( 'NONE', *, *, #6958, .F. ) ;
#8140=ADVANCED_FACE ( 'NONE', ( #8531 ), #1767, .T. ) ;
#8144=ORIENTED_EDGE ( 'NONE', *, *, #10596, .F. ) ;
#8145=ORIENTED_EDGE ( 'NONE', *, *, #9159, .F. ) ;
#8146=ORIENTED_EDGE ( 'NONE', *, *, #2015, .T. ) ;
#8151=AXIS2_PLACEMENT_3D ( 'NONE', #32, #10512, #11724 ) ;
#8153=FACE_OUTER_BOUND ( 'NONE', #11862, .T. ) ;
#8157=CIRCLE ( 'NONE', #1535, 24.12539914357697413 ) ;
#8160=ADVANCED_FACE ( 'NONE', ( #3846 ), #10403, .T. ) ;
#8166=ORIENTED_EDGE ( 'NONE', *, *, #4051, .T. ) ;
#8170=ORIENTED_EDGE ( 'NONE', *, *, #6839, .T. ) ;
#8173=FACE_OUTER_BOUND ( 'NONE', #2407, .T. ) ;
#8174=CARTESIAN_POINT ( 'NONE',  ( 2.789999999999999147, -5.535312321042889394, 23.48180575137727999 ) ) ;
#8176=CARTESIAN_POINT ( 'NONE',  ( 0.000000000000000000, -15.74360496233370021, -18.28042085475294698 ) ) ;
#8182=FACE_OUTER_BOUND ( 'NONE', #7514, .T. ) ;
#8184=DIRECTION ( 'NONE',  ( -1.000000000000000000, -0.000000000000000000, -0.000000000000000000 ) ) ;
#8190=CARTESIAN_POINT ( 'NONE',  ( 0.5321745379877897975, -12.96514671151783915, 23.74442027961355706 ) ) ;
#8197=ORIENTED_EDGE ( 'NONE', *, *, #10499, .F. ) ;
#8203=CARTESIAN_POINT ( 'NONE',  ( 0.02436607992776498519, -21.30679549418621832, -12.59161484032935618 ) ) ;
#8207=ORIENTED_EDGE ( 'NONE', *, *, #842, .T. ) ;
#8211=CARTESIAN_POINT ( 'NONE',  ( -7.770166132776744975E-14, -12.51293083811813389, 20.85287692521926672 ) ) ;
#8222=ADVANCED_FACE ( 'NONE', ( #7543 ), #858, .T. ) ;
#8226=ORIENTED_EDGE ( 'NONE', *, *, #13779, .F. ) ;
#8231=B_SPLINE_CURVE_WITH_KNOTS ( 'NONE', 3,
 ( #6360, #8586, #11043, #1820, #9886, #14585 ),
 .UNSPECIFIED., .F., .F.,
 ( 4, 2, 4 ),
 ( 4.462636678112536814E-07, 0.001879885020955181143, 0.003759323778242551310 ),
 .UNSPECIFIED. ) ;
#8234=CARTESIAN_POINT ( 'NONE',  ( 0.000000000000000000, 0.000000000000000000, 0.000000000000000000 ) ) ;
#8238=CARTESIAN_POINT ( 'NONE',  ( 2.765633920072236851, -22.71065055754445439, -9.836394144775947979 ) ) ;
#8243=EDGE_CURVE ( 'NONE', #1849, #7933, #11637, .T. ) ;
#8246=CYLINDRICAL_SURFACE ( 'NONE', #8686, 2.524999999999995914 ) ;
#8247=ORIENTED_EDGE ( 'NONE', *, *, #3988, .T. ) ;
#8252=ORIENTED_EDGE ( 'NONE', *, *, #7138, .T. ) ;
#8256=CARTESIAN_POINT ( 'NONE',  ( 2.780897501012522977, 21.10878525316979903, -12.54316204260869760 ) ) ;
#8258=AXIS2_PLACEMENT_3D ( 'NONE', #5245, #7468, #1625 ) ;
#8259=CARTESIAN_POINT ( 'NONE',  ( 1.039999999999997593, -24.89775460606841051, 12.96210679857778025 ) ) ;
#8266=CARTESIAN_POINT ( 'NONE',  ( 2.257825477245772650, 19.66801664102704095, 18.57583492944426951 ) ) ;
#8268=CARTESIAN_POINT ( 'NONE',  ( 2.789999999999999147, 0.000000000000000000, 0.000000000000000000 ) ) ;
#8269=CARTESIAN_POINT ( 'NONE',  ( -10.00000000000000000, 0.000000000000000000, 0.000000000000000000 ) ) ;
#8274=ORIENTED_EDGE ( 'NONE', *, *, #6275, .F. ) ;
#8275=TOROIDAL_SURFACE ( 'NONE', #167, 24.12539914357697768, 8.000000000000000000 ) ;
#8277=DIRECTION ( 'NONE',  ( -1.000000000000000000, -0.000000000000000000, -0.000000000000000000 ) ) ;
#8279=CIRCLE ( 'NONE', #956, 28.06981291497571362 ) ;
#8281=DIRECTION ( 'NONE',  ( -1.000000000000000000, -0.000000000000000000, -0.000000000000000000 ) ) ;
#8289=CARTESIAN_POINT ( 'NONE',  ( 0.000000000000000000, 0.000000000000000000, 0.000000000000000000 ) ) ;
#8290=VECTOR ( 'NONE', #10611, 1000.000000000000000 ) ;
#8292=EDGE_CURVE ( 'NONE', #13868, #10903, #9816, .T. ) ;
#8296=ORIENTED_EDGE ( 'NONE', *, *, #8888, .F. ) ;
#8297=ORIENTED_EDGE ( 'NONE', *, *, #13799, .F. ) ;
#8300=CARTESIAN_POINT ( 'NONE',  ( 2.765633920072233742, -24.15498966839966855, 5.391175441198523544 ) ) ;
#8301=DIRECTION ( 'NONE',  ( 0.000000000000000000, 0.000000000000000000, 1.000000000000000000 ) ) ;
#8307=ADVANCED_FACE ( 'NONE', ( #12449 ), #10143, .T. ) ;
#8311=AXIS2_PLACEMENT_3D ( 'NONE', #3895, #565, #9876 ) ;
#8313=ORIENTED_EDGE ( 'NONE', *, *, #2597, .F. ) ;
#8318=ORIENTED_EDGE ( 'NONE', *, *, #4205, .T. ) ;
#8327=EDGE_CURVE ( 'NONE', #1528, #11073, #3314, .T. ) ;
#8330=FACE_OUTER_BOUND ( 'NONE', #12198, .T. ) ;
#8332=ORIENTED_EDGE ( 'NONE', *, *, #3716, .T. ) ;
#8333=ORIENTED_EDGE ( 'NONE', *, *, #505, .T. ) ;
#8339=CARTESIAN_POINT ( 'NONE',  ( 1.749999999999998002, 0.000000000000000000, 0.000000000000000000 ) ) ;
#8340=CARTESIAN_POINT ( 'NONE',  ( 8.000000000000000000, 0.000000000000000000, 0.000000000000000000 ) ) ;
#8341=CARTESIAN_POINT ( 'NONE',  ( 1.749999999999998002, -27.76164181293054511, 4.147968289691195132 ) ) ;
#8342=ORIENTED_EDGE ( 'NONE', *, *, #5568, .F. ) ;
#8343=CARTESIAN_POINT ( 'NONE',  ( 2.789999999999999147, 22.25075486061751207, -9.324097380959219805 ) ) ;
#8346=ORIENTED_EDGE ( 'NONE', *, *, #11989, .T. ) ;
#8349=EDGE_CURVE ( 'NONE', #1588, #5525, #5532, .T. ) ;
#8350=VERTEX_POINT ( 'NONE', #13677 ) ;
#8353=EDGE_CURVE ( 'NONE', #2853, #1779, #1556, .T. ) ;
#8355=CARTESIAN_POINT ( 'NONE',  ( 0.02436607992776108206, -24.15498966839966855, 5.391175441198523544 ) ) ;
#8358=VERTEX_POINT ( 'NONE', #3076 ) ;
#8359=CYLINDRICAL_SURFACE ( 'NONE', #14984, 2.524999999999995914 ) ;
#8360=EDGE_CURVE ( 'NONE', #14624, #8921, #9208, .T. ) ;
#8361=EDGE_LOOP ( 'NONE', ( #6051, #9170, #6850, #13519 ) ) ;
#8362=CARTESIAN_POINT ( 'NONE',  ( 0.000000000000000000, -20.70663861606282197, 15.04425356660753188 ) ) ;
#8365=ORIENTED_EDGE ( 'NONE', *, *, #1210, .F. ) ;
#8366=ORIENTED_EDGE ( 'NONE', *, *, #109, .F. ) ;
#8368=ORIENTED_EDGE ( 'NONE', *, *, #4466, .F. ) ;
#8373=CARTESIAN_POINT ( 'NONE',  ( 2.783068961317271217, -12.53626894672843051, 21.08061549536610713 ) ) ;
#8374=ORIENTED_EDGE ( 'NONE', *, *, #9310, .T. ) ;
#8375=DIRECTION ( 'NONE',  ( 0.000000000000000000, 0.000000000000000000, 1.000000000000000000 ) ) ;
#8377=ORIENTED_EDGE ( 'NONE', *, *, #4698, .F. ) ;
#8380=FACE_OUTER_BOUND ( 'NONE', #11381, .T. ) ;
#8381=ORIENTED_EDGE ( 'NONE', *, *, #11277, .T. ) ;
#8382=VERTEX_POINT ( 'NONE', #5542 ) ;
#8388=B_SPLINE_CURVE_WITH_KNOTS ( 'NONE', 3,
 ( #561, #5282, #13862, #14088, #9177, #10630 ),
 .UNSPECIFIED., .F., .F.,
 ( 4, 2, 4 ),
 ( 2.321268216997094965E-07, 0.001878622960950492287, 0.003757013795079284547 ),
 .UNSPECIFIED. ) ;
#8389=CARTESIAN_POINT ( 'NONE',  ( 2.789999999999999147, 9.324097380959445402, 22.25075486061742325 ) ) ;
#8393=CARTESIAN_POINT ( 'NONE',  ( 2.789999999999999147, -23.31896751603326834, -7.334849878007764445 ) ) ;
#8396=CARTESIAN_POINT ( 'NONE',  ( 2.789999999999999147, -24.04302995059966719, 1.991882183130210482 ) ) ;
#8398=ORIENTED_EDGE ( 'NONE', *, *, #3432, .F. ) ;
#8399=EDGE_LOOP ( 'NONE', ( #9584, #11962, #8978, #10332, #1728, #5368 ) ) ;
#8400=CARTESIAN_POINT ( 'NONE',  ( 0.02436607992776411782, -24.63872515616084513, 2.336989772644183283 ) ) ;
#8401=CARTESIAN_POINT ( 'NONE',  ( 0.000000000000000000, -23.48180575137727288, -5.535312321042949790 ) ) ;
#8402=ADVANCED_FACE ( 'NONE', ( #12876 ), #2362, .T. ) ;
#8406=CARTESIAN_POINT ( 'NONE',  ( 1.749999999999998002, 0.000000000000000000, 0.000000000000000000 ) ) ;
#8407=ORIENTED_EDGE ( 'NONE', *, *, #13023, .F. ) ;
#8409=DIRECTION ( 'NONE',  ( -1.000000000000000000, -0.000000000000000000, -0.000000000000000000 ) ) ;
#8411=DIRECTION ( 'NONE',  ( 0.000000000000000000, 0.000000000000000000, 1.000000000000000000 ) ) ;
#8417=VERTEX_POINT ( 'NONE', #4609 ) ;
#8418=CARTESIAN_POINT ( 'NONE',  ( 0.000000000000000000, 15.74360496233409634, -18.28042085475261302 ) ) ;
#8426=CARTESIAN_POINT ( 'NONE',  ( 0.5321745087963422050, -11.58891744060090367, -24.44564404695856297 ) ) ;
#8430=ORIENTED_EDGE ( 'NONE', *, *, #5524, .T. ) ;
#8431=CARTESIAN_POINT ( 'NONE',  ( 1.039999999999996927, 20.02152543075374069, -19.67366047555508501 ) ) ;
#8435=ORIENTED_EDGE ( 'NONE', *, *, #6769, .T. ) ;
#8439=ORIENTED_EDGE ( 'NONE', *, *, #10755, .F. ) ;
#8443=DIRECTION ( 'NONE',  ( -1.000000000000000000, -0.000000000000000000, -0.000000000000000000 ) ) ;
#8448=AXIS2_PLACEMENT_3D ( 'NONE', #4693, #2452, #12881 ) ;
#8451=AXIS2_PLACEMENT_3D ( 'NONE', #13352, #13278, #13436 ) ;
#8453=CARTESIAN_POINT ( 'NONE',  ( 1.394999999999999574, 27.76164181293051669, 4.147968289691385202 ) ) ;
#8456=VERTEX_POINT ( 'NONE', #1215 ) ;
#8465=AXIS2_PLACEMENT_3D ( 'NONE', #13492, #2963, #14876 ) ;
#8467=CARTESIAN_POINT ( 'NONE',  ( 2.790000000000000480, -22.37986894186679265, 9.514945144208653005 ) ) ;
#8468=CARTESIAN_POINT ( 'NONE',  ( 0.1882239034349760531, 12.84621645676876867, -22.54313264454999199 ) ) ;
#8469=CARTESIAN_POINT ( 'NONE',  ( 2.604434261026090880, -25.39738473784997552, -5.253342437939998888 ) ) ;
#8470=ORIENTED_EDGE ( 'NONE', *, *, #6661, .T. ) ;
#8472=EDGE_CURVE ( 'NONE', #1779, #12872, #3397, .T. ) ;
#8473=CARTESIAN_POINT ( 'NONE',  ( 2.765633920072235519, -18.55949924794880346, -16.37294372382878649 ) ) ;
#8474=ORIENTED_EDGE ( 'NONE', *, *, #6381, .T. ) ;
#8475=DIRECTION ( 'NONE',  ( 0.000000000000000000, 0.000000000000000000, 1.000000000000000000 ) ) ;
#8480=CARTESIAN_POINT ( 'NONE',  ( 0.000000000000000000, -24.34211360614294506, -7.909232158575071558 ) ) ;
#8481=CARTESIAN_POINT ( 'NONE',  ( 1.749999999999998002, -25.12109765559643648, -12.52377138324252570 ) ) ;
#8486=CARTESIAN_POINT ( 'NONE',  ( 2.790000000000000036, 18.34424029220134500, -15.96500990068104997 ) ) ;
#8487=AXIS2_PLACEMENT_3D ( 'NONE', #13666, #9073, #5166 ) ;
#8488=EDGE_CURVE ( 'NONE', #15084, #1974, #14389, .T. ) ;
#8496=B_SPLINE_CURVE_WITH_KNOTS ( 'NONE', 3,
 ( #1372, #4702, #1295, #11753 ),
 .UNSPECIFIED., .F., .F.,
 ( 4, 4 ),
 ( 0.003263275852154239043, 0.003756984793529996591 ),
 .UNSPECIFIED. ) ;
#8498=AXIS2_PLACEMENT_3D ( 'NONE', #11987, #1473, #5869 ) ;
#8504=CIRCLE ( 'NONE', #655, 2.524999999999996358 ) ;
#8505=CYLINDRICAL_SURFACE ( 'NONE', #13621, 13.19999999999999929 ) ;
#8511=CARTESIAN_POINT ( 'NONE',  ( 2.765633920072233742, -24.15498966839966855, 5.391175441198523544 ) ) ;
#8517=VERTEX_POINT ( 'NONE', #13552 ) ;
#8519=CIRCLE ( 'NONE', #6803, 2.524999999999997247 ) ;
#8520=CARTESIAN_POINT ( 'NONE',  ( 0.000000000000000000, 2.680914349914567470E-13, -23.06981291497571362 ) ) ;
#8521=FACE_OUTER_BOUND ( 'NONE', #4199, .T. ) ;
#8522=VECTOR ( 'NONE', #10359, 1000.000000000000000 ) ;
#8526=CARTESIAN_POINT ( 'NONE',  ( 0.000000000000000000, 20.62201879784911540, 12.52067188844362100 ) ) ;
#8531=FACE_OUTER_BOUND ( 'NONE', #10450, .T. ) ;
#8532=EDGE_CURVE ( 'NONE', #2696, #7479, #10025, .T. ) ;
#8539=VECTOR ( 'NONE', #2091, 1000.000000000000000 ) ;
#8543=ORIENTED_EDGE ( 'NONE', *, *, #3705, .F. ) ;
#8546=EDGE_LOOP ( 'NONE', ( #9508, #12319, #8332, #4753, #11475, #3994, #2626, #10002 ) ) ;
#8547=AXIS2_PLACEMENT_3D ( 'NONE', #9955, #10874, #4043 ) ;
#8549=ORIENTED_EDGE ( 'NONE', *, *, #227, .T. ) ;
#8551=CARTESIAN_POINT ( 'NONE',  ( 0.02436607992775934733, -2.336989772644440855, 24.63872515616082026 ) ) ;
#8553=CARTESIAN_POINT ( 'NONE',  ( 0.07181525480391388883, 12.74223776959231991, -21.92234060054331479 ) ) ;
#8558=B_SPLINE_CURVE_WITH_KNOTS ( 'NONE', 3,
 ( #8396, #9563, #15132, #12012 ),
 .UNSPECIFIED., .F., .F.,
 ( 4, 4 ),
 ( 0.005258120783916810613, 0.005948386350302961936 ),
 .UNSPECIFIED. ) ;
#8559=CARTESIAN_POINT ( 'NONE',  ( 2.790000000000079527, -18.34439787333494820, -15.96555658743782580 ) ) ;
#8564=ORIENTED_EDGE ( 'NONE', *, *, #1586, .T. ) ;
#8566=CARTESIAN_POINT ( 'NONE',  ( 2.789999999999999147, 2.336989772644613161, -24.63872515616080250 ) ) ;
#8568=CARTESIAN_POINT ( 'NONE',  ( 0.1882239080259275332, 25.40949241676353410, 5.251266773802457877 ) ) ;
#8575=DIRECTION ( 'NONE',  ( 0.000000000000000000, 0.8090169943749527803, -0.5877852522924655876 ) ) ;
#8577=ORIENTED_EDGE ( 'NONE', *, *, #15118, .T. ) ;
#8583=CARTESIAN_POINT ( 'NONE',  ( 8.000000000000000000, 0.000000000000000000, 0.000000000000000000 ) ) ;
#8586=CARTESIAN_POINT ( 'NONE',  ( 2.030753602223783094, -4.828194074574165384, -27.14986936243579763 ) ) ;
#8593=ORIENTED_EDGE ( 'NONE', *, *, #14613, .T. ) ;
#8598=B_SPLINE_CURVE_WITH_KNOTS ( 'NONE', 3,
 ( #7660, #11187, #663, #11852, #5815, #7185 ),
 .UNSPECIFIED., .F., .F.,
 ( 4, 2, 4 ),
 ( 4.462636808949230078E-07, 0.001879885123572232067, 0.003759323983463569441 ),
 .UNSPECIFIED. ) ;
#8599=DIRECTION ( 'NONE',  ( -1.000000000000000000, -0.000000000000000000, 0.000000000000000000 ) ) ;
#8603=VERTEX_POINT ( 'NONE', #11248 ) ;
#8604=CARTESIAN_POINT ( 'NONE',  ( 2.783068945535915439, 24.42321038836782776, -2.248820353273055517 ) ) ;
#8606=CARTESIAN_POINT ( 'NONE',  ( 1.394999999999999574, -12.52377138324241734, 25.12109765559649688 ) ) ;
#8607=CARTESIAN_POINT ( 'NONE',  ( 1.039999999999997371, -4.147968289691092991, -27.76164181293055933 ) ) ;
#8608=DIRECTION ( 'NONE',  ( -1.000000000000000000, -0.000000000000000000, -0.000000000000000000 ) ) ;
#8615=EDGE_CURVE ( 'NONE', #9774, #3458, #5763, .T. ) ;
#8616=VERTEX_POINT ( 'NONE', #7939 ) ;
#8620=EDGE_LOOP ( 'NONE', ( #13549, #9455, #3033, #12752, #215, #2910, #8951, #12596 ) ) ;
#8623=CARTESIAN_POINT ( 'NONE',  ( 2.718184767880469810, -10.24584646439555691, 23.19431517146929878 ) ) ;
#8626=EDGE_CURVE ( 'NONE', #11392, #3403, #7989, .T. ) ;
#8628=DIRECTION ( 'NONE',  ( 0.000000000000000000, 0.000000000000000000, 1.000000000000000000 ) ) ;
#8630=DIRECTION ( 'NONE',  ( -1.000000000000000000, -0.000000000000000000, -0.000000000000000000 ) ) ;
#8637=DIRECTION ( 'NONE',  ( -1.000000000000000000, 0.000000000000000000, 0.000000000000000000 ) ) ;
#8649=ORIENTED_EDGE ( 'NONE', *, *, #6275, .T. ) ;
#8653=CARTESIAN_POINT ( 'NONE',  ( 2.601776144743014996, -23.64332819722373813, -10.68696068830432466 ) ) ;
#8657=CARTESIAN_POINT ( 'NONE',  ( 2.789999999999999147, -0.2301004812059262439, 24.44424927289185590 ) ) ;
#8658=CARTESIAN_POINT ( 'NONE',  ( 0.02436607992776368414, 18.55949924794916228, -16.37294372382838148 ) ) ;
#8662=ORIENTED_EDGE ( 'NONE', *, *, #10774, .F. ) ;
#8667=CARTESIAN_POINT ( 'NONE',  ( 2.789999999999999147, 15.74360496233408213, -18.28042085475260592 ) ) ;
#8678=ORIENTED_EDGE ( 'NONE', *, *, #47, .F. ) ;
#8680=EDGE_LOOP ( 'NONE', ( #13537, #12730, #7608, #8649 ) ) ;
#8685=AXIS2_PLACEMENT_3D ( 'NONE', #14861, #632, #14785 ) ;
#8686=AXIS2_PLACEMENT_3D ( 'NONE', #8108, #3419, #13001 ) ;
#8689=EDGE_CURVE ( 'NONE', #13319, #447, #8098, .T. ) ;
#8691=EDGE_CURVE ( 'NONE', #11975, #3303, #5652, .T. ) ;
#8694=CIRCLE ( 'NONE', #14608, 24.12539914357697413 ) ;
#8696=CYLINDRICAL_SURFACE ( 'NONE', #1574, 2.524999999999995914 ) ;
#8704=VERTEX_POINT ( 'NONE', #7874 ) ;
#8705=VERTEX_POINT ( 'NONE', #869 ) ;
#8706=CARTESIAN_POINT ( 'NONE',  ( -7.765813458258934317E-14, -24.22524813288764278, 2.133839912090720325 ) ) ;
#8710=CIRCLE ( 'NONE', #12394, 24.12539914357697768 ) ;
#8713=EDGE_CURVE ( 'NONE', #11370, #6946, #1096, .T. ) ;
#8716=B_SPLINE_CURVE_WITH_KNOTS ( 'NONE', 3,
 ( #7671, #7381, #1454, #5002, #9977, #11053 ),
 .UNSPECIFIED., .F., .F.,
 ( 4, 2, 4 ),
 ( 4.462636677693390501E-07, 0.001879885020955137558, 0.003759323778242505774 ),
 .UNSPECIFIED. ) ;
#8718=CARTESIAN_POINT ( 'NONE',  ( 2.789999999999999147, 0.000000000000000000, 0.000000000000000000 ) ) ;
#8719=CARTESIAN_POINT ( 'NONE',  ( 0.006931069955678950678, -18.43696893154746164, -16.17493693894899209 ) ) ;
#8721=CARTESIAN_POINT ( 'NONE',  ( 2.789999999999999147, -18.28042085475289369, 15.74360496233375173 ) ) ;
#8727=CARTESIAN_POINT ( 'NONE',  ( 1.749999999999998002, 25.12109765559653596, 12.52377138324232675 ) ) ;
#8728=DIRECTION ( 'NONE',  ( 0.000000000000000000, 0.000000000000000000, 1.000000000000000000 ) ) ;
#8729=CARTESIAN_POINT ( 'NONE',  ( 2.789999999999999147, -24.63872515616084513, 2.336989772644183283 ) ) ;
#8733=CIRCLE ( 'NONE', #9239, 4.000000000000000000 ) ;
#8739=FACE_OUTER_BOUND ( 'NONE', #13865, .T. ) ;
#8747=CIRCLE ( 'NONE', #7285, 28.06981291497571007 ) ;
#8748=EDGE_LOOP ( 'NONE', ( #3758, #7838, #6274, #9355, #11256, #14135 ) ) ;
#8754=EDGE_CURVE ( 'NONE', #10954, #13796, #3007, .T. ) ;
#8768=ORIENTED_EDGE ( 'NONE', *, *, #3200, .T. ) ;
#8769=DIRECTION ( 'NONE',  ( -1.000000000000000000, 0.000000000000000000, 0.000000000000000000 ) ) ;
#8771=CARTESIAN_POINT ( 'NONE',  ( 2.257825477245773982, 18.57583492944447556, -19.66801664102683489 ) ) ;
#8774=AXIS2_PLACEMENT_3D ( 'NONE', #3428, #4816, #10725 ) ;
#8775=EDGE_CURVE ( 'NONE', #368, #6042, #8710, .T. ) ;
#8776=AXIS2_PLACEMENT_3D ( 'NONE', #7912, #6755, #11432 ) ;
#8777=DIRECTION ( 'NONE',  ( -1.000000000000000000, -0.000000000000000000, -0.000000000000000000 ) ) ;
#8782=DIRECTION ( 'NONE',  ( 1.000000000000000000, 0.000000000000000000, 0.000000000000000000 ) ) ;
#8784=CARTESIAN_POINT ( 'NONE',  ( 2.789999999999999147, 20.70663861606293210, -12.51925356660738053 ) ) ;
#8785=DIRECTION ( 'NONE',  ( 0.000000000000000000, 0.000000000000000000, 1.000000000000000000 ) ) ;
#8789=ADVANCED_FACE ( 'NONE', ( #1246 ), #12140, .T. ) ;
#8791=ORIENTED_EDGE ( 'NONE', *, *, #1840, .F. ) ;
#8793=CARTESIAN_POINT ( 'NONE',  ( 1.749999999999998002, 0.000000000000000000, 0.000000000000000000 ) ) ;
#8795=CARTESIAN_POINT ( 'NONE',  ( 2.604434261026087771, 25.39738473785002526, 5.253342437939815923 ) ) ;
#8796=EDGE_CURVE ( 'NONE', #2082, #7850, #6092, .T. ) ;
#8798=CIRCLE ( 'NONE', #6844, 4.000000000000000000 ) ;
#8800=ORIENTED_EDGE ( 'NONE', *, *, #8120, .F. ) ;
#8801=CARTESIAN_POINT ( 'NONE',  ( 2.765633920072235519, 9.836394144776026138, -22.71065055754441531 ) ) ;
#8803=ORIENTED_EDGE ( 'NONE', *, *, #14955, .F. ) ;
#8818=ORIENTED_EDGE ( 'NONE', *, *, #9923, .T. ) ;
#8825=EDGE_CURVE ( 'NONE', #7330, #9808, #13120, .T. ) ;
#8828=VERTEX_POINT ( 'NONE', #3863 ) ;
#8829=ORIENTED_EDGE ( 'NONE', *, *, #5263, .T. ) ;
#8830=CARTESIAN_POINT ( 'NONE',  ( -5.209999999999999964, 0.000000000000000000, 0.000000000000000000 ) ) ;
#8833=CARTESIAN_POINT ( 'NONE',  ( 2.789999999999999147, 24.34211360614310848, -7.909232158574561744 ) ) ;
#8835=DIRECTION ( 'NONE',  ( 1.000000000000000000, 0.000000000000000000, 0.000000000000000000 ) ) ;
#8839=CARTESIAN_POINT ( 'NONE',  ( 2.789999999999999147, 0.000000000000000000, 0.000000000000000000 ) ) ;
#8841=ORIENTED_EDGE ( 'NONE', *, *, #711, .F. ) ;
#8845=ORIENTED_EDGE ( 'NONE', *, *, #2301, .T. ) ;
#8847=CARTESIAN_POINT ( 'NONE',  ( 2.789895169984651702, -20.67846228565646172, -12.51925356660783528 ) ) ;
#8848=UNCERTAINTY_MEASURE_WITH_UNIT (LENGTH_MEASURE( 1.000000000000000082E-05 ), #1546, 'distance_accuracy_value', 'NONE');
#8855=CARTESIAN_POINT ( 'NONE',  ( 0.02436607992776281678, 2.336989772644269436, 24.63872515616083447 ) ) ;
#8858=FACE_OUTER_BOUND ( 'NONE', #7073, .T. ) ;
#8869=CARTESIAN_POINT ( 'NONE',  ( 1.749999999999998002, 0.000000000000000000, 0.000000000000000000 ) ) ;
#8873=EDGE_CURVE ( 'NONE', #13815, #9813, #5954, .T. ) ;
#8878=ADVANCED_FACE ( 'NONE', ( #8380 ), #7091, .T. ) ;
#8881=CARTESIAN_POINT ( 'NONE',  ( 0.02436607992776585255, -5.391175441198789109, 24.15498966839961170 ) ) ;
#8882=CARTESIAN_POINT ( 'NONE',  ( -7.700916879387133607E-14, 12.51293083811828843, -20.85287692521917080 ) ) ;
#8886=CYLINDRICAL_SURFACE ( 'NONE', #1823, 13.19999999999999929 ) ;
#8888=EDGE_CURVE ( 'NONE', #5940, #14085, #11451, .T. ) ;
#8889=ORIENTED_EDGE ( 'NONE', *, *, #331, .T. ) ;
#8891=CIRCLE ( 'NONE', #11350, 2.524999999999996358 ) ;
#8892=CIRCLE ( 'NONE', #3009, 2.524999999999996358 ) ;
#8895=CARTESIAN_POINT ( 'NONE',  ( 2.789999999999999147, -24.15498966839958683, -5.391175441198872598 ) ) ;
#8898=DIRECTION ( 'NONE',  ( 0.000000000000000000, 0.000000000000000000, 1.000000000000000000 ) ) ;
#8901=CARTESIAN_POINT ( 'NONE',  ( -10.00000000000000000, 0.000000000000000000, 0.000000000000000000 ) ) ;
#8904=MANIFOLD_SOLID_BREP ( 'Bore', #7575 ) ;
#8905=CARTESIAN_POINT ( 'NONE',  ( 2.789999999999999147, 0.000000000000000000, 0.000000000000000000 ) ) ;
#8908=EDGE_CURVE ( 'NONE', #11392, #7854, #3323, .T. ) ;
#8909=CARTESIAN_POINT ( 'NONE',  ( 0.02436607992776411782, 22.71065055754465689, -9.836394144775473691 ) ) ;
#8912=ORIENTED_EDGE ( 'NONE', *, *, #1126, .T. ) ;
#8913=B_SPLINE_CURVE_WITH_KNOTS ( 'NONE', 3,
 ( #2650, #7344, #1492, #6176, #12314, #2094 ),
 .UNSPECIFIED., .F., .F.,
 ( 4, 2, 4 ),
 ( 4.462636732872785396E-07, 0.001879885066975069564, 0.003759323870276851630 ),
 .UNSPECIFIED. ) ;
#8915=B_SPLINE_CURVE_WITH_KNOTS ( 'NONE', 3,
 ( #10203, #6603, #11423, #3284 ),
 .UNSPECIFIED., .F., .F.,
 ( 4, 4 ),
 ( 3.059063720746924101E-07, 0.0006888942284913933487 ),
 .UNSPECIFIED. ) ;
#8921=VERTEX_POINT ( 'NONE', #6397 ) ;
#8923=LINE ( 'NONE', #4009, #6029 ) ;
#8924=DIRECTION ( 'NONE',  ( 0.000000000000000000, 0.000000000000000000, 1.000000000000000000 ) ) ;
#8930=VERTEX_POINT ( 'NONE', #2274 ) ;
#8931=CARTESIAN_POINT ( 'NONE',  ( 1.039999999999997593, -12.52377138324241557, 25.12109765559648977 ) ) ;
#8935=ORIENTED_EDGE ( 'NONE', *, *, #10029, .T. ) ;
#8943=AXIS2_PLACEMENT_3D ( 'NONE', #11294, #5468, #1698 ) ;
#8946=CARTESIAN_POINT ( 'NONE',  ( 2.790000000000000924, 0.000000000000000000, 0.000000000000000000 ) ) ;
#8947=B_SPLINE_CURVE_WITH_KNOTS ( 'NONE', 3,
 ( #11126, #13592, #9766, #6453 ),
 .UNSPECIFIED., .F., .F.,
 ( 4, 4 ),
 ( 1.981826382900849143E-07, 0.0006887856082032012620 ),
 .UNSPECIFIED. ) ;
#8950=DIRECTION ( 'NONE',  ( 1.000000000000000000, 0.000000000000000000, 0.000000000000000000 ) ) ;
#8951=ORIENTED_EDGE ( 'NONE', *, *, #10388, .T. ) ;
#8956=CIRCLE ( 'NONE', #14862, 28.06981291497571007 ) ;
#8961=DIRECTION ( 'NONE',  ( -1.000000000000000000, -0.000000000000000000, -0.000000000000000000 ) ) ;
#8964=EDGE_CURVE ( 'NONE', #9957, #9499, #8956, .T. ) ;
#8968=ORIENTED_EDGE ( 'NONE', *, *, #2802, .F. ) ;
#8974=CARTESIAN_POINT ( 'NONE',  ( 2.765633920072235963, -16.37294372382871188, 18.55949924794887096 ) ) ;
#8975=EDGE_LOOP ( 'NONE', ( #3608, #10967, #4297, #6756, #6861, #10652 ) ) ;
#8976=CARTESIAN_POINT ( 'NONE',  ( 2.789999999999999147, 5.535312321042718864, 23.48180575137732262 ) ) ;
#8977=CARTESIAN_POINT ( 'NONE',  ( 0.02436607992776411782, -16.37294372382844543, -18.55949924794910544 ) ) ;
#8978=ORIENTED_EDGE ( 'NONE', *, *, #12161, .T. ) ;
#8979=ORIENTED_EDGE ( 'NONE', *, *, #14455, .F. ) ;
#8980=CARTESIAN_POINT ( 'NONE',  ( 2.765633920072242624, -22.71065055754459650, 9.836394144775621129 ) ) ;
#8981=AXIS2_PLACEMENT_3D ( 'NONE', #595, #5233, #11058 ) ;
#8983=EDGE_CURVE ( 'NONE', #11249, #5438, #14012, .T. ) ;
#8984=DIRECTION ( 'NONE',  ( 0.000000000000000000, 0.000000000000000000, -1.000000000000000000 ) ) ;
#8986=DIRECTION ( 'NONE',  ( 0.000000000000000000, 0.9510565162951498674, 0.3090169943749583870 ) ) ;
#8989=EDGE_LOOP ( 'NONE', ( #4467, #235, #7765, #12102, #5654, #3892 ) ) ;
#8995=ORIENTED_EDGE ( 'NONE', *, *, #9107, .F. ) ;
#9004=EDGE_CURVE ( 'NONE', #6879, #12150, #8798, .T. ) ;
#9008=DIRECTION ( 'NONE',  ( -1.000000000000000000, -0.000000000000000000, -0.000000000000000000 ) ) ;
#9011=DIRECTION ( 'NONE',  ( 0.000000000000000000, 0.000000000000000000, 1.000000000000000000 ) ) ;
#9012=CARTESIAN_POINT ( 'NONE',  ( 2.789999999999999147, -23.48180575137726223, -5.535312321042966666 ) ) ;
#9017=EDGE_CURVE ( 'NONE', #12081, #389, #11267, .T. ) ;
#9018=AXIS2_PLACEMENT_3D ( 'NONE', #1062, #6976, #5756 ) ;
#9024=CIRCLE ( 'NONE', #8776, 28.06981291497571007 ) ;
#9025=ORIENTED_EDGE ( 'NONE', *, *, #14570, .F. ) ;
#9027=AXIS2_PLACEMENT_3D ( 'NONE', #8946, #12327, #13637 ) ;
#9028=DIRECTION ( 'NONE',  ( 0.000000000000000000, 0.000000000000000000, -1.000000000000000000 ) ) ;
#9032=CARTESIAN_POINT ( 'NONE',  ( 2.789999999999999147, -0.2301004812055740811, -24.44424927289185590 ) ) ;
#9034=CARTESIAN_POINT ( 'NONE',  ( 2.789999999999999147, -5.391175441198450713, -24.15498966839968276 ) ) ;
#9041=DIRECTION ( 'NONE',  ( 0.000000000000000000, 5.496153587253259026E-15, -1.000000000000000000 ) ) ;
#9043=ORIENTED_EDGE ( 'NONE', *, *, #4399, .T. ) ;
#9053=CARTESIAN_POINT ( 'NONE',  ( 0.5279273620711150139, 23.73240184472514613, -12.96450951081191150 ) ) ;
#9056=CARTESIAN_POINT ( 'NONE',  ( 2.765633920072239516, -24.63872515616084513, 2.336989772644183283 ) ) ;
#9058=CARTESIAN_POINT ( 'NONE',  ( 2.789999999999999147, -24.34211360614294506, -7.909232158575071558 ) ) ;
#9059=ORIENTED_EDGE ( 'NONE', *, *, #10617, .F. ) ;
#9060=AXIS2_PLACEMENT_3D ( 'NONE', #4681, #4909, #2213 ) ;
#9061=CIRCLE ( 'NONE', #9027, 4.000000000000000000 ) ;
#9062=CIRCLE ( 'NONE', #2433, 2.524999999999996803 ) ;
#9064=CARTESIAN_POINT ( 'NONE',  ( 2.790000000000077751, 5.456611084821854085, 23.69897269326679279 ) ) ;
#9065=CARTESIAN_POINT ( 'NONE',  ( 2.789999999999999147, -24.44424927289185590, 0.2301004812056573479 ) ) ;
#9067=VERTEX_POINT ( 'NONE', #3245 ) ;
#9073=DIRECTION ( 'NONE',  ( -1.000000000000000000, -0.000000000000000000, -0.000000000000000000 ) ) ;
#9074=CARTESIAN_POINT ( 'NONE',  ( 0.7592463834391194322, -24.80264696524891477, 12.05220173035428921 ) ) ;
#9075=CARTESIAN_POINT ( 'NONE',  ( 0.7589665349472715095, 27.14933624560914893, -4.828387785247743480 ) ) ;
#9076=AXIS2_PLACEMENT_3D ( 'NONE', #1847, #13680, #11297 ) ;
#9078=DIRECTION ( 'NONE',  ( -1.000000000000000000, -0.000000000000000000, -0.000000000000000000 ) ) ;
#9083=EDGE_LOOP ( 'NONE', ( #13071, #12688, #5955, #8818 ) ) ;
#9089=CARTESIAN_POINT ( 'NONE',  ( 2.718131853594929037, -12.74240566898999383, 21.92302674874958868 ) ) ;
#9098=CARTESIAN_POINT ( 'NONE',  ( 1.039999999999996483, 4.147968289691283950, 27.76164181293052735 ) ) ;
#9100=CARTESIAN_POINT ( 'NONE',  ( 0.1855657389739094887, -5.253342437939553022, -25.39738473785006079 ) ) ;
#9105=CARTESIAN_POINT ( 'NONE',  ( 2.789999999999999147, -7.909232158574647009, -24.34211360614308006 ) ) ;
#9106=EDGE_CURVE ( 'NONE', #2082, #9825, #14209, .T. ) ;
#9107=EDGE_CURVE ( 'NONE', #10848, #860, #7969, .T. ) ;
#9108=ORIENTED_EDGE ( 'NONE', *, *, #12489, .T. ) ;
#9111=EDGE_CURVE ( 'NONE', #4155, #13280, #217, .T. ) ;
#9112=CARTESIAN_POINT ( 'NONE',  ( 2.718184767880471142, 10.24584646439571500, -23.19431517146922417 ) ) ;
#9113=DIRECTION ( 'NONE',  ( -1.000000000000000000, -0.000000000000000000, -0.000000000000000000 ) ) ;
#9117=VERTEX_POINT ( 'NONE', #3611 ) ;
#9118=B_SPLINE_CURVE_WITH_KNOTS ( 'NONE', 3,
 ( #12365, #9074, #10299, #3162, #6762, #11217 ),
 .UNSPECIFIED., .F., .F.,
 ( 4, 2, 4 ),
 ( 4.462636882236601199E-07, 0.001879885203074806947, 0.003759324142461389993 ),
 .UNSPECIFIED. ) ;
#9120=EDGE_LOOP ( 'NONE', ( #5855, #537, #12303, #11355 ) ) ;
#9122=FACE_OUTER_BOUND ( 'NONE', #13584, .T. ) ;
#9123=CARTESIAN_POINT ( 'NONE',  ( 1.749999999999998002, 4.633866840649310426, -27.68468304288254345 ) ) ;
#9124=CARTESIAN_POINT ( 'NONE',  ( 0.7592463977762147209, -4.828194074574546413, 27.14986936243572657 ) ) ;
#9127=FACE_OUTER_BOUND ( 'NONE', #10061, .T. ) ;
#9130=CARTESIAN_POINT ( 'NONE',  ( 2.789999999999999147, 15.04425356660760293, 20.70663861606276868 ) ) ;
#9137=ORIENTED_EDGE ( 'NONE', *, *, #8825, .T. ) ;
#9139=CARTESIAN_POINT ( 'NONE',  ( 2.718131864678290821, 25.22589920183360945, -2.577209017047097372 ) ) ;
#9140=ORIENTED_EDGE ( 'NONE', *, *, #6102, .T. ) ;
#9141=CARTESIAN_POINT ( 'NONE',  ( 2.790000000000078639, 15.96555658743789152, -18.34439787333489136 ) ) ;
#9145=CARTESIAN_POINT ( 'NONE',  ( 0.5321745087963410947, 24.44564404695860205, -11.58891744060082019 ) ) ;
#9150=ADVANCED_FACE ( 'NONE', ( #5930 ), #4618, .T. ) ;
#9153=ORIENTED_EDGE ( 'NONE', *, *, #14930, .F. ) ;
#9154=EDGE_LOOP ( 'NONE', ( #4471, #5505, #4706, #6629 ) ) ;
#9155=EDGE_LOOP ( 'NONE', ( #14224, #9651, #1458, #13482 ) ) ;
#9159=EDGE_CURVE ( 'NONE', #860, #5525, #1741, .T. ) ;
#9163=CARTESIAN_POINT ( 'NONE',  ( 2.783068888626318405, 9.685942809247050533, 22.53293026234507579 ) ) ;
#9169=CARTESIAN_POINT ( 'NONE',  ( 2.789999999999999147, 15.04425356660790136, -18.18163861606255338 ) ) ;
#9170=ORIENTED_EDGE ( 'NONE', *, *, #9649, .T. ) ;
#9171=ORIENTED_EDGE ( 'NONE', *, *, #12489, .F. ) ;
#9174=CARTESIAN_POINT ( 'NONE',  ( -10.00000000000000000, 0.000000000000000000, 0.000000000000000000 ) ) ;
#9177=CARTESIAN_POINT ( 'NONE',  ( 2.031033479673592268, -19.86422722021325882, 19.12621924769859660 ) ) ;
#9178=CARTESIAN_POINT ( 'NONE',  ( 0.1882238552569852619, 10.68696068830407420, 23.64332819722385182 ) ) ;
#9191=FACE_OUTER_BOUND ( 'NONE', #9155, .T. ) ;
#9193=EDGE_CURVE ( 'NONE', #7336, #14793, #6076, .T. ) ;
#9198=DIRECTION ( 'NONE',  ( 0.000000000000000000, 0.000000000000000000, 1.000000000000000000 ) ) ;
#9204=VECTOR ( 'NONE', #12423, 1000.000000000000000 ) ;
#9205=CARTESIAN_POINT ( 'NONE',  ( 2.789999999999999147, 20.70663861606293210, -15.04425356660737556 ) ) ;
#9206=AXIS2_PLACEMENT_3D ( 'NONE', #12997, #7098, #9470 ) ;
#9207=ORIENTED_EDGE ( 'NONE', *, *, #15037, .T. ) ;
#9208=CIRCLE ( 'NONE', #346, 2.524999999999997247 ) ;
#9223=CARTESIAN_POINT ( 'NONE',  ( 2.724374482943360487, 21.84204283372364230, 12.72258903105646688 ) ) ;
#9226=CARTESIAN_POINT ( 'NONE',  ( 2.789999999999999147, 23.48180575137730131, 5.535312321042802353 ) ) ;
#9230=ORIENTED_EDGE ( 'NONE', *, *, #13267, .T. ) ;
#9234=PLANE ( 'NONE',  #2170 ) ;
#9235=DIRECTION ( 'NONE',  ( 0.000000000000000000, 0.000000000000000000, 1.000000000000000000 ) ) ;
#9239=AXIS2_PLACEMENT_3D ( 'NONE', #3149, #1994, #14827 ) ;
#9241=CARTESIAN_POINT ( 'NONE',  ( 2.765633920072242624, 9.836394144775706394, 22.71065055754456097 ) ) ;
#9247=ORIENTED_EDGE ( 'NONE', *, *, #47, .T. ) ;
#9255=CARTESIAN_POINT ( 'NONE',  ( 1.039999999999997593, 0.000000000000000000, 0.000000000000000000 ) ) ;
#9256=ORIENTED_EDGE ( 'NONE', *, *, #13839, .F. ) ;
#9260=CARTESIAN_POINT ( 'NONE',  ( 0.001865824574860882289, 20.90825775245787455, -12.51925356660738053 ) ) ;
#9263=ORIENTED_EDGE ( 'NONE', *, *, #8360, .F. ) ;
#9264=AXIS2_PLACEMENT_3D ( 'NONE', #12643, #887, #3276 ) ;
#9269=ORIENTED_EDGE ( 'NONE', *, *, #7138, .F. ) ;
#9271=DIRECTION ( 'NONE',  ( 0.000000000000000000, 1.374038396813314756E-15, -1.000000000000000000 ) ) ;
#9273=AXIS2_PLACEMENT_3D ( 'NONE', #14121, #4831, #3587 ) ;
#9274=DIRECTION ( 'NONE',  ( 0.000000000000000000, 0.000000000000000000, 1.000000000000000000 ) ) ;
#9275=CARTESIAN_POINT ( 'NONE',  ( 2.789999999999999147, 24.15498966839963302, 5.391175441198700291 ) ) ;
#9277=CIRCLE ( 'NONE', #13932, 28.06981291497571362 ) ;
#9279=AXIS2_PLACEMENT_3D ( 'NONE', #810, #11341, #15041 ) ;
#9286=CARTESIAN_POINT ( 'NONE',  ( 0.02436607992775978102, 16.37294372382885044, -18.55949924794875017 ) ) ;
#9289=ORIENTED_EDGE ( 'NONE', *, *, #8292, .T. ) ;
#9292=ORIENTED_EDGE ( 'NONE', *, *, #2254, .T. ) ;
#9299=CARTESIAN_POINT ( 'NONE',  ( 2.789999999999999147, 15.74360496233408213, -18.28042085475260592 ) ) ;
#9300=DIRECTION ( 'NONE',  ( 0.000000000000000000, 0.000000000000000000, 1.000000000000000000 ) ) ;
#9307=CARTESIAN_POINT ( 'NONE',  ( 0.000000000000000000, -12.52067188844335988, -20.62201879784928238 ) ) ;
#9309=CARTESIAN_POINT ( 'NONE',  ( 2.789999999999999147, 0.000000000000000000, 0.000000000000000000 ) ) ;
#9310=EDGE_CURVE ( 'NONE', #14933, #15005, #4158, .T. ) ;
#9311=ORIENTED_EDGE ( 'NONE', *, *, #4419, .T. ) ;
#9316=CARTESIAN_POINT ( 'NONE',  ( 1.749999999999998002, -12.52377138324241734, 25.12109765559649688 ) ) ;
#9317=DIRECTION ( 'NONE',  ( -1.000000000000000000, -0.000000000000000000, -0.000000000000000000 ) ) ;
#9318=EDGE_CURVE ( 'NONE', #13854, #552, #11988, .T. ) ;
#9321=CARTESIAN_POINT ( 'NONE',  ( 0.5279273746168620107, 4.996265754456365116, 26.57710921259763026 ) ) ;
#9323=CARTESIAN_POINT ( 'NONE',  ( 1.039999999999996483, -27.76164181293054511, 4.147968289691193355 ) ) ;
#9324=AXIS2_PLACEMENT_3D ( 'NONE', #3, #5785, #1388 ) ;
#9333=ORIENTED_EDGE ( 'NONE', *, *, #13267, .F. ) ;
#9335=CARTESIAN_POINT ( 'NONE',  ( -7.728448779411724935E-14, -2.133839912090635949, -24.22524813288764989 ) ) ;
#9340=DIRECTION ( 'NONE',  ( 0.000000000000000000, 0.000000000000000000, 1.000000000000000000 ) ) ;
#9342=ORIENTED_EDGE ( 'NONE', *, *, #12554, .F. ) ;
#9345=CARTESIAN_POINT ( 'NONE',  ( 2.783025228907523019, 9.686319561461266048, -22.53337530003393141 ) ) ;
#9346=FACE_OUTER_BOUND ( 'NONE', #12854, .T. ) ;
#9348=CARTESIAN_POINT ( 'NONE',  ( 2.765633920072239516, -24.63872515616084513, 2.336989772644183283 ) ) ;
#9351=CYLINDRICAL_SURFACE ( 'NONE', #698, 13.20000000000000284 ) ;
#9352=DIRECTION ( 'NONE',  ( -1.000000000000000000, 0.000000000000000000, 0.000000000000000000 ) ) ;
#9354=CARTESIAN_POINT ( 'NONE',  ( 2.765633920072235963, 22.71065055754452544, 9.836394144775786330 ) ) ;
#9355=ORIENTED_EDGE ( 'NONE', *, *, #15037, .F. ) ;
#9359=FACE_OUTER_BOUND ( 'NONE', #8361, .T. ) ;
#9366=CARTESIAN_POINT ( 'NONE',  ( 0.07186813532171117125, -25.22589920183359169, -2.577209017047271011 ) ) ;
#9368=ORIENTED_EDGE ( 'NONE', *, *, #9615, .T. ) ;
#9371=ORIENTED_EDGE ( 'NONE', *, *, #10049, .F. ) ;
#9372=VERTEX_POINT ( 'NONE', #8063 ) ;
#9376=EDGE_CURVE ( 'NONE', #10254, #14234, #12542, .T. ) ;
#9380=EDGE_CURVE ( 'NONE', #4433, #8382, #5538, .T. ) ;
#9389=CARTESIAN_POINT ( 'NONE',  ( 0.07181525696555274285, -24.78695292654917637, -5.344212458769628249 ) ) ;
#9390=ORIENTED_EDGE ( 'NONE', *, *, #3929, .T. ) ;
#9391=VERTEX_POINT ( 'NONE', #12738 ) ;
#9394=ORIENTED_EDGE ( 'NONE', *, *, #14137, .F. ) ;
#9395=DIRECTION ( 'NONE',  ( -1.000000000000000000, 0.000000000000000000, 0.000000000000000000 ) ) ;
#9408=CARTESIAN_POINT ( 'NONE',  ( 0.006931038682727013421, -21.08061549536624568, 12.53626894672821201 ) ) ;
#9412=ORIENTED_EDGE ( 'NONE', *, *, #8615, .F. ) ;
#9413=CARTESIAN_POINT ( 'NONE',  ( 1.039999999999995817, -27.76164181293048472, -4.147968289691575272 ) ) ;
#9414=AXIS2_PLACEMENT_3D ( 'NONE', #12113, #2909, #11116 ) ;
#9416=CARTESIAN_POINT ( 'NONE',  ( 0.5321745227542249435, 18.57583492944418779, 19.66801664102709779 ) ) ;
#9418=ORIENTED_EDGE ( 'NONE', *, *, #4306, .F. ) ;
#9422=CARTESIAN_POINT ( 'NONE',  ( 0.7589665283900991488, 27.31260702007175567, 3.797536611356412628 ) ) ;
#9428=ADVANCED_FACE ( 'NONE', ( #764 ), #12446, .T. ) ;
#9434=VECTOR ( 'NONE', #2391, 1000.000000000000000 ) ;
#9437=CARTESIAN_POINT ( 'NONE',  ( 1.039999999999996705, -20.02152543075331081, -19.67366047555552555 ) ) ;
#9447=VERTEX_POINT ( 'NONE', #13673 ) ;
#9454=CARTESIAN_POINT ( 'NONE',  ( 1.039999999999995817, 4.633866840648921404, 27.68468304288260029 ) ) ;
#9455=ORIENTED_EDGE ( 'NONE', *, *, #7976, .T. ) ;
#9456=FACE_OUTER_BOUND ( 'NONE', #13977, .T. ) ;
#9470=DIRECTION ( 'NONE',  ( 0.000000000000000000, 0.000000000000000000, 1.000000000000000000 ) ) ;
#9471=CARTESIAN_POINT ( 'NONE',  ( 1.394999999999998685, 20.02152543075374425, -19.67366047555508857 ) ) ;
#9472=EDGE_CURVE ( 'NONE', #11571, #9661, #9024, .T. ) ;
#9473=EDGE_CURVE ( 'NONE', #10254, #11686, #909, .T. ) ;
#9475=CIRCLE ( 'NONE', #11923, 28.06981291497571007 ) ;
#9479=CARTESIAN_POINT ( 'NONE',  ( 1.749999999999998002, 0.000000000000000000, 0.000000000000000000 ) ) ;
#9481=B_SPLINE_CURVE_WITH_KNOTS ( 'NONE', 3,
 ( #10267, #11265, #4274, #803, #3205, #15034 ),
 .UNSPECIFIED., .F., .F.,
 ( 4, 2, 4 ),
 ( 4.462636695652347161E-07, 0.001879885036799764601, 0.003759323809929963987 ),
 .UNSPECIFIED. ) ;
#9482=B_SPLINE_CURVE_WITH_KNOTS ( 'NONE', 3,
 ( #11020, #9864, #9799, #14640 ),
 .UNSPECIFIED., .F., .F.,
 ( 4, 4 ),
 ( 0.005258139959819246867, 0.005948405594583413246 ),
 .UNSPECIFIED. ) ;
#9483=CARTESIAN_POINT ( 'NONE',  ( 1.394999999999999574, 12.96210679857786552, 24.89775460606837143 ) ) ;
#9484=COLOUR_RGB ( '',1.000000000000000000, 0.9490196078431372140, 0.9098039215686274384 ) ;
#9486=ORIENTED_EDGE ( 'NONE', *, *, #8052, .F. ) ;
#9492=CARTESIAN_POINT ( 'NONE',  ( 2.765633920072235519, 9.836394144776026138, -22.71065055754441531 ) ) ;
#9499=VERTEX_POINT ( 'NONE', #14333 ) ;
#9506=ORIENTED_EDGE ( 'NONE', *, *, #13431, .T. ) ;
#9508=ORIENTED_EDGE ( 'NONE', *, *, #12061, .T. ) ;
#9514=DIRECTION ( 'NONE',  ( 0.000000000000000000, 0.8090169943749527803, -0.5877852522924655876 ) ) ;
#9518=CARTESIAN_POINT ( 'NONE',  ( 1.039999999999997371, -4.147968289691092991, -27.76164181293055933 ) ) ;
#9520=ORIENTED_EDGE ( 'NONE', *, *, #12220, .T. ) ;
#9528=EDGE_LOOP ( 'NONE', ( #14033, #6067, #3335, #7744, #6924, #10864 ) ) ;
#9531=CARTESIAN_POINT ( 'NONE',  ( 2.789999999999999147, -21.30679549418621832, -12.59161484032935618 ) ) ;
#9533=CARTESIAN_POINT ( 'NONE',  ( 0.000000000000000000, 0.000000000000000000, 0.000000000000000000 ) ) ;
#9534=CARTESIAN_POINT ( 'NONE',  ( 1.394999999999999574, -25.12109765559663188, 12.52377138324214378 ) ) ;
#9540=B_SPLINE_CURVE_WITH_KNOTS ( 'NONE', 3,
 ( #8607, #9990, #601, #10142, #11215, #689 ),
 .UNSPECIFIED., .F., .F.,
 ( 4, 2, 4 ),
 ( 4.462636732861906317E-07, 0.001879885066975067178, 0.003759323870276848160 ),
 .UNSPECIFIED. ) ;
#9542=TOROIDAL_SURFACE ( 'NONE', #3902, 24.12539914357697413, 8.000000000000000000 ) ;
#9543=ORIENTED_EDGE ( 'NONE', *, *, #13952, .F. ) ;
#9545=CARTESIAN_POINT ( 'NONE',  ( 2.718131853594931258, -21.92302674874953539, -12.74240566899008442 ) ) ;
#9546=CARTESIAN_POINT ( 'NONE',  ( 2.030753616560879493, 24.80264696524883306, 12.05220173035447750 ) ) ;
#9551=EDGE_CURVE ( 'NONE', #4420, #6027, #3339, .T. ) ;
#9557=DIRECTION ( 'NONE',  ( -1.000000000000000000, 0.000000000000000000, -0.000000000000000000 ) ) ;
#9561=DIRECTION ( 'NONE',  ( 0.000000000000000000, 0.000000000000000000, 1.000000000000000000 ) ) ;
#9562=ORIENTED_EDGE ( 'NONE', *, *, #7788, .T. ) ;
#9563=CARTESIAN_POINT ( 'NONE',  ( 2.789999999999999591, -24.22479935914660487, 2.133490293296927742 ) ) ;
#9566=EDGE_CURVE ( 'NONE', #9867, #3792, #3689, .T. ) ;
#9568=VECTOR ( 'NONE', #10891, 1000.000000000000000 ) ;
#9569=LINE ( 'NONE', #13080, #11485 ) ;
#9572=DIRECTION ( 'NONE',  ( -1.000000000000000000, -0.000000000000000000, -0.000000000000000000 ) ) ;
#9573=DIRECTION ( 'NONE',  ( 0.000000000000000000, 0.000000000000000000, 1.000000000000000000 ) ) ;
#9575=B_SPLINE_CURVE_WITH_KNOTS ( 'NONE', 3,
 ( #696, #9996, #379, #7690 ),
 .UNSPECIFIED., .F., .F.,
 ( 4, 4 ),
 ( 3.059063720746923042E-07, 0.0006888942284913959508 ),
 .UNSPECIFIED. ) ;
#9576=CARTESIAN_POINT ( 'NONE',  ( 0.009102498987474663336, -21.10878525316950771, -12.54316204260915768 ) ) ;
#9578=CARTESIAN_POINT ( 'NONE',  ( 2.601776121706763423, 19.18368891937490517, 17.47009390565497711 ) ) ;
#9581=CARTESIAN_POINT ( 'NONE',  ( 2.765633920072236407, -2.336989772644440855, 24.63872515616082026 ) ) ;
#9584=ORIENTED_EDGE ( 'NONE', *, *, #13206, .T. ) ;
#9585=ORIENTED_EDGE ( 'NONE', *, *, #12009, .F. ) ;
#9589=FACE_OUTER_BOUND ( 'NONE', #10114, .T. ) ;
#9594=DIRECTION ( 'NONE',  ( 0.000000000000000000, 0.000000000000000000, 1.000000000000000000 ) ) ;
#9603=CARTESIAN_POINT ( 'NONE',  ( 0.006974674093432167536, 2.249040938978497994, 24.42374957165206695 ) ) ;
#9604=DIRECTION ( 'NONE',  ( 1.000000000000000000, 0.000000000000000000, -0.000000000000000000 ) ) ;
#9608=DIRECTION ( 'NONE',  ( -1.000000000000000000, -0.000000000000000000, 0.000000000000000000 ) ) ;
#9611=CARTESIAN_POINT ( 'NONE',  ( 2.789999999999999147, 19.91106274590514147, 14.18181402625749676 ) ) ;
#9615=EDGE_CURVE ( 'NONE', #15073, #13780, #12931, .T. ) ;
#9618=ORIENTED_EDGE ( 'NONE', *, *, #12801, .F. ) ;
#9624=FACE_OUTER_BOUND ( 'NONE', #133, .T. ) ;
#9626=CARTESIAN_POINT ( 'NONE',  ( 2.789999999999999147, -7.909232158574647009, -21.81711360614308148 ) ) ;
#9627=CARTESIAN_POINT ( 'NONE',  ( 1.039999999999996261, 24.89775460606850999, -12.96210679857759018 ) ) ;
#9628=DIRECTION ( 'NONE',  ( -1.000000000000000000, -0.000000000000000000, -0.000000000000000000 ) ) ;
#9629=VERTEX_POINT ( 'NONE', #3669 ) ;
#9635=ADVANCED_FACE ( 'NONE', ( #7594 ), #4629, .T. ) ;
#9639=CARTESIAN_POINT ( 'NONE',  ( 2.789999999999999147, -9.324097380959603498, 22.25075486061734864 ) ) ;
#9640=DIRECTION ( 'NONE',  ( 1.000000000000000000, 0.000000000000000000, 0.000000000000000000 ) ) ;
#9644=ORIENTED_EDGE ( 'NONE', *, *, #520, .F. ) ;
#9647=CARTESIAN_POINT ( 'NONE',  ( 0.000000000000000000, -18.28042085475266632, -15.74360496233403239 ) ) ;
#9649=EDGE_CURVE ( 'NONE', #12104, #9763, #12106, .T. ) ;
#9651=ORIENTED_EDGE ( 'NONE', *, *, #5364, .T. ) ;
#9652=EDGE_CURVE ( 'NONE', #13720, #1158, #1315, .T. ) ;
#9655=LINE ( 'NONE', #9737, #11468 ) ;
#9656=CARTESIAN_POINT ( 'NONE',  ( 1.749999999999998002, 0.000000000000000000, 0.000000000000000000 ) ) ;
#9657=DIRECTION ( 'NONE',  ( 0.000000000000000000, 0.000000000000000000, -1.000000000000000000 ) ) ;
#9658=CARTESIAN_POINT ( 'NONE',  ( 1.039999999999997149, -27.68468304288261805, 4.633866840648821039 ) ) ;
#9660=CARTESIAN_POINT ( 'NONE',  ( 1.749999999999998002, 12.96210679857786552, 24.89775460606837143 ) ) ;
#9661=VERTEX_POINT ( 'NONE', #573 ) ;
#9662=CARTESIAN_POINT ( 'NONE',  ( 0.7589665203264086557, -19.86422722021297815, -19.12621924769889148 ) ) ;
#9663=CYLINDRICAL_SURFACE ( 'NONE', #7220, 2.524999999999995914 ) ;
#9665=CARTESIAN_POINT ( 'NONE',  ( 1.394999999999999574, 27.76164181293051669, -4.147968289691385202 ) ) ;
#9671=CIRCLE ( 'NONE', #12120, 24.12539914357697413 ) ;
#9673=B_SPLINE_CURVE_WITH_KNOTS ( 'NONE', 3,
 ( #12263, #3809, #13185, #2810 ),
 .UNSPECIFIED., .F., .F.,
 ( 4, 4 ),
 ( 3.059063720795842371E-07, 0.0006888942284914355242 ),
 .UNSPECIFIED. ) ;
#9674=B_SPLINE_CURVE_WITH_KNOTS ( 'NONE', 3,
 ( #12584, #12734, #13817, #3289, #10063, #11427 ),
 .UNSPECIFIED., .F., .F.,
 ( 4, 2, 4 ),
 ( 1.979325885420663486E-07, 0.001878588715165612974, 0.003756979497742683576 ),
 .UNSPECIFIED. ) ;
#9677=ORIENTED_EDGE ( 'NONE', *, *, #11225, .T. ) ;
#9680=CARTESIAN_POINT ( 'NONE',  ( 2.030753602223782206, -27.14986936243577986, 4.828194074574245320 ) ) ;
#9681=B_SPLINE_CURVE_WITH_KNOTS ( 'NONE', 3,
 ( #5078, #6215, #3915, #2756 ),
 .UNSPECIFIED., .F., .F.,
 ( 4, 4 ),
 ( 0.005258105385878709091, 0.005948373736081389272 ),
 .UNSPECIFIED. ) ;
#9694=TOROIDAL_SURFACE ( 'NONE', #5530, 24.12539914357697768, 8.000000000000000000 ) ;
#9699=CARTESIAN_POINT ( 'NONE',  ( 1.749999999999998002, 25.12109765559653596, 12.52377138324232675 ) ) ;
#9700=EDGE_CURVE ( 'NONE', #13976, #2534, #5602, .T. ) ;
#9701=ORIENTED_EDGE ( 'NONE', *, *, #11745, .T. ) ;
#9704=ORIENTED_EDGE ( 'NONE', *, *, #14809, .F. ) ;
#9708=ADVANCED_FACE ( 'NONE', ( #4137 ), #1919, .T. ) ;
#9710=ORIENTED_EDGE ( 'NONE', *, *, #2884, .T. ) ;
#9711=CARTESIAN_POINT ( 'NONE',  ( 0.7589665283900990378, 3.797536611356696845, -27.31260702007171304 ) ) ;
#9712=EDGE_CURVE ( 'NONE', #3345, #2360, #6826, .T. ) ;
#9716=TOROIDAL_SURFACE ( 'NONE', #11670, 24.12539914357697413, 8.000000000000000000 ) ;
#9720=CARTESIAN_POINT ( 'NONE',  ( 2.790000000000077307, -9.515416771311352662, 22.38018801136472646 ) ) ;
#9724=CIRCLE ( 'NONE', #2606, 2.524999999999995914 ) ;
#9725=DIRECTION ( 'NONE',  ( -1.000000000000000000, -0.000000000000000000, -0.000000000000000000 ) ) ;
#9726=EDGE_LOOP ( 'NONE', ( #13992, #13377, #7293, #106, #4558, #1262 ) ) ;
#9729=DIRECTION ( 'NONE',  ( 1.000000000000000000, 0.000000000000000000, 0.000000000000000000 ) ) ;
#9730=CARTESIAN_POINT ( 'NONE',  ( 0.000000000000000000, 24.34211360614300190, 7.909232158574900140 ) ) ;
#9732=ORIENTED_EDGE ( 'NONE', *, *, #12360, .T. ) ;
#9737=CARTESIAN_POINT ( 'NONE',  ( 1.394999999999998685, 25.12109765559653596, 12.52377138324232675 ) ) ;
#9743=CIRCLE ( 'NONE', #3605, 4.000000000000000000 ) ;
#9747=DIRECTION ( 'NONE',  ( 0.000000000000000000, 0.000000000000000000, 1.000000000000000000 ) ) ;
#9750=ORIENTED_EDGE ( 'NONE', *, *, #8360, .T. ) ;
#9752=AXIS2_PLACEMENT_3D ( 'NONE', #10109, #4203, #4352 ) ;
#9763=VERTEX_POINT ( 'NONE', #12190 ) ;
#9764=CARTESIAN_POINT ( 'NONE',  ( 2.765633920072241736, -9.836394144775550075, -22.71065055754462492 ) ) ;
#9766=CARTESIAN_POINT ( 'NONE',  ( -7.646929282184496191E-14, 5.456611084822186264, -23.69897269326672884 ) ) ;
#9773=ADVANCED_FACE ( 'NONE', ( #6427 ), #11110, .T. ) ;
#9774=VERTEX_POINT ( 'NONE', #12419 ) ;
#9783=ORIENTED_EDGE ( 'NONE', *, *, #10498, .T. ) ;
#9785=AXIS2_PLACEMENT_3D ( 'NONE', #5285, #10948, #14506 ) ;
#9787=CARTESIAN_POINT ( 'NONE',  ( 1.394999999999998685, -4.147968289691093879, -27.76164181293055933 ) ) ;
#9791=CARTESIAN_POINT ( 'NONE',  ( 2.789999999999999147, -22.25075486061744812, 9.324097380959361914 ) ) ;
#9793=AXIS2_PLACEMENT_3D ( 'NONE', #1507, #10951, #6196 ) ;
#9797=CARTESIAN_POINT ( 'NONE',  ( 1.039999999999997593, 0.000000000000000000, 0.000000000000000000 ) ) ;
#9799=CARTESIAN_POINT ( 'NONE',  ( 0.006931038682726457442, 12.53626894672828485, 21.08061549536619950 ) ) ;
#9801=ORIENTED_EDGE ( 'NONE', *, *, #13027, .T. ) ;
#9807=CARTESIAN_POINT ( 'NONE',  ( -5.209999999999999964, 0.000000000000000000, 0.000000000000000000 ) ) ;
#9808=VERTEX_POINT ( 'NONE', #886 ) ;
#9811=CARTESIAN_POINT ( 'NONE',  ( 2.789999999999999147, -5.391175441198789109, 24.15498966839961170 ) ) ;
#9813=VERTEX_POINT ( 'NONE', #3047 ) ;
#9816=B_SPLINE_CURVE_WITH_KNOTS ( 'NONE', 3,
 ( #3160, #10216, #10071, #7845 ),
 .UNSPECIFIED., .F., .F.,
 ( 4, 4 ),
 ( 1.981826382900813409E-07, 0.0006887856082032186092 ),
 .UNSPECIFIED. ) ;
#9820=DIRECTION ( 'NONE',  ( -1.000000000000000000, 0.000000000000000000, 0.000000000000000000 ) ) ;
#9825=VERTEX_POINT ( 'NONE', #6664 ) ;
#9827=DIRECTION ( 'NONE',  ( -1.000000000000000000, -0.000000000000000000, -0.000000000000000000 ) ) ;
#9828=ORIENTED_EDGE ( 'NONE', *, *, #8353, .T. ) ;
#9833=ORIENTED_EDGE ( 'NONE', *, *, #5415, .F. ) ;
#9834=CYLINDRICAL_SURFACE ( 'NONE', #11915, 2.524999999999995914 ) ;
#9837=ORIENTED_EDGE ( 'NONE', *, *, #9934, .F. ) ;
#9840=ADVANCED_FACE ( 'NONE', ( #9122 ), #13801, .T. ) ;
#9842=CARTESIAN_POINT ( 'NONE',  ( 2.031033479673589159, 19.12621924769867121, 19.86422722021319487 ) ) ;
#9843=CARTESIAN_POINT ( 'NONE',  ( 1.749999999999998002, 0.000000000000000000, 0.000000000000000000 ) ) ;
#9845=CARTESIAN_POINT ( 'NONE',  ( 0.000000000000000000, 20.62201879784932856, -12.52067188844328705 ) ) ;
#9847=DIRECTION ( 'NONE',  ( -1.000000000000000000, -0.000000000000000000, -0.000000000000000000 ) ) ;
#9848=ADVANCED_FACE ( 'NONE', ( #745 ), #10193, .T. ) ;
#9850=ORIENTED_EDGE ( 'NONE', *, *, #8983, .F. ) ;
#9852=DIRECTION ( 'NONE',  ( -1.000000000000000000, -0.000000000000000000, -0.000000000000000000 ) ) ;
#9857=VERTEX_POINT ( 'NONE', #10340 ) ;
#9860=CARTESIAN_POINT ( 'NONE',  ( 2.765633920072239516, 16.37294372382858398, 18.55949924794898465 ) ) ;
#9861=CARTESIAN_POINT ( 'NONE',  ( 0.000000000000000000, 23.48180575137739368, -5.535312321042471062 ) ) ;
#9862=FACE_OUTER_BOUND ( 'NONE', #13394, .T. ) ;
#9864=CARTESIAN_POINT ( 'NONE',  ( 2.459751808031945922E-16, 12.51294990530016271, 20.85230829256858343 ) ) ;
#9865=CARTESIAN_POINT ( 'NONE',  ( 2.789999999999999147, 2.336989772644269436, 24.63872515616083447 ) ) ;
#9866=ORIENTED_EDGE ( 'NONE', *, *, #3200, .F. ) ;
#9867=VERTEX_POINT ( 'NONE', #8881 ) ;
#9876=DIRECTION ( 'NONE',  ( 0.000000000000000000, 0.000000000000000000, 1.000000000000000000 ) ) ;
#9879=ORIENTED_EDGE ( 'NONE', *, *, #13416, .T. ) ;
#9880=ORIENTED_EDGE ( 'NONE', *, *, #11826, .F. ) ;
#9881=ORIENTED_EDGE ( 'NONE', *, *, #5143, .F. ) ;
#9882=CARTESIAN_POINT ( 'NONE',  ( 0.02436607992776498519, -21.30679549418621832, -12.59161484032935618 ) ) ;
#9885=CARTESIAN_POINT ( 'NONE',  ( 2.718131864678289933, -2.577209017046833583, -25.22589920183363787 ) ) ;
#9886=CARTESIAN_POINT ( 'NONE',  ( 2.718184743034447681, -5.344212458769196594, -24.78695292654926519 ) ) ;
#9890=CARTESIAN_POINT ( 'NONE',  ( 1.749999999999998002, 25.12109765559671004, -12.52377138324198391 ) ) ;
#9899=CARTESIAN_POINT ( 'NONE',  ( 1.039999999999998925, -4.147968289691484678, 27.76164181293050248 ) ) ;
#9900=ORIENTED_EDGE ( 'NONE', *, *, #11578, .T. ) ;
#9907=TOROIDAL_SURFACE ( 'NONE', #12003, 24.12539914357697413, 8.000000000000000000 ) ;
#9909=DIRECTION ( 'NONE',  ( -1.000000000000000000, -0.000000000000000000, -0.000000000000000000 ) ) ;
#9911=CARTESIAN_POINT ( 'NONE',  ( 2.790000000000076419, -2.133839912090968127, 24.22524813288760726 ) ) ;
#9913=ADVANCED_FACE ( 'NONE', ( #9191 ), #6731, .T. ) ;
#9914=AXIS2_PLACEMENT_3D ( 'NONE', #7209, #11885, #13038 ) ;
#9918=DIRECTION ( 'NONE',  ( -1.000000000000000000, 0.000000000000000000, 0.000000000000000000 ) ) ;
#9922=AXIS2_PLACEMENT_3D ( 'NONE', #13291, #8608, #2771 ) ;
#9923=EDGE_CURVE ( 'NONE', #1158, #12816, #11636, .T. ) ;
#9926=DIRECTION ( 'NONE',  ( 0.000000000000000000, 0.000000000000000000, 1.000000000000000000 ) ) ;
#9930=CARTESIAN_POINT ( 'NONE',  ( -6.403158385254602634E-17, -23.69843731927173991, 5.456805104201007950 ) ) ;
#9932=EDGE_CURVE ( 'NONE', #9447, #1296, #9569, .T. ) ;
#9934=EDGE_CURVE ( 'NONE', #6218, #10191, #12671, .T. ) ;
#9935=CARTESIAN_POINT ( 'NONE',  ( 0.07186808533286645484, -10.24630254990532663, 23.19485392143210944 ) ) ;
#9938=CARTESIAN_POINT ( 'NONE',  ( 0.006931111373680289185, 9.685942809247373830, -22.53293026234493723 ) ) ;
#9939=EDGE_LOOP ( 'NONE', ( #10712, #10112, #5701, #473, #3082, #1189, #1345, #4447 ) ) ;
#9942=VERTEX_POINT ( 'NONE', #2497 ) ;
#9953=EDGE_CURVE ( 'NONE', #6110, #8350, #11786, .T. ) ;
#9955=CARTESIAN_POINT ( 'NONE',  ( 2.789999999999999147, -24.44424927289185590, -0.2301004812060095106 ) ) ;
#9956=DIRECTION ( 'NONE',  ( -1.000000000000000000, -0.000000000000000000, -0.000000000000000000 ) ) ;
#9957=VERTEX_POINT ( 'NONE', #2273 ) ;
#9961=ORIENTED_EDGE ( 'NONE', *, *, #5649, .T. ) ;
#9965=CARTESIAN_POINT ( 'NONE',  ( 0.1882238946918228795, -25.78859396478530641, 2.857713464478602194 ) ) ;
#9966=CARTESIAN_POINT ( 'NONE',  ( 0.1855654851361735469, 10.67816411292198175, -23.63475234378971379 ) ) ;
#9968=DIRECTION ( 'NONE',  ( 1.000000000000000000, -0.000000000000000000, 0.000000000000000000 ) ) ;
#9970=CARTESIAN_POINT ( 'NONE',  ( 2.783025325906568259, 24.42374957165205629, 2.249040938978581927 ) ) ;
#9971=CIRCLE ( 'NONE', #13896, 28.06981291497571362 ) ;
#9973=CARTESIAN_POINT ( 'NONE',  ( 0.7589665326895898012, 24.32849926382769468, -12.98167595240995986 ) ) ;
#9977=CARTESIAN_POINT ( 'NONE',  ( 2.718184743034448569, 24.78695292654929005, -5.344212458769106888 ) ) ;
#9978=CIRCLE ( 'NONE', #3349, 28.06981291497571362 ) ;
#9987=DIRECTION ( 'NONE',  ( 1.000000000000000000, 0.000000000000000000, 0.000000000000000000 ) ) ;
#9989=CARTESIAN_POINT ( 'NONE',  ( 2.765633920072239516, 16.37294372382858398, 18.55949924794898465 ) ) ;
#9990=CARTESIAN_POINT ( 'NONE',  ( 0.7592463941534229876, -3.797885586973023475, -27.31305418910213234 ) ) ;
#9994=ADVANCED_FACE ( 'NONE', ( #8182 ), #1198, .F. ) ;
#9995=ORIENTED_EDGE ( 'NONE', *, *, #13946, .F. ) ;
#9996=CARTESIAN_POINT ( 'NONE',  ( 0.006974771092478813939, -22.53337530003410905, 9.686319561460866367 ) ) ;
#10002=ORIENTED_EDGE ( 'NONE', *, *, #5263, .F. ) ;
#10004=CARTESIAN_POINT ( 'NONE',  ( 0.02436607992775761261, 22.71065055754452544, 9.836394144775786330 ) ) ;
#10007=B_SPLINE_CURVE_WITH_KNOTS ( 'NONE', 3,
 ( #12042, #5229, #1606, #3830 ),
 .UNSPECIFIED., .F., .F.,
 ( 4, 4 ),
 ( 0.003263275852154340524, 0.003756984793530001795 ),
 .UNSPECIFIED. ) ;
#10009=CIRCLE ( 'NONE', #12945, 2.524999999999995914 ) ;
#10012=B_SPLINE_CURVE_WITH_KNOTS ( 'NONE', 3,
 ( #9348, #973, #3357, #5674, #4820, #8341 ),
 .UNSPECIFIED., .F., .F.,
 ( 4, 2, 4 ),
 ( 2.132675795043207789E-07, 0.001878604073277004988, 0.003756994878974505639 ),
 .UNSPECIFIED. ) ;
#10015=CARTESIAN_POINT ( 'NONE',  ( 0.7592463941534238758, 27.31305418910209681, -3.797885586973310801 ) ) ;
#10016=CYLINDRICAL_SURFACE ( 'NONE', #6816, 28.06981291497571362 ) ;
#10018=EDGE_CURVE ( 'NONE', #910, #1849, #12858, .T. ) ;
#10023=ORIENTED_EDGE ( 'NONE', *, *, #5595, .F. ) ;
#10025=LINE ( 'NONE', #9865, #1339 ) ;
#10026=ORIENTED_EDGE ( 'NONE', *, *, #4051, .F. ) ;
#10027=ORIENTED_EDGE ( 'NONE', *, *, #2913, .F. ) ;
#10029=EDGE_CURVE ( 'NONE', #85, #11822, #10723, .T. ) ;
#10030=EDGE_CURVE ( 'NONE', #672, #4130, #7332, .T. ) ;
#10038=ORIENTED_EDGE ( 'NONE', *, *, #4570, .T. ) ;
#10045=B_SPLINE_CURVE_WITH_KNOTS ( 'NONE', 3,
 ( #13980, #6684, #6615, #989, #835, #3447 ),
 .UNSPECIFIED., .F., .F.,
 ( 4, 2, 4 ),
 ( 1.979325885420663486E-07, 0.001878588715165609938, 0.003756979497742677504 ),
 .UNSPECIFIED. ) ;
#10049=EDGE_CURVE ( 'NONE', #3458, #1390, #7176, .T. ) ;
#10055=CARTESIAN_POINT ( 'NONE',  ( 0.000000000000000000, 23.48180575137739368, -5.535312321042471062 ) ) ;
#10056=EDGE_CURVE ( 'NONE', #3010, #6024, #6442, .T. ) ;
#10061=EDGE_LOOP ( 'NONE', ( #13783, #4134, #7655, #14097 ) ) ;
#10063=CARTESIAN_POINT ( 'NONE',  ( 2.031033465052724196, 4.828387785248403397, -27.14933624560903525 ) ) ;
#10065=ORIENTED_EDGE ( 'NONE', *, *, #9376, .F. ) ;
#10068=CARTESIAN_POINT ( 'NONE',  ( 1.774186184918758212E-16, 2.133490293297354956, -24.22479935914658000 ) ) ;
#10071=CARTESIAN_POINT ( 'NONE',  ( 2.790000000000077307, -5.456611084821691549, -23.69897269326682832 ) ) ;
#10073=CARTESIAN_POINT ( 'NONE',  ( 0.02436607992776325046, -18.55949924794904504, 16.37294372382852004 ) ) ;
#10074=ORIENTED_EDGE ( 'NONE', *, *, #13596, .F. ) ;
#10076=LINE ( 'NONE', #14772, #10657 ) ;
#10078=( LENGTH_UNIT ( ) NAMED_UNIT ( * ) SI_UNIT ( .MILLI., .METRE. ) );
#10086=DIRECTION ( 'NONE',  ( -1.000000000000000000, -0.000000000000000000, -0.000000000000000000 ) ) ;
#10090=CARTESIAN_POINT ( 'NONE',  ( 0.5279272304333944010, -11.57956866523235462, 24.43806413951671530 ) ) ;
#10091=CARTESIAN_POINT ( 'NONE',  ( 0.8291131470075020493, -24.44424927289185590, 12.96989951879399072 ) ) ;
#10098=ORIENTED_EDGE ( 'NONE', *, *, #13764, .T. ) ;
#10100=EDGE_CURVE ( 'NONE', #949, #14075, #4082, .T. ) ;
#10102=FACE_OUTER_BOUND ( 'NONE', #8091, .T. ) ;
#10106=DIRECTION ( 'NONE',  ( -1.000000000000000000, -0.000000000000000000, -0.000000000000000000 ) ) ;
#10107=CARTESIAN_POINT ( 'NONE',  ( 0.006974693931643255289, 16.17543236987988919, 18.43727551351037519 ) ) ;
#10109=CARTESIAN_POINT ( 'NONE',  ( 2.789999999999999147, 24.34211360614310848, -7.909232158574561744 ) ) ;
#10111=ORIENTED_EDGE ( 'NONE', *, *, #14144, .T. ) ;
#10112=ORIENTED_EDGE ( 'NONE', *, *, #2644, .T. ) ;
#10114=EDGE_LOOP ( 'NONE', ( #13994, #9486, #4539, #14970 ) ) ;
#10115=CARTESIAN_POINT ( 'NONE',  ( 2.031033471609898111, 3.797536611356316705, 27.31260702007176988 ) ) ;
#10122=CARTESIAN_POINT ( 'NONE',  ( 0.1855657168891852171, 22.53097606933003405, -12.84444904262000975 ) ) ;
#10124=ADVANCED_FACE ( 'NONE', ( #6184 ), #3962, .F. ) ;
#10129=DIRECTION ( 'NONE',  ( -1.000000000000000000, -0.000000000000000000, -0.000000000000000000 ) ) ;
#10130=FACE_OUTER_BOUND ( 'NONE', #153, .T. ) ;
#10132=EDGE_CURVE ( 'NONE', #4420, #6654, #6340, .T. ) ;
#10133=VERTEX_POINT ( 'NONE', #5130 ) ;
#10135=CARTESIAN_POINT ( 'NONE',  ( 2.783025336474040934, -21.08118142846912235, 12.53640742967745858 ) ) ;
#10136=ORIENTED_EDGE ( 'NONE', *, *, #10132, .T. ) ;
#10138=FACE_OUTER_BOUND ( 'NONE', #4721, .T. ) ;
#10142=CARTESIAN_POINT ( 'NONE',  ( 0.1882238946918232125, -2.857713464478510268, -25.78859396478530996 ) ) ;
#10143=CYLINDRICAL_SURFACE ( 'NONE', #12383, 28.06981291497571362 ) ;
#10144=CARTESIAN_POINT ( 'NONE',  ( 1.039999999999996705, -19.67366047555515252, -20.02152543075367319 ) ) ;
#10145=CARTESIAN_POINT ( 'NONE',  ( 2.765633920072238627, 5.391175441198956086, -24.15498966839956907 ) ) ;
#10146=EDGE_CURVE ( 'NONE', #11722, #14952, #4985, .T. ) ;
#10147=VERTEX_POINT ( 'NONE', #13401 ) ;
#10150=EDGE_CURVE ( 'NONE', #1390, #1547, #13210, .T. ) ;
#10153=ORIENTED_EDGE ( 'NONE', *, *, #14469, .F. ) ;
#10154=ORIENTED_EDGE ( 'NONE', *, *, #5346, .F. ) ;
#10156=DIRECTION ( 'NONE',  ( 1.000000000000000000, -0.000000000000000000, -0.000000000000000000 ) ) ;
#10163=EDGE_CURVE ( 'NONE', #7854, #13647, #2395, .T. ) ;
#10167=VECTOR ( 'NONE', #7618, 1000.000000000000000 ) ;
#10169=ORIENTED_EDGE ( 'NONE', *, *, #4453, .T. ) ;
#10174=B_SPLINE_CURVE_WITH_KNOTS ( 'NONE', 3,
 ( #2306, #9603, #3686, #1380 ),
 .UNSPECIFIED., .F., .F.,
 ( 4, 4 ),
 ( 2.135345996173297489E-07, 0.0006888010880210770339 ),
 .UNSPECIFIED. ) ;
#10182=EDGE_LOOP ( 'NONE', ( #14349, #2981, #4424, #2532 ) ) ;
#10183=DIRECTION ( 'NONE',  ( 0.000000000000000000, 0.000000000000000000, 1.000000000000000000 ) ) ;
#10187=VERTEX_POINT ( 'NONE', #4264 ) ;
#10189=ORIENTED_EDGE ( 'NONE', *, *, #2913, .T. ) ;
#10190=AXIS2_PLACEMENT_3D ( 'NONE', #7243, #10779, #11770 ) ;
#10191=VERTEX_POINT ( 'NONE', #14000 ) ;
#10192=CYLINDRICAL_SURFACE ( 'NONE', #8041, 13.19999999999999929 ) ;
#10193=CYLINDRICAL_SURFACE ( 'NONE', #12944, 28.06981291497571362 ) ;
#10194=B_SPLINE_CURVE_WITH_KNOTS ( 'NONE', 3,
 ( #13982, #12882, #2294, #5844 ),
 .UNSPECIFIED., .F., .F.,
 ( 4, 4 ),
 ( 1.981826382900847290E-07, 0.0006887856082032348722 ),
 .UNSPECIFIED. ) ;
#10198=FACE_OUTER_BOUND ( 'NONE', #12049, .T. ) ;
#10203=CARTESIAN_POINT ( 'NONE',  ( 0.02436607992776368414, -9.836394144775550075, -22.71065055754462492 ) ) ;
#10205=ORIENTED_EDGE ( 'NONE', *, *, #10975, .F. ) ;
#10206=EDGE_CURVE ( 'NONE', #9372, #7839, #10274, .T. ) ;
#10208=CARTESIAN_POINT ( 'NONE',  ( 0.006974693931642682830, -16.17543236987975064, -18.43727551351049598 ) ) ;
#10209=ORIENTED_EDGE ( 'NONE', *, *, #742, .F. ) ;
#10211=DIRECTION ( 'NONE',  ( 0.000000000000000000, 0.000000000000000000, 1.000000000000000000 ) ) ;
#10216=CARTESIAN_POINT ( 'NONE',  ( 2.783025342027735327, -5.408388659523925668, -23.92335783895643075 ) ) ;
#10217=ADVANCED_FACE ( 'NONE', ( #8153 ), #4642, .T. ) ;
#10220=CARTESIAN_POINT ( 'NONE',  ( 0.02436607992776151574, 24.15498966839970052, -5.391175441198366336 ) ) ;
#10225=CARTESIAN_POINT ( 'NONE',  ( 0.02436607992776108206, -24.15498966839966855, 5.391175441198523544 ) ) ;
#10226=B_SPLINE_CURVE_WITH_KNOTS ( 'NONE', 3,
 ( #9354, #4826, #10734, #192 ),
 .UNSPECIFIED., .F., .F.,
 ( 4, 4 ),
 ( 3.059063720746937335E-07, 0.0006888942284914101538 ),
 .UNSPECIFIED. ) ;
#10228=ORIENTED_EDGE ( 'NONE', *, *, #3382, .T. ) ;
#10230=EDGE_LOOP ( 'NONE', ( #5203, #2305, #1938, #11764, #5128, #6214, #10249, #13458 ) ) ;
#10235=AXIS2_PLACEMENT_3D ( 'NONE', #9058, #6745, #11424 ) ;
#10237=CARTESIAN_POINT ( 'NONE',  ( 1.749999999999998002, -27.68468304288255766, -4.633866840649213614 ) ) ;
#10246=AXIS2_PLACEMENT_3D ( 'NONE', #14251, #13003, #5950 ) ;
#10248=AXIS2_PLACEMENT_3D ( 'NONE', #1356, #13104, #2591 ) ;
#10249=ORIENTED_EDGE ( 'NONE', *, *, #249, .T. ) ;
#10254=VERTEX_POINT ( 'NONE', #14794 ) ;
#10256=VECTOR ( 'NONE', #14573, 1000.000000000000000 ) ;
#10260=DIRECTION ( 'NONE',  ( -1.000000000000000000, 0.000000000000000000, 0.000000000000000000 ) ) ;
#10261=DIRECTION ( 'NONE',  ( 0.000000000000000000, 0.000000000000000000, 1.000000000000000000 ) ) ;
#10262=DIRECTION ( 'NONE',  ( 0.000000000000000000, -0.3090169943749406234, -0.9510565162951558627 ) ) ;
#10264=AXIS2_PLACEMENT_3D ( 'NONE', #14215, #13846, #6863 ) ;
#10267=CARTESIAN_POINT ( 'NONE',  ( 1.749999999999998002, 12.96210679857786552, 24.89775460606837143 ) ) ;
#10274=CIRCLE ( 'NONE', #2418, 28.06981291497571362 ) ;
#10281=B_SPLINE_CURVE_WITH_KNOTS ( 'NONE', 3,
 ( #13202, #1680, #11049, #432, #6364, #5075 ),
 .UNSPECIFIED., .F., .F.,
 ( 4, 2, 4 ),
 ( 2.032124546189621919E-07, 0.001878594002992312268, 0.003756984793530005265 ),
 .UNSPECIFIED. ) ;
#10287=DIRECTION ( 'NONE',  ( 0.000000000000000000, 0.000000000000000000, 1.000000000000000000 ) ) ;
#10288=CARTESIAN_POINT ( 'NONE',  ( 2.790000000000076419, -20.85287692521938752, 12.51293083811791718 ) ) ;
#10289=EDGE_LOOP ( 'NONE', ( #5159, #8474, #13534, #10831 ) ) ;
#10292=CARTESIAN_POINT ( 'NONE',  ( 2.789999999999999147, 24.63872515616082737, -2.336989772644355590 ) ) ;
#10293=EDGE_CURVE ( 'NONE', #9857, #5968, #3859, .T. ) ;
#10296=LINE ( 'NONE', #2293, #4289 ) ;
#10299=CARTESIAN_POINT ( 'NONE',  ( 0.5321745087963413168, -24.44564404695853455, 11.58891744060097295 ) ) ;
#10301=VECTOR ( 'NONE', #5418, 1000.000000000000000 ) ;
#10303=DIRECTION ( 'NONE',  ( -1.000000000000000000, -0.000000000000000000, 0.000000000000000000 ) ) ;
#10306=EDGE_CURVE ( 'NONE', #9372, #8828, #13555, .T. ) ;
#10307=( NAMED_UNIT ( * ) SI_UNIT ( $, .STERADIAN. ) SOLID_ANGLE_UNIT ( ) );
#10310=VERTEX_POINT ( 'NONE', #2 ) ;
#10311=ORIENTED_EDGE ( 'NONE', *, *, #8983, .T. ) ;
#10314=CARTESIAN_POINT ( 'NONE',  ( 0.5279272304333941790, -24.43806413951667622, -11.57956866523244166 ) ) ;
#10317=ORIENTED_EDGE ( 'NONE', *, *, #14233, .T. ) ;
#10318=CARTESIAN_POINT ( 'NONE',  ( 0.5279272304333949561, 24.43806413951675793, 11.57956866523226580 ) ) ;
#10320=ADVANCED_FACE ( 'NONE', ( #11323 ), #1011, .T. ) ;
#10323=ADVANCED_FACE ( 'NONE', ( #7001 ), #13709, .T. ) ;
#10332=ORIENTED_EDGE ( 'NONE', *, *, #3663, .T. ) ;
#10336=ORIENTED_EDGE ( 'NONE', *, *, #13988, .F. ) ;
#10339=ORIENTED_EDGE ( 'NONE', *, *, #1979, .T. ) ;
#10340=CARTESIAN_POINT ( 'NONE',  ( 1.749999999999998002, -24.89775460606842117, 12.96210679857777137 ) ) ;
#10343=CARTESIAN_POINT ( 'NONE',  ( 0.9659243001600011924, 24.74770846292485516, 12.96726489871199028 ) ) ;
#10349=DIRECTION ( 'NONE',  ( -1.000000000000000000, 0.000000000000000000, -0.000000000000000000 ) ) ;
#10352=ORIENTED_EDGE ( 'NONE', *, *, #1686, .T. ) ;
#10353=EDGE_CURVE ( 'NONE', #10147, #1055, #7155, .T. ) ;
#10355=CARTESIAN_POINT ( 'NONE',  ( 2.765633920072238627, 12.59161484032942901, -21.30679549418617924 ) ) ;
#10356=ORIENTED_EDGE ( 'NONE', *, *, #11904, .F. ) ;
#10357=EDGE_LOOP ( 'NONE', ( #5992, #12441, #3122, #10209 ) ) ;
#10359=DIRECTION ( 'NONE',  ( 1.000000000000000000, -0.000000000000000000, -0.000000000000000000 ) ) ;
#10360=ORIENTED_EDGE ( 'NONE', *, *, #10432, .T. ) ;
#10361=DIRECTION ( 'NONE',  ( -1.000000000000000000, -0.000000000000000000, 0.000000000000000000 ) ) ;
#10363=B_SPLINE_CURVE_WITH_KNOTS ( 'NONE', 3,
 ( #3190, #10390, #9100, #2024, #13933, #10475 ),
 .UNSPECIFIED., .F., .F.,
 ( 4, 2, 4 ),
 ( 1.979325885420528755E-07, 0.001878588715165608204, 0.003756979497742674035 ),
 .UNSPECIFIED. ) ;
#10364=CARTESIAN_POINT ( 'NONE',  ( 2.789895104907798906, 20.67847077765723185, -12.51925356660737876 ) ) ;
#10367=CARTESIAN_POINT ( 'NONE',  ( 0.02436607992775978102, -12.59161484032896361, -21.30679549418645280 ) ) ;
#10368=CARTESIAN_POINT ( 'NONE',  ( 1.960886852992457241, 24.44424927289185945, 12.96989951879416125 ) ) ;
#10370=ORIENTED_EDGE ( 'NONE', *, *, #7629, .F. ) ;
#10372=DIRECTION ( 'NONE',  ( -1.000000000000000000, -0.000000000000000000, -0.000000000000000000 ) ) ;
#10374=VERTEX_POINT ( 'NONE', #7227 ) ;
#10381=CARTESIAN_POINT ( 'NONE',  ( 1.749999999999998002, 27.76164181293051669, -4.147968289691384314 ) ) ;
#10388=EDGE_CURVE ( 'NONE', #6042, #14329, #14310, .T. ) ;
#10389=ORIENTED_EDGE ( 'NONE', *, *, #14425, .F. ) ;
#10390=CARTESIAN_POINT ( 'NONE',  ( 0.07186815222488071586, -5.344160105508533931, -24.78765742476144140 ) ) ;
#10392=EDGE_LOOP ( 'NONE', ( #12226, #8803, #13938, #8368, #2026, #6048, #4262 ) ) ;
#10394=DIRECTION ( 'NONE',  ( 0.000000000000000000, 0.000000000000000000, 1.000000000000000000 ) ) ;
#10403=TOROIDAL_SURFACE ( 'NONE', #14610, 24.12539914357697413, 8.000000000000000000 ) ;
#10412=B_SPLINE_CURVE_WITH_KNOTS ( 'NONE', 3,
 ( #8431, #4483, #15015, #13118, #2529, #3321 ),
 .UNSPECIFIED., .F., .F.,
 ( 4, 2, 4 ),
 ( 4.462636808902389156E-07, 0.001879885123572227514, 0.003759323983463565104 ),
 .UNSPECIFIED. ) ;
#10420=DIRECTION ( 'NONE',  ( -1.000000000000000000, -0.000000000000000000, -0.000000000000000000 ) ) ;
#10421=B_SPLINE_CURVE_WITH_KNOTS ( 'NONE', 3,
 ( #7682, #10068, #1841, #1697 ),
 .UNSPECIFIED., .F., .F.,
 ( 4, 4 ),
 ( 0.005258120783916789796, 0.005948386350302923772 ),
 .UNSPECIFIED. ) ;
#10430=DIRECTION ( 'NONE',  ( -1.000000000000000000, -0.000000000000000000, 0.000000000000000000 ) ) ;
#10432=EDGE_CURVE ( 'NONE', #3410, #11249, #5933, .T. ) ;
#10433=ORIENTED_EDGE ( 'NONE', *, *, #589, .T. ) ;
#10435=CYLINDRICAL_SURFACE ( 'NONE', #13655, 13.19999999999999929 ) ;
#10438=ORIENTED_EDGE ( 'NONE', *, *, #10206, .T. ) ;
#10439=DIRECTION ( 'NONE',  ( -1.000000000000000000, 0.000000000000000000, 0.000000000000000000 ) ) ;
#10448=CARTESIAN_POINT ( 'NONE',  ( 2.789999999999999147, -15.74360496233394002, 18.28042085475272671 ) ) ;
#10450=EDGE_LOOP ( 'NONE', ( #14921, #7910, #11313, #13307 ) ) ;
#10463=EDGE_CURVE ( 'NONE', #9117, #5459, #79, .T. ) ;
#10465=CARTESIAN_POINT ( 'NONE',  ( 2.765633920072239071, -12.59161484032927092, 21.30679549418627161 ) ) ;
#10470=B_SPLINE_CURVE_WITH_KNOTS ( 'NONE', 3,
 ( #6983, #6435, #4998, #12197 ),
 .UNSPECIFIED., .F., .F.,
 ( 4, 4 ),
 ( 2.034713381942717623E-07, 0.0006887909409525219510 ),
 .UNSPECIFIED. ) ;
#10472=AXIS2_PLACEMENT_3D ( 'NONE', #8839, #9847, #14541 ) ;
#10475=CARTESIAN_POINT ( 'NONE',  ( 1.039999999999997149, -4.633866840648735774, -27.68468304288263226 ) ) ;
#10476=VECTOR ( 'NONE', #15092, 1000.000000000000000 ) ;
#10479=ORIENTED_EDGE ( 'NONE', *, *, #1979, .F. ) ;
#10485=CARTESIAN_POINT ( 'NONE',  ( 0.006930995026450970445, 23.92277630352802831, -5.408431875071194384 ) ) ;
#10487=DIRECTION ( 'NONE',  ( -1.000000000000000000, -0.000000000000000000, -0.000000000000000000 ) ) ;
#10490=AXIS2_PLACEMENT_3D ( 'NONE', #10959, #4988, #423 ) ;
#10491=ORIENTED_EDGE ( 'NONE', *, *, #11745, .F. ) ;
#10497=EDGE_CURVE ( 'NONE', #14161, #2553, #587, .T. ) ;
#10498=EDGE_CURVE ( 'NONE', #8078, #1582, #12857, .T. ) ;
#10499=EDGE_CURVE ( 'NONE', #5734, #2490, #9540, .T. ) ;
#10500=ORIENTED_EDGE ( 'NONE', *, *, #1310, .T. ) ;
#10502=CARTESIAN_POINT ( 'NONE',  ( 1.394999999999998685, 25.12109765559671004, -12.52377138324198214 ) ) ;
#10504=FACE_OUTER_BOUND ( 'NONE', #8680, .T. ) ;
#10507=B_SPLINE_CURVE_WITH_KNOTS ( 'NONE', 3,
 ( #13702, #6932, #9163, #9241 ),
 .UNSPECIFIED., .F., .F.,
 ( 4, 4 ),
 ( 0.005258105385878685673, 0.005948373736081384068 ),
 .UNSPECIFIED. ) ;
#10508=AXIS2_PLACEMENT_3D ( 'NONE', #2946, #11241, #13471 ) ;
#10511=FACE_OUTER_BOUND ( 'NONE', #7678, .T. ) ;
#10512=DIRECTION ( 'NONE',  ( -1.000000000000000000, -0.000000000000000000, -0.000000000000000000 ) ) ;
#10515=ADVANCED_FACE ( 'NONE', ( #3999 ), #6380, .F. ) ;
#10517=CIRCLE ( 'NONE', #3885, 24.12539914357697413 ) ;
#10519=EDGE_CURVE ( 'NONE', #14952, #495, #3540, .T. ) ;
#10523=AXIS2_PLACEMENT_3D ( 'NONE', #13329, #2807, #260 ) ;
#10528=DIRECTION ( 'NONE',  ( 0.000000000000000000, 0.000000000000000000, 1.000000000000000000 ) ) ;
#10530=CARTESIAN_POINT ( 'NONE',  ( 1.039999999999997149, -24.89775460606822577, -12.96210679857813730 ) ) ;
#10540=ORIENTED_EDGE ( 'NONE', *, *, #10056, .F. ) ;
#10541=EDGE_LOOP ( 'NONE', ( #3609, #5579, #7198, #8374, #850, #8577, #8435, #8313 ) ) ;
#10542=ORIENTED_EDGE ( 'NONE', *, *, #10163, .T. ) ;
#10544=CARTESIAN_POINT ( 'NONE',  ( 2.718184743034447237, -24.78695292654925808, 5.344212458769271201 ) ) ;
#10545=CARTESIAN_POINT ( 'NONE',  ( -5.209999999999999964, 0.000000000000000000, 0.000000000000000000 ) ) ;
#10547=CIRCLE ( 'NONE', #11993, 2.524999999999996803 ) ;
#10549=ORIENTED_EDGE ( 'NONE', *, *, #13006, .F. ) ;
#10552=VERTEX_POINT ( 'NONE', #10990 ) ;
#10553=CARTESIAN_POINT ( 'NONE',  ( 1.960886852992457241, 24.44424927289185945, 12.96989951879416125 ) ) ;
#10560=ORIENTED_EDGE ( 'NONE', *, *, #13952, .T. ) ;
#10563=ADVANCED_FACE ( 'NONE', ( #11064 ), #3063, .T. ) ;
#10566=ORIENTED_EDGE ( 'NONE', *, *, #4999, .T. ) ;
#10570=EDGE_LOOP ( 'NONE', ( #7029, #9710, #13822, #5834 ) ) ;
#10574=CARTESIAN_POINT ( 'NONE',  ( -7.723595606797438030E-14, -23.69897269326674305, -5.456611084822102775 ) ) ;
#10575=CARTESIAN_POINT ( 'NONE',  ( 0.000000000000000000, -24.34211360614305875, 7.909232158574721616 ) ) ;
#10576=LINE ( 'NONE', #2349, #13113 ) ;
#10578=B_SPLINE_CURVE_WITH_KNOTS ( 'NONE', 3,
 ( #12008, #10858, #5197, #317, #9711, #398 ),
 .UNSPECIFIED., .F., .F.,
 ( 4, 2, 4 ),
 ( 2.132675795045763710E-07, 0.001878604073277002169, 0.003756994878974500001 ),
 .UNSPECIFIED. ) ;
#10580=ADVANCED_FACE ( 'NONE', ( #2927 ), #7683, .T. ) ;
#10583=CARTESIAN_POINT ( 'NONE',  ( 1.039999999999996483, -12.96210679857803783, 24.89775460606827551 ) ) ;
#10585=CARTESIAN_POINT ( 'NONE',  ( 2.789999999999999147, 2.680914349914567470E-13, -25.59481291497571220 ) ) ;
#10586=EDGE_LOOP ( 'NONE', ( #4047, #405, #5716, #5758 ) ) ;
#10587=ORIENTED_EDGE ( 'NONE', *, *, #646, .T. ) ;
#10594=CYLINDRICAL_SURFACE ( 'NONE', #14363, 28.06981291497571362 ) ;
#10595=CARTESIAN_POINT ( 'NONE',  ( 2.789679245949058917, 20.70663861606308487, -12.51925356660738053 ) ) ;
#10596=EDGE_CURVE ( 'NONE', #14085, #5202, #7545, .T. ) ;
#10605=ORIENTED_EDGE ( 'NONE', *, *, #1712, .F. ) ;
#10606=ORIENTED_EDGE ( 'NONE', *, *, #14570, .T. ) ;
#10610=CIRCLE ( 'NONE', #8151, 28.06981291497571007 ) ;
#10611=DIRECTION ( 'NONE',  ( 1.000000000000000000, 0.000000000000000000, -0.000000000000000000 ) ) ;
#10613=EDGE_CURVE ( 'NONE', #9942, #7028, #6618, .T. ) ;
#10617=EDGE_CURVE ( 'NONE', #9825, #9957, #10296, .T. ) ;
#10627=CARTESIAN_POINT ( 'NONE',  ( 2.789999999999999147, 23.48180575137730131, 5.535312321042802353 ) ) ;
#10630=CARTESIAN_POINT ( 'NONE',  ( 1.749999999999998002, -20.02152543075360214, 19.67366047555523068 ) ) ;
#10633=ORIENTED_EDGE ( 'NONE', *, *, #5649, .F. ) ;
#10635=CARTESIAN_POINT ( 'NONE',  ( 2.789999999999999147, 18.55949924794892780, 16.37294372382865504 ) ) ;
#10637=ORIENTED_EDGE ( 'NONE', *, *, #11336, .T. ) ;
#10642=DIRECTION ( 'NONE',  ( 0.000000000000000000, 0.000000000000000000, 1.000000000000000000 ) ) ;
#10643=CARTESIAN_POINT ( 'NONE',  ( 2.718131885465892239, -16.91241718341984779, -18.89333555428573774 ) ) ;
#10647=CARTESIAN_POINT ( 'NONE',  ( 2.765633920072235519, 18.55949924794892780, 16.37294372382865504 ) ) ;
#10652=ORIENTED_EDGE ( 'NONE', *, *, #12475, .T. ) ;
#10654=AXIS2_PLACEMENT_3D ( 'NONE', #7616, #12292, #1766 ) ;
#10657=VECTOR ( 'NONE', #4239, 1000.000000000000000 ) ;
#10659=CARTESIAN_POINT ( 'NONE',  ( -7.688810570594222860E-14, -5.456611084822025504, 23.69897269326675016 ) ) ;
#10660=CARTESIAN_POINT ( 'NONE',  ( 1.749999999999998002, -27.76164181293049182, -4.147968289691579713 ) ) ;
#10661=DIRECTION ( 'NONE',  ( 1.000000000000000000, 0.000000000000000000, 0.000000000000000000 ) ) ;
#10663=CARTESIAN_POINT ( 'NONE',  ( 2.765633920072235519, 24.15498966839970052, -5.391175441198366336 ) ) ;
#10667=CIRCLE ( 'NONE', #14114, 28.06981291497571362 ) ;
#10668=AXIS2_PLACEMENT_3D ( 'NONE', #10927, #12238, #6244 ) ;
#10687=AXIS2_PLACEMENT_3D ( 'NONE', #3475, #3191, #11688 ) ;
#10688=DIRECTION ( 'NONE',  ( 0.000000000000000000, 0.000000000000000000, 1.000000000000000000 ) ) ;
#10692=CARTESIAN_POINT ( 'NONE',  ( 2.789999999999999147, 1.991882183130294637, 24.04302995059966364 ) ) ;
#10695=EDGE_CURVE ( 'NONE', #11429, #11249, #4538, .T. ) ;
#10697=ORIENTED_EDGE ( 'NONE', *, *, #1696, .T. ) ;
#10698=DIRECTION ( 'NONE',  ( 0.000000000000000000, 0.000000000000000000, 1.000000000000000000 ) ) ;
#10703=ORIENTED_EDGE ( 'NONE', *, *, #227, .F. ) ;
#10705=DIRECTION ( 'NONE',  ( -1.000000000000000000, 0.000000000000000000, 0.000000000000000000 ) ) ;
#10706=ADVANCED_FACE ( 'NONE', ( #8134 ), #1585, .T. ) ;
#10708=DIRECTION ( 'NONE',  ( 0.000000000000000000, 0.000000000000000000, 1.000000000000000000 ) ) ;
#10710=CIRCLE ( 'NONE', #11679, 24.12539914357697768 ) ;
#10712=ORIENTED_EDGE ( 'NONE', *, *, #1592, .T. ) ;
#10715=DIRECTION ( 'NONE',  ( 1.000000000000000000, 0.000000000000000000, -0.000000000000000000 ) ) ;
#10721=ORIENTED_EDGE ( 'NONE', *, *, #8349, .F. ) ;
#10723=LINE ( 'NONE', #1337, #13949 ) ;
#10725=DIRECTION ( 'NONE',  ( 0.000000000000000000, 0.000000000000000000, 1.000000000000000000 ) ) ;
#10728=CARTESIAN_POINT ( 'NONE',  ( 0.001869172971454433714, -20.90869469097853894, -12.51925356660784594 ) ) ;
#10732=AXIS2_PLACEMENT_3D ( 'NONE', #4777, #8443, #11759 ) ;
#10733=CARTESIAN_POINT ( 'NONE',  ( 0.1882238782932344201, 17.47009390565490605, 19.18368891937496556 ) ) ;
#10734=CARTESIAN_POINT ( 'NONE',  ( 2.790000000000077307, 22.38018801136476554, 9.515416771311276278 ) ) ;
#10737=ORIENTED_EDGE ( 'NONE', *, *, #14618, .F. ) ;
#10738=ORIENTED_EDGE ( 'NONE', *, *, #1696, .F. ) ;
#10740=DIRECTION ( 'NONE',  ( -1.000000000000000000, 0.000000000000000000, 0.000000000000000000 ) ) ;
#10741=CARTESIAN_POINT ( 'NONE',  ( 2.765633920072236407, 2.336989772644613161, -24.63872515616080250 ) ) ;
#10743=AXIS2_PLACEMENT_3D ( 'NONE', #9656, #8277, #6977 ) ;
#10744=CARTESIAN_POINT ( 'NONE',  ( 0.000000000000000000, 0.000000000000000000, 0.000000000000000000 ) ) ;
#10748=ORIENTED_EDGE ( 'NONE', *, *, #1310, .F. ) ;
#10755=EDGE_CURVE ( 'NONE', #4429, #15084, #5766, .T. ) ;
#10758=VECTOR ( 'NONE', #251, 1000.000000000000000 ) ;
#10763=CARTESIAN_POINT ( 'NONE',  ( 2.789999999999999147, 15.04425356660790136, -18.18163861606255338 ) ) ;
#10768=CARTESIAN_POINT ( 'NONE',  ( 2.718131885465890463, 18.89333555428578748, -16.91241718341978029 ) ) ;
#10772=CARTESIAN_POINT ( 'NONE',  ( 1.039999999999997149, -4.633866840648735774, -27.68468304288263226 ) ) ;
#10773=EDGE_CURVE ( 'NONE', #10133, #5736, #2389, .T. ) ;
#10774=EDGE_CURVE ( 'NONE', #8517, #9447, #3782, .T. ) ;
#10775=TOROIDAL_SURFACE ( 'NONE', #9060, 24.12539914357697413, 8.000000000000000000 ) ;
#10778=CARTESIAN_POINT ( 'NONE',  ( 2.789999999999999147, -22.25075486061731667, -9.324097380959683434 ) ) ;
#10779=DIRECTION ( 'NONE',  ( -1.000000000000000000, 0.000000000000000000, -0.000000000000000000 ) ) ;
#10781=ORIENTED_EDGE ( 'NONE', *, *, #2673, .F. ) ;
#10783=ADVANCED_FACE ( 'NONE', ( #9589 ), #10594, .T. ) ;
#10784=EDGE_LOOP ( 'NONE', ( #1837, #13018, #4809, #4772 ) ) ;
#10793=DIRECTION ( 'NONE',  ( 0.000000000000000000, 0.000000000000000000, 1.000000000000000000 ) ) ;
#10796=VERTEX_POINT ( 'NONE', #1446 ) ;
#10803=CARTESIAN_POINT ( 'NONE',  ( 0.0003207540509381473352, -20.70663861606275447, -12.51925356660783528 ) ) ;
#10804=EDGE_LOOP ( 'NONE', ( #13149, #3811, #13415, #1153 ) ) ;
#10812=ORIENTED_EDGE ( 'NONE', *, *, #7802, .F. ) ;
#10818=DIRECTION ( 'NONE',  ( -1.000000000000000000, 0.000000000000000000, 0.000000000000000000 ) ) ;
#10819=EDGE_LOOP ( 'NONE', ( #15069, #6148, #9961, #6407 ) ) ;
#10822=ORIENTED_EDGE ( 'NONE', *, *, #2155, .F. ) ;
#10828=B_SPLINE_CURVE_WITH_KNOTS ( 'NONE', 3,
 ( #12924, #16, #7103, #9178, #11778, #13863 ),
 .UNSPECIFIED., .F., .F.,
 ( 4, 2, 4 ),
 ( 4.462636882221166670E-07, 0.001879885203074802827, 0.003759324142461383488 ),
 .UNSPECIFIED. ) ;
#10829=DIRECTION ( 'NONE',  ( 0.000000000000000000, 0.000000000000000000, -1.000000000000000000 ) ) ;
#10831=ORIENTED_EDGE ( 'NONE', *, *, #9004, .T. ) ;
#10839=DIRECTION ( 'NONE',  ( 0.000000000000000000, 0.000000000000000000, 1.000000000000000000 ) ) ;
#10841=ORIENTED_EDGE ( 'NONE', *, *, #11277, .F. ) ;
#10848=VERTEX_POINT ( 'NONE', #273 ) ;
#10850=EDGE_LOOP ( 'NONE', ( #4350, #4830, #7694, #2145, #5880, #12910 ) ) ;
#10855=CARTESIAN_POINT ( 'NONE',  ( 2.789999999999999147, -2.336989772644097574, -24.63872515616085224 ) ) ;
#10856=EDGE_CURVE ( 'NONE', #3207, #383, #2199, .T. ) ;
#10857=ORIENTED_EDGE ( 'NONE', *, *, #2527, .T. ) ;
#10858=CARTESIAN_POINT ( 'NONE',  ( 0.07186813532171051899, 2.577209017047360717, -25.22589920183358814 ) ) ;
#10859=CARTESIAN_POINT ( 'NONE',  ( 0.000000000000000000, 12.52067188844379864, -20.62201879784900882 ) ) ;
#10863=AXIS2_PLACEMENT_3D ( 'NONE', #5039, #6252, #2868 ) ;
#10864=ORIENTED_EDGE ( 'NONE', *, *, #14729, .T. ) ;
#10867=CARTESIAN_POINT ( 'NONE',  ( 1.749999999999998002, -12.52377138324206030, -25.12109765559667096 ) ) ;
#10868=ADVANCED_FACE ( 'NONE', ( #14357 ), #8505, .T. ) ;
#10870=CARTESIAN_POINT ( 'NONE',  ( 0.7592463977762113903, 27.14986936243574078, 4.828194074574446049 ) ) ;
#10874=DIRECTION ( 'NONE',  ( -1.000000000000000000, 0.000000000000000000, 0.000000000000000000 ) ) ;
#10875=CARTESIAN_POINT ( 'NONE',  ( 0.000000000000000000, 0.000000000000000000, 0.000000000000000000 ) ) ;
#10879=EDGE_CURVE ( 'NONE', #7933, #7573, #13424, .T. ) ;
#10883=DIRECTION ( 'NONE',  ( 1.000000000000000000, -0.000000000000000000, -0.000000000000000000 ) ) ;
#10884=CARTESIAN_POINT ( 'NONE',  ( 0.02436607992775674525, 9.836394144776026138, -22.71065055754441531 ) ) ;
#10886=DIRECTION ( 'NONE',  ( -1.000000000000000000, -0.000000000000000000, 0.000000000000000000 ) ) ;
#10887=CARTESIAN_POINT ( 'NONE',  ( 0.02436607992776368414, -9.836394144775550075, -22.71065055754462492 ) ) ;
#10890=ORIENTED_EDGE ( 'NONE', *, *, #11492, .T. ) ;
#10891=DIRECTION ( 'NONE',  ( -1.000000000000000000, 0.000000000000000000, 0.000000000000000000 ) ) ;
#10892=DIRECTION ( 'NONE',  ( -1.000000000000000000, -0.000000000000000000, -0.000000000000000000 ) ) ;
#10897=ORIENTED_EDGE ( 'NONE', *, *, #13068, .F. ) ;
#10898=CIRCLE ( 'NONE', #3533, 2.524999999999995914 ) ;
#10902=EDGE_LOOP ( 'NONE', ( #7979, #6898, #6093, #5360, #11845, #9900 ) ) ;
#10903=VERTEX_POINT ( 'NONE', #11191 ) ;
#10907=CARTESIAN_POINT ( 'NONE',  ( 2.718184745196086549, -12.74223776959184207, -21.92234060054359901 ) ) ;
#10915=DIRECTION ( 'NONE',  ( 0.000000000000000000, 0.000000000000000000, 1.000000000000000000 ) ) ;
#10916=EDGE_CURVE ( 'NONE', #14511, #7149, #14669, .T. ) ;
#10917=VECTOR ( 'NONE', #6711, 1000.000000000000000 ) ;
#10927=CARTESIAN_POINT ( 'NONE',  ( -5.209999999999999964, 0.000000000000000000, 0.000000000000000000 ) ) ;
#10928=CARTESIAN_POINT ( 'NONE',  ( 0.1855656748306462045, -2.851997810081830842, 25.77772010606605235 ) ) ;
#10929=DIRECTION ( 'NONE',  ( -1.000000000000000000, 0.000000000000000000, -0.000000000000000000 ) ) ;
#10930=VERTEX_POINT ( 'NONE', #10887 ) ;
#10932=CARTESIAN_POINT ( 'NONE',  ( 0.5279273620711159021, 12.96450951081217084, 23.73240184472501113 ) ) ;
#10937=CARTESIAN_POINT ( 'NONE',  ( 0.000000000000000000, 18.28042085475278000, 15.74360496233386719 ) ) ;
#10939=EDGE_LOOP ( 'NONE', ( #3882, #10136, #12304, #1604 ) ) ;
#10945=CARTESIAN_POINT ( 'NONE',  ( 2.789999999999999147, 18.28042085475301093, -15.74360496233361673 ) ) ;
#10948=DIRECTION ( 'NONE',  ( -1.000000000000000000, -0.000000000000000000, -0.000000000000000000 ) ) ;
#10951=DIRECTION ( 'NONE',  ( -1.000000000000000000, 0.000000000000000000, 0.000000000000000000 ) ) ;
#10952=ADVANCED_FACE ( 'NONE', ( #7663 ), #14442, .T. ) ;
#10954=VERTEX_POINT ( 'NONE', #14746 ) ;
#10957=CIRCLE ( 'NONE', #14157, 24.12539914357697768 ) ;
#10959=CARTESIAN_POINT ( 'NONE',  ( 0.000000000000000000, 0.000000000000000000, 0.000000000000000000 ) ) ;
#10961=AXIS2_PLACEMENT_3D ( 'NONE', #8830, #14532, #14377 ) ;
#10967=ORIENTED_EDGE ( 'NONE', *, *, #2679, .T. ) ;
#10975=EDGE_CURVE ( 'NONE', #1423, #13868, #8231, .T. ) ;
#10977=VECTOR ( 'NONE', #5614, 1000.000000000000000 ) ;
#10980=DIRECTION ( 'NONE',  ( -1.000000000000000000, -0.000000000000000000, -0.000000000000000000 ) ) ;
#10986=CARTESIAN_POINT ( 'NONE',  ( 2.765633920072235075, 24.63872515616082737, -2.336989772644355590 ) ) ;
#10989=DIRECTION ( 'NONE',  ( 1.000000000000000000, -0.000000000000000000, -0.000000000000000000 ) ) ;
#10990=CARTESIAN_POINT ( 'NONE',  ( 1.039999999999996927, 20.02152543075374069, -19.67366047555508501 ) ) ;
#10992=B_SPLINE_CURVE_WITH_KNOTS ( 'NONE', 3,
 ( #6496, #11180, #7726, #11483, #9112, #8801 ),
 .UNSPECIFIED., .F., .F.,
 ( 4, 2, 4 ),
 ( 4.462636882221166670E-07, 0.001879885203074807814, 0.003759324142461393462 ),
 .UNSPECIFIED. ) ;
#10994=DIRECTION ( 'NONE',  ( 0.000000000000000000, 0.000000000000000000, 1.000000000000000000 ) ) ;
#11011=CARTESIAN_POINT ( 'NONE',  ( 0.1882238946918237121, 25.78859396478527799, -2.857713464478781162 ) ) ;
#11019=ORIENTED_EDGE ( 'NONE', *, *, #13983, .F. ) ;
#11020=CARTESIAN_POINT ( 'NONE',  ( 0.000000000000000000, 12.52067188844351442, 20.62201879784919001 ) ) ;
#11021=CARTESIAN_POINT ( 'NONE',  ( 0.02436607992776064838, 18.55949924794892780, 16.37294372382865504 ) ) ;
#11022=ORIENTED_EDGE ( 'NONE', *, *, #14334, .F. ) ;
#11025=CARTESIAN_POINT ( 'NONE',  ( 2.031033491000346913, -12.05173163741705444, -24.80232951178391332 ) ) ;
#11029=CARTESIAN_POINT ( 'NONE',  ( 1.394999999999999574, -27.68468304288262161, 4.633866840648820151 ) ) ;
#11030=EDGE_CURVE ( 'NONE', #12114, #8358, #8694, .T. ) ;
#11034=CARTESIAN_POINT ( 'NONE',  ( 1.394999999999999574, -12.96210679857803960, 24.89775460606827551 ) ) ;
#11037=AXIS2_PLACEMENT_3D ( 'NONE', #8657, #4059, #13346 ) ;
#11039=ORIENTED_EDGE ( 'NONE', *, *, #9111, .F. ) ;
#11043=CARTESIAN_POINT ( 'NONE',  ( 2.257825459230522913, -4.993157874727630841, -26.58873630738057159 ) ) ;
#11047=EDGE_CURVE ( 'NONE', #3303, #13854, #11708, .T. ) ;
#11049=CARTESIAN_POINT ( 'NONE',  ( 2.604434283110813819, 12.84444904262057818, -22.53097606932971075 ) ) ;
#11051=ORIENTED_EDGE ( 'NONE', *, *, #3467, .F. ) ;
#11053=CARTESIAN_POINT ( 'NONE',  ( 2.765633920072235519, 24.15498966839970052, -5.391175441198366336 ) ) ;
#11055=ORIENTED_EDGE ( 'NONE', *, *, #4883, .F. ) ;
#11056=EDGE_CURVE ( 'NONE', #4228, #9067, #3214, .T. ) ;
#11057=DIRECTION ( 'NONE',  ( -1.000000000000000000, -0.000000000000000000, -0.000000000000000000 ) ) ;
#11058=DIRECTION ( 'NONE',  ( 0.000000000000000000, 0.000000000000000000, 1.000000000000000000 ) ) ;
#11059=ORIENTED_EDGE ( 'NONE', *, *, #3847, .T. ) ;
#11064=FACE_OUTER_BOUND ( 'NONE', #14595, .T. ) ;
#11065=DIRECTION ( 'NONE',  ( -1.000000000000000000, -0.000000000000000000, -0.000000000000000000 ) ) ;
#11066=ADVANCED_FACE ( 'NONE', ( #8118 ), #15121, .T. ) ;
#11067=EDGE_CURVE ( 'NONE', #13334, #15084, #1844, .T. ) ;
#11069=ORIENTED_EDGE ( 'NONE', *, *, #3847, .F. ) ;
#11073=VERTEX_POINT ( 'NONE', #12573 ) ;
#11084=DIRECTION ( 'NONE',  ( 0.000000000000000000, 0.000000000000000000, 1.000000000000000000 ) ) ;
#11086=ADVANCED_FACE ( 'NONE', ( #12719 ), #3429, .F. ) ;
#11087=CARTESIAN_POINT ( 'NONE',  ( 0.02436607992775717893, -9.836394144775869819, 22.71065055754449347 ) ) ;
#11088=B_SPLINE_CURVE_WITH_KNOTS ( 'NONE', 3,
 ( #4125, #10107, #7654, #801 ),
 .UNSPECIFIED., .F., .F.,
 ( 4, 4 ),
 ( 2.324263106244698315E-07, 0.0006888201370294716810 ),
 .UNSPECIFIED. ) ;
#11090=CARTESIAN_POINT ( 'NONE',  ( 0.07186814640506923590, 12.74240566898984284, 21.92302674874967749 ) ) ;
#11098=FACE_OUTER_BOUND ( 'NONE', #4107, .T. ) ;
#11100=VERTEX_POINT ( 'NONE', #6888 ) ;
#11101=CYLINDRICAL_SURFACE ( 'NONE', #8547, 13.19999999999999929 ) ;
#11102=CARTESIAN_POINT ( 'NONE',  ( 1.039999999999997593, -12.52377138324241557, 25.12109765559648977 ) ) ;
#11108=EDGE_LOOP ( 'NONE', ( #8995, #12957, #14798, #9171, #12678, #8145 ) ) ;
#11109=CARTESIAN_POINT ( 'NONE',  ( 1.039999999999996483, -27.76164181293054511, 4.147968289691193355 ) ) ;
#11110=CYLINDRICAL_SURFACE ( 'NONE', #9279, 13.19999999999999929 ) ;
#11111=EDGE_CURVE ( 'NONE', #8828, #9867, #4759, .T. ) ;
#11112=CARTESIAN_POINT ( 'NONE',  ( 1.749999999999998002, -25.12109765559643648, -12.52377138324252570 ) ) ;
#11114=CARTESIAN_POINT ( 'NONE',  ( 2.790000000000077751, 24.22524813288762147, 2.133839912090885527 ) ) ;
#11115=CARTESIAN_POINT ( 'NONE',  ( 1.749999999999998002, 27.76164181293051669, 4.147968289691386090 ) ) ;
#11116=DIRECTION ( 'NONE',  ( 0.000000000000000000, 0.000000000000000000, 1.000000000000000000 ) ) ;
#11117=ORIENTED_EDGE ( 'NONE', *, *, #1816, .F. ) ;
#11118=CARTESIAN_POINT ( 'NONE',  ( 0.02436607992776325046, 16.37294372382858398, 18.55949924794898465 ) ) ;
#11124=VERTEX_POINT ( 'NONE', #13804 ) ;
#11126=CARTESIAN_POINT ( 'NONE',  ( 0.02436607992776455150, 5.391175441198956086, -24.15498966839956907 ) ) ;
#11128=DIRECTION ( 'NONE',  ( 0.000000000000000000, 0.000000000000000000, 1.000000000000000000 ) ) ;
#11132=CARTESIAN_POINT ( 'NONE',  ( 2.604434404052930141, 19.17825124759803401, -17.45907811351434802 ) ) ;
#11143=VERTEX_POINT ( 'NONE', #3573 ) ;
#11147=CARTESIAN_POINT ( 'NONE',  ( 2.789999999999999147, -20.62201879784904079, -12.52067188844374179 ) ) ;
#11151=DIRECTION ( 'NONE',  ( -1.000000000000000000, -0.000000000000000000, -0.000000000000000000 ) ) ;
#11152=CARTESIAN_POINT ( 'NONE',  ( 0.5321745227542252765, -19.66801664102716884, 18.57583492944412384 ) ) ;
#11153=EDGE_LOOP ( 'NONE', ( #7074, #9879, #8170, #13432, #802, #1173, #1276, #2219 ) ) ;
#11156=ADVANCED_FACE ( 'NONE', ( #5959 ), #3312, .T. ) ;
#11157=VECTOR ( 'NONE', #9968, 1000.000000000000000 ) ;
#11158=EDGE_CURVE ( 'NONE', #7278, #12816, #10667, .T. ) ;
#11162=ADVANCED_FACE ( 'NONE', ( #9346 ), #12941, .T. ) ;
#11163=CYLINDRICAL_SURFACE ( 'NONE', #2629, 13.20000000000000284 ) ;
#11166=PRODUCT ( 'short pitch roller chain wheel_s_iso_Chain wheel ISO - 20Z 05B-1 --20SA8.0N', 'short pitch roller chain wheel_s_iso_Chain wheel ISO - 20Z 05B-1 --20SA8.0N', '', ( #11192 ) ) ;
#11167=CARTESIAN_POINT ( 'NONE',  ( 0.7592463977762105021, -27.14986936243570526, -4.828194074574642336 ) ) ;
#11169=ORIENTED_EDGE ( 'NONE', *, *, #5143, .T. ) ;
#11173=EDGE_CURVE ( 'NONE', #11143, #4786, #10576, .T. ) ;
#11177=CARTESIAN_POINT ( 'NONE',  ( 1.749999999999998002, 4.147968289691286614, 27.76164181293053090 ) ) ;
#11179=ORIENTED_EDGE ( 'NONE', *, *, #3036, .F. ) ;
#11180=CARTESIAN_POINT ( 'NONE',  ( 2.030753616560877717, 12.05220173035473863, -24.80264696524870516 ) ) ;
#11181=DIRECTION ( 'NONE',  ( 0.000000000000000000, 1.000000000000000000, 1.099230717450651647E-14 ) ) ;
#11182=ORIENTED_EDGE ( 'NONE', *, *, #9106, .T. ) ;
#11184=CARTESIAN_POINT ( 'NONE',  ( 2.030753605846573162, -27.31305418910207905, -3.797885586973501759 ) ) ;
#11187=CARTESIAN_POINT ( 'NONE',  ( 0.7592463896980118365, -19.12676442129330212, -19.86438386685682644 ) ) ;
#11191=CARTESIAN_POINT ( 'NONE',  ( 2.789999999999999147, -5.535312321042557215, -23.48180575137735815 ) ) ;
#11192=PRODUCT_CONTEXT ( 'NONE', #13103, 'mechanical' ) ;
#11193=CARTESIAN_POINT ( 'NONE',  ( 2.765633920072239516, -2.336989772644097574, -24.63872515616085224 ) ) ;
#11196=DIRECTION ( 'NONE',  ( -1.000000000000000000, -0.000000000000000000, 0.000000000000000000 ) ) ;
#11197=ORIENTED_EDGE ( 'NONE', *, *, #7945, .F. ) ;
#11200=DIRECTION ( 'NONE',  ( 0.000000000000000000, 0.000000000000000000, 1.000000000000000000 ) ) ;
#11210=CIRCLE ( 'NONE', #13165, 24.12539914357697413 ) ;
#11211=ORIENTED_EDGE ( 'NONE', *, *, #7614, .T. ) ;
#11215=CARTESIAN_POINT ( 'NONE',  ( 0.07181525068722535710, -2.576941577947229334, -25.22524549359953383 ) ) ;
#11216=DIRECTION ( 'NONE',  ( -1.000000000000000000, -0.000000000000000000, -0.000000000000000000 ) ) ;
#11217=CARTESIAN_POINT ( 'NONE',  ( 0.02436607992776455150, -22.71065055754459650, 9.836394144775621129 ) ) ;
#11221=CARTESIAN_POINT ( 'NONE',  ( 0.000000000000000000, 5.535312321042724193, 23.48180575137730841 ) ) ;
#11225=EDGE_CURVE ( 'NONE', #13039, #9942, #7497, .T. ) ;
#11226=EDGE_LOOP ( 'NONE', ( #5088, #8252, #14645, #7304 ) ) ;
#11230=EDGE_LOOP ( 'NONE', ( #5428, #9732, #12842, #5054 ) ) ;
#11232=( LENGTH_UNIT ( ) NAMED_UNIT ( * ) SI_UNIT ( .MILLI., .METRE. ) );
#11241=DIRECTION ( 'NONE',  ( -1.000000000000000000, -0.000000000000000000, -0.000000000000000000 ) ) ;
#11242=CARTESIAN_POINT ( 'NONE',  ( 2.789999999999999147, -15.04425356660774682, 20.70663861606266209 ) ) ;
#11248=CARTESIAN_POINT ( 'NONE',  ( 2.765633920072236407, -2.336989772644440855, 24.63872515616082026 ) ) ;
#11249=VERTEX_POINT ( 'NONE', #15203 ) ;
#11252=EDGE_CURVE ( 'NONE', #1565, #11809, #2009, .T. ) ;
#11256=ORIENTED_EDGE ( 'NONE', *, *, #7954, .F. ) ;
#11260=ORIENTED_EDGE ( 'NONE', *, *, #10030, .T. ) ;
#11262=DIRECTION ( 'NONE',  ( 0.000000000000000000, 0.000000000000000000, 1.000000000000000000 ) ) ;
#11264=B_SPLINE_CURVE_WITH_KNOTS ( 'NONE', 3,
 ( #11109, #1590, #1442, #9965, #14665, #2818 ),
 .UNSPECIFIED., .F., .F.,
 ( 4, 2, 4 ),
 ( 4.462636732861906317E-07, 0.001879885066975067612, 0.003759323870276849028 ),
 .UNSPECIFIED. ) ;
#11265=CARTESIAN_POINT ( 'NONE',  ( 2.030753603471114666, 12.98165646470082457, 24.32906614999620132 ) ) ;
#11266=CARTESIAN_POINT ( 'NONE',  ( 2.718184749312774429, -25.22524549359948409, -2.576941577947671647 ) ) ;
#11267=B_SPLINE_CURVE_WITH_KNOTS ( 'NONE', 3,
 ( #856, #4324, #4553, #10314, #2014, #7929 ),
 .UNSPECIFIED., .F., .F.,
 ( 4, 2, 4 ),
 ( 2.586195665722962057E-07, 0.001878649493629687504, 0.003757040367692802973 ),
 .UNSPECIFIED. ) ;
#11270=CARTESIAN_POINT ( 'NONE',  ( 0.8291131470075423504, 24.44424927289185945, 12.96989951879416125 ) ) ;
#11272=DIRECTION ( 'NONE',  ( -1.000000000000000000, 0.000000000000000000, -0.000000000000000000 ) ) ;
#11277=EDGE_CURVE ( 'NONE', #14161, #4113, #3472, .T. ) ;
#11281=CYLINDRICAL_SURFACE ( 'NONE', #4476, 2.524999999999995914 ) ;
#11282=AXIS2_PLACEMENT_3D ( 'NONE', #5179, #4000, #3850 ) ;
#11284=ADVANCED_FACE ( 'NONE', ( #11098 ), #1656, .T. ) ;
#11285=B_SPLINE_CURVE_WITH_KNOTS ( 'NONE', 3,
 ( #11087, #9935, #6560, #10090, #4256, #8931 ),
 .UNSPECIFIED., .F., .F.,
 ( 4, 2, 4 ),
 ( 2.586195665723156346E-07, 0.001878649493629684468, 0.003757040367692796902 ),
 .UNSPECIFIED. ) ;
#11286=EDGE_LOOP ( 'NONE', ( #10336, #7535, #2210, #232, #2888, #11931, #10540 ) ) ;
#11287=CARTESIAN_POINT ( 'NONE',  ( 2.783025342027733995, 5.408388659524090869, 23.92335783895639523 ) ) ;
#11291=LINE ( 'NONE', #2143, #10977 ) ;
#11294=CARTESIAN_POINT ( 'NONE',  ( 0.000000000000000000, 0.000000000000000000, 0.000000000000000000 ) ) ;
#11296=DIRECTION ( 'NONE',  ( 0.000000000000000000, 0.000000000000000000, 1.000000000000000000 ) ) ;
#11297=DIRECTION ( 'NONE',  ( 0.000000000000000000, 0.000000000000000000, 1.000000000000000000 ) ) ;
#11298=CARTESIAN_POINT ( 'NONE',  ( 1.039999999999997815, 27.68468304288265003, -4.633866840648637186 ) ) ;
#11312=CARTESIAN_POINT ( 'NONE',  ( 0.1882238782932339760, -19.18368891937503307, 17.47009390565483855 ) ) ;
#11313=ORIENTED_EDGE ( 'NONE', *, *, #6102, .F. ) ;
#11314=CARTESIAN_POINT ( 'NONE',  ( 1.394999999999998685, 27.68468304288265358, -4.633866840648637186 ) ) ;
#11321=ORIENTED_EDGE ( 'NONE', *, *, #11173, .T. ) ;
#11322=ORIENTED_EDGE ( 'NONE', *, *, #5616, .T. ) ;
#11323=FACE_OUTER_BOUND ( 'NONE', #14857, .T. ) ;
#11325=CARTESIAN_POINT ( 'NONE',  ( 1.394999999999999574, -20.02152543075331081, -19.67366047555552555 ) ) ;
#11330=CARTESIAN_POINT ( 'NONE',  ( 8.000000000000000000, 0.000000000000000000, 0.000000000000000000 ) ) ;
#11333=CARTESIAN_POINT ( 'NONE',  ( 1.039999999999996039, 19.67366047555559305, -20.02152543075323976 ) ) ;
#11336=EDGE_CURVE ( 'NONE', #13280, #9067, #4016, .T. ) ;
#11338=EDGE_CURVE ( 'NONE', #4228, #4155, #522, .T. ) ;
#11340=CARTESIAN_POINT ( 'NONE',  ( 2.604434325169354913, 2.851997810081644769, 25.77772010606606301 ) ) ;
#11341=DIRECTION ( 'NONE',  ( -1.000000000000000000, 0.000000000000000000, 0.000000000000000000 ) ) ;
#11343=CARTESIAN_POINT ( 'NONE',  ( 0.1882239080259289210, -5.251266773802552024, 25.40949241676352344 ) ) ;
#11344=SHAPE_DEFINITION_REPRESENTATION ( #4819, #14263 ) ;
#11345=B_SPLINE_CURVE_WITH_KNOTS ( 'NONE', 3,
 ( #6956, #11710, #4897, #11634, #23, #7031 ),
 .UNSPECIFIED., .F., .F.,
 ( 4, 2, 4 ),
 ( 4.462636695653044375E-07, 0.001879885036799765685, 0.003759323809929966155 ),
 .UNSPECIFIED. ) ;
#11346=CARTESIAN_POINT ( 'NONE',  ( 2.789999999999999147, 18.28042085475301093, -15.74360496233361673 ) ) ;
#11350=AXIS2_PLACEMENT_3D ( 'NONE', #5691, #1146, #3673 ) ;
#11351=CARTESIAN_POINT ( 'NONE',  ( -10.00000000000000000, 0.000000000000000000, 0.000000000000000000 ) ) ;
#11355=ORIENTED_EDGE ( 'NONE', *, *, #8116, .T. ) ;
#11358=CARTESIAN_POINT ( 'NONE',  ( 2.789999999999999591, 12.51294990530046292, -20.85230829256839513 ) ) ;
#11361=CARTESIAN_POINT ( 'NONE',  ( 2.789999999999999147, 19.64056340710875048, -14.55412442567624609 ) ) ;
#11370=VERTEX_POINT ( 'NONE', #11177 ) ;
#11374=VERTEX_POINT ( 'NONE', #408 ) ;
#11376=ORIENTED_EDGE ( 'NONE', *, *, #10150, .F. ) ;
#11377=CARTESIAN_POINT ( 'NONE',  ( 2.030753605846571386, 27.31305418910209326, 3.797885586973312133 ) ) ;
#11381=EDGE_LOOP ( 'NONE', ( #206, #7865, #11730, #8841 ) ) ;
#11383=CARTESIAN_POINT ( 'NONE',  ( 0.7589665089996495695, 24.80232951178378187, 12.05173163741731202 ) ) ;
#11384=DIRECTION ( 'NONE',  ( 0.000000000000000000, 0.000000000000000000, 1.000000000000000000 ) ) ;
#11385=LINE ( 'NONE', #14720, #11598 ) ;
#11390=CARTESIAN_POINT ( 'NONE',  ( 0.02436607992776325046, -24.15498966839958683, -5.391175441198872598 ) ) ;
#11392=VERTEX_POINT ( 'NONE', #12488 ) ;
#11402=B_SPLINE_CURVE_WITH_KNOTS ( 'NONE', 3,
 ( #6586, #11184, #13795, #13645, #11266, #6804 ),
 .UNSPECIFIED., .F., .F.,
 ( 4, 2, 4 ),
 ( 4.462636732861209103E-07, 0.001879885066975070214, 0.003759323870276854232 ),
 .UNSPECIFIED. ) ;
#11403=DIRECTION ( 'NONE',  ( -1.000000000000000000, -0.000000000000000000, 0.000000000000000000 ) ) ;
#11409=ADVANCED_FACE ( 'NONE', ( #6571 ), #6270, .T. ) ;
#11410=VERTEX_POINT ( 'NONE', #12556 ) ;
#11415=CARTESIAN_POINT ( 'NONE',  ( 2.789999999999999147, 24.04302995059966364, 1.991882183130384121 ) ) ;
#11418=ADVANCED_FACE ( 'NONE', ( #10102 ), #12405, .F. ) ;
#11420=CARTESIAN_POINT ( 'NONE',  ( 1.749999999999998002, 0.000000000000000000, 0.000000000000000000 ) ) ;
#11421=AXIS2_PLACEMENT_3D ( 'NONE', #13058, #70, #1313 ) ;
#11422=EDGE_CURVE ( 'NONE', #6526, #2853, #1350, .T. ) ;
#11423=CARTESIAN_POINT ( 'NONE',  ( -7.682766964941417370E-14, -9.515416771311052457, -22.38018801136486502 ) ) ;
#11424=DIRECTION ( 'NONE',  ( 0.000000000000000000, 0.000000000000000000, 1.000000000000000000 ) ) ;
#11426=CYLINDRICAL_SURFACE ( 'NONE', #1877, 28.06981291497571362 ) ;
#11427=CARTESIAN_POINT ( 'NONE',  ( 1.749999999999998002, 4.633866840649310426, -27.68468304288254345 ) ) ;
#11429=VERTEX_POINT ( 'NONE', #1884 ) ;
#11432=DIRECTION ( 'NONE',  ( 0.000000000000000000, 0.000000000000000000, 1.000000000000000000 ) ) ;
#11435=CARTESIAN_POINT ( 'NONE',  ( 8.000000000000000000, 0.000000000000000000, 0.000000000000000000 ) ) ;
#11436=DIRECTION ( 'NONE',  ( -1.000000000000000000, -0.000000000000000000, -0.000000000000000000 ) ) ;
#11447=STYLED_ITEM ( 'NONE', ( #13916 ), #1226 ) ;
#11449=ADVANCED_FACE ( 'NONE', ( #4265 ), #6651, .T. ) ;
#11450=( NAMED_UNIT ( * ) PLANE_ANGLE_UNIT ( ) SI_UNIT ( $, .RADIAN. ) );
#11451=B_SPLINE_CURVE_WITH_KNOTS ( 'NONE', 3,
 ( #11147, #1783, #8847, #6318 ),
 .UNSPECIFIED., .F., .F.,
 ( 4, 4 ),
 ( 0.005258139959819238193, 0.005342776758202895035 ),
 .UNSPECIFIED. ) ;
#11455=LINE ( 'NONE', #1008, #1892 ) ;
#11457=FACE_OUTER_BOUND ( 'NONE', #8038, .T. ) ;
#11461=CIRCLE ( 'NONE', #4614, 2.524999999999995914 ) ;
#11466=CARTESIAN_POINT ( 'NONE',  ( 0.000000000000000000, -7.909232158574988958, 24.34211360614297348 ) ) ;
#11467=EDGE_CURVE ( 'NONE', #6969, #14971, #3115, .T. ) ;
#11468=VECTOR ( 'NONE', #10883, 1000.000000000000000 ) ;
#11469=ORIENTED_EDGE ( 'NONE', *, *, #15112, .T. ) ;
#11475=ORIENTED_EDGE ( 'NONE', *, *, #6088, .T. ) ;
#11476=AXIS2_PLACEMENT_3D ( 'NONE', #9032, #5504, #4198 ) ;
#11479=EDGE_CURVE ( 'NONE', #14329, #9661, #1466, .T. ) ;
#11483=CARTESIAN_POINT ( 'NONE',  ( 2.601776144743014108, 10.68696068830440815, -23.64332819722370260 ) ) ;
#11484=CARTESIAN_POINT ( 'NONE',  ( 2.789999999999999147, 12.52067188844351442, 20.62201879784917935 ) ) ;
#11485=VECTOR ( 'NONE', #6957, 1000.000000000000000 ) ;
#11486=ORIENTED_EDGE ( 'NONE', *, *, #14408, .T. ) ;
#11490=CARTESIAN_POINT ( 'NONE',  ( 1.749999999999998002, 4.147968289691286614, 27.76164181293053090 ) ) ;
#11492=EDGE_CURVE ( 'NONE', #11124, #1547, #4801, .T. ) ;
#11499=ORIENTED_EDGE ( 'NONE', *, *, #4556, .F. ) ;
#11501=DIRECTION ( 'NONE',  ( 0.000000000000000000, 0.000000000000000000, 1.000000000000000000 ) ) ;
#11510=CARTESIAN_POINT ( 'NONE',  ( 2.789999999999999147, -20.70663861606260170, -15.04425356660783031 ) ) ;
#11514=CARTESIAN_POINT ( 'NONE',  ( 0.000000000000000000, -15.04425356660744839, -20.70663861606288236 ) ) ;
#11515=CARTESIAN_POINT ( 'NONE',  ( 2.788134175425139194, -20.90825775245756191, -12.51925356660783528 ) ) ;
#11519=VECTOR ( 'NONE', #9608, 1000.000000000000000 ) ;
#11526=ORIENTED_EDGE ( 'NONE', *, *, #9004, .F. ) ;
#11536=B_SPLINE_CURVE_WITH_KNOTS ( 'NONE', 3,
 ( #3974, #3903, #7592, #572, #14582, #9882 ),
 .UNSPECIFIED., .F., .F.,
 ( 4, 2, 4 ),
 ( 4.462636695690012598E-07, 0.001879885036799766119, 0.003759323809929963553 ),
 .UNSPECIFIED. ) ;
#11548=VERTEX_POINT ( 'NONE', #14013 ) ;
#11549=ORIENTED_EDGE ( 'NONE', *, *, #7856, .T. ) ;
#11553=ORIENTED_EDGE ( 'NONE', *, *, #6049, .T. ) ;
#11555=CARTESIAN_POINT ( 'NONE',  ( 0.000000000000000000, -12.52067188844364587, 20.62201879784910119 ) ) ;
#11559=ORIENTED_EDGE ( 'NONE', *, *, #13946, .T. ) ;
#11566=CARTESIAN_POINT ( 'NONE',  ( 2.789999999999999147, 23.17675759782029843, 7.772527002114834715 ) ) ;
#11568=CARTESIAN_POINT ( 'NONE',  ( 0.5321745407694777885, -4.993157874728001211, 26.58873630738050409 ) ) ;
#11570=CARTESIAN_POINT ( 'NONE',  ( 0.02436607992776325046, -18.55949924794904504, 16.37294372382852004 ) ) ;
#11571=VERTEX_POINT ( 'NONE', #75 ) ;
#11572=CARTESIAN_POINT ( 'NONE',  ( 2.789999999999999147, 14.18181402625742749, 19.91106274590519121 ) ) ;
#11573=CARTESIAN_POINT ( 'NONE',  ( 0.02436607992776238310, -12.59161484032927092, 21.30679549418627161 ) ) ;
#11574=CARTESIAN_POINT ( 'NONE',  ( 1.749999999999998002, -12.96210679857767367, -24.89775460606847091 ) ) ;
#11578=EDGE_CURVE ( 'NONE', #8828, #11849, #2840, .T. ) ;
#11582=VERTEX_POINT ( 'NONE', #10627 ) ;
#11587=DIRECTION ( 'NONE',  ( -1.000000000000000000, -0.000000000000000000, -0.000000000000000000 ) ) ;
#11590=AXIS2_PLACEMENT_3D ( 'NONE', #10875, #8409, #3968 ) ;
#11592=FACE_OUTER_BOUND ( 'NONE', #6842, .T. ) ;
#11598=VECTOR ( 'NONE', #12478, 1000.000000000000000 ) ;
#11599=ORIENTED_EDGE ( 'NONE', *, *, #4306, .T. ) ;
#11600=ORIENTED_EDGE ( 'NONE', *, *, #8964, .T. ) ;
#11603=ADVANCED_FACE ( 'NONE', ( #4723 ), #11617, .T. ) ;
#11606=DIRECTION ( 'NONE',  ( 0.000000000000000000, 0.000000000000000000, 1.000000000000000000 ) ) ;
#11612=ORIENTED_EDGE ( 'NONE', *, *, #2538, .F. ) ;
#11617=CYLINDRICAL_SURFACE ( 'NONE', #15111, 13.20000000000000284 ) ;
#11618=EDGE_CURVE ( 'NONE', #8456, #12831, #6194, .T. ) ;
#11622=CARTESIAN_POINT ( 'NONE',  ( 2.765633920072238183, -18.55949924794904504, 16.37294372382852004 ) ) ;
#11628=VERTEX_POINT ( 'NONE', #2552 ) ;
#11632=ADVANCED_FACE ( 'NONE', ( #5942 ), #2257, .F. ) ;
#11634=CARTESIAN_POINT ( 'NONE',  ( 2.601776096565022289, 22.54313264455032240, -12.84621645676820201 ) ) ;
#11636=LINE ( 'NONE', #7265, #5626 ) ;
#11637=CIRCLE ( 'NONE', #3544, 28.06981291497571007 ) ;
#11643=DIRECTION ( 'NONE',  ( -1.000000000000000000, -0.000000000000000000, 0.000000000000000000 ) ) ;
#11649=DIRECTION ( 'NONE',  ( 0.000000000000000000, 0.000000000000000000, 1.000000000000000000 ) ) ;
#11657=CARTESIAN_POINT ( 'NONE',  ( 2.780931166827226519, -21.10834851580694504, -12.54305517365643929 ) ) ;
#11659=AXIS2_PLACEMENT_3D ( 'NONE', #3032, #12624, #9028 ) ;
#11670=AXIS2_PLACEMENT_3D ( 'NONE', #13153, #13383, #1635 ) ;
#11679=AXIS2_PLACEMENT_3D ( 'NONE', #8289, #7296, #5768 ) ;
#11683=CARTESIAN_POINT ( 'NONE',  ( 0.000000000000000000, -22.25075486061732732, -9.324097380959701198 ) ) ;
#11685=VECTOR ( 'NONE', #2315, 1000.000000000000000 ) ;
#11686=VERTEX_POINT ( 'NONE', #1552 ) ;
#11687=CARTESIAN_POINT ( 'NONE',  ( 2.031033467310412011, -24.32849926382740335, -12.98167595241049277 ) ) ;
#11688=DIRECTION ( 'NONE',  ( 0.000000000000000000, 0.000000000000000000, 1.000000000000000000 ) ) ;
#11689=ORIENTED_EDGE ( 'NONE', *, *, #10755, .T. ) ;
#11695=ORIENTED_EDGE ( 'NONE', *, *, #12875, .T. ) ;
#11697=CARTESIAN_POINT ( 'NONE',  ( 6.560148031203755073E-16, 23.69843731927177544, -5.456805104200854295 ) ) ;
#11699=CARTESIAN_POINT ( 'NONE',  ( 2.765633920072235519, 18.55949924794892780, 16.37294372382865504 ) ) ;
#11702=AXIS2_PLACEMENT_3D ( 'NONE', #11361, #832, #12587 ) ;
#11708=B_SPLINE_CURVE_WITH_KNOTS ( 'NONE', 3,
 ( #6667, #10343, #2047, #888 ),
 .UNSPECIFIED., .F., .F.,
 ( 4, 4 ),
 ( 4.462636695653741059E-07, 0.0004963285629696456008 ),
 .UNSPECIFIED. ) ;
#11710=CARTESIAN_POINT ( 'NONE',  ( 2.030753603471114221, 24.32906614999634698, -12.98165646470055634 ) ) ;
#11713=ADVANCED_FACE ( 'NONE', ( #6324 ), #9716, .T. ) ;
#11715=DIRECTION ( 'NONE',  ( -1.000000000000000000, -0.000000000000000000, -0.000000000000000000 ) ) ;
#11716=DIRECTION ( 'NONE',  ( -1.000000000000000000, -0.000000000000000000, -0.000000000000000000 ) ) ;
#11721=DIRECTION ( 'NONE',  ( 0.000000000000000000, 0.000000000000000000, 1.000000000000000000 ) ) ;
#11722=VERTEX_POINT ( 'NONE', #2640 ) ;
#11724=DIRECTION ( 'NONE',  ( 0.000000000000000000, 0.000000000000000000, 1.000000000000000000 ) ) ;
#11725=CARTESIAN_POINT ( 'NONE',  ( 1.039999999999996927, -25.12109765559644714, -12.52377138324250438 ) ) ;
#11726=CARTESIAN_POINT ( 'NONE',  ( 2.030753605846573606, -3.797885586973408056, 27.31305418910209326 ) ) ;
#11730=ORIENTED_EDGE ( 'NONE', *, *, #6985, .T. ) ;
#11731=ADVANCED_FACE ( 'NONE', ( #2863 ), #7559, .F. ) ;
#11742=B_SPLINE_CURVE_WITH_KNOTS ( 'NONE', 3,
 ( #8473, #13163, #8559, #12010 ),
 .UNSPECIFIED., .F., .F.,
 ( 4, 4 ),
 ( 2.324263106244728226E-07, 0.0006888201370294799210 ),
 .UNSPECIFIED. ) ;
#11743=CARTESIAN_POINT ( 'NONE',  ( 0.7589665283900980386, -27.31260702007172725, -3.797536611356600034 ) ) ;
#11745=EDGE_CURVE ( 'NONE', #8704, #5734, #392, .T. ) ;
#11753=CARTESIAN_POINT ( 'NONE',  ( 1.039999999999997593, -24.89775460606841051, 12.96210679857778025 ) ) ;
#11756=ORIENTED_EDGE ( 'NONE', *, *, #6899, .T. ) ;
#11759=DIRECTION ( 'NONE',  ( 0.000000000000000000, 0.000000000000000000, 1.000000000000000000 ) ) ;
#11762=CIRCLE ( 'NONE', #5413, 24.12539914357697413 ) ;
#11763=CARTESIAN_POINT ( 'NONE',  ( 0.02436607992776064838, 5.391175441198615914, 24.15498966839965078 ) ) ;
#11764=ORIENTED_EDGE ( 'NONE', *, *, #6970, .T. ) ;
#11766=AXIS2_PLACEMENT_3D ( 'NONE', #14979, #12428, #12511 ) ;
#11768=FACE_OUTER_BOUND ( 'NONE', #963, .T. ) ;
#11770=DIRECTION ( 'NONE',  ( 0.000000000000000000, 0.000000000000000000, 1.000000000000000000 ) ) ;
#11778=CARTESIAN_POINT ( 'NONE',  ( 0.07181523211953061425, 10.24584646439538993, 23.19431517146936983 ) ) ;
#11782=CARTESIAN_POINT ( 'NONE',  ( 1.749999999999998002, -20.02152543075331081, -19.67366047555553266 ) ) ;
#11783=EDGE_LOOP ( 'NONE', ( #11834, #7800, #6422, #382 ) ) ;
#11784=ORIENTED_EDGE ( 'NONE', *, *, #9551, .T. ) ;
#11786=LINE ( 'NONE', #14101, #14699 ) ;
#11791=CARTESIAN_POINT ( 'NONE',  ( 0.006974693931642885793, -18.43727551351043203, 16.17543236987982525 ) ) ;
#11794=CYLINDRICAL_SURFACE ( 'NONE', #1770, 13.19999999999999929 ) ;
#11796=CARTESIAN_POINT ( 'NONE',  ( 0.006931069955679000985, 16.17493693894905959, -18.43696893154741190 ) ) ;
#11797=ADVANCED_FACE ( 'NONE', ( #6554 ), #7261, .T. ) ;
#11800=EDGE_LOOP ( 'NONE', ( #1472, #10479, #10356, #793, #4983, #1177 ) ) ;
#11809=VERTEX_POINT ( 'NONE', #12387 ) ;
#11815=LINE ( 'NONE', #8009, #8539 ) ;
#11818=EDGE_CURVE ( 'NONE', #11571, #4492, #12961, .T. ) ;
#11819=ORIENTED_EDGE ( 'NONE', *, *, #10100, .T. ) ;
#11822=VERTEX_POINT ( 'NONE', #366 ) ;
#11823=EDGE_LOOP ( 'NONE', ( #4151, #12599, #7364, #13250 ) ) ;
#11826=EDGE_CURVE ( 'NONE', #5700, #672, #14082, .T. ) ;
#11831=ORIENTED_EDGE ( 'NONE', *, *, #8472, .F. ) ;
#11834=ORIENTED_EDGE ( 'NONE', *, *, #3432, .T. ) ;
#11835=CARTESIAN_POINT ( 'NONE',  ( 1.749999999999998002, -24.89775460606821866, -12.96210679857815684 ) ) ;
#11836=DIRECTION ( 'NONE',  ( 1.000000000000000000, 0.000000000000000000, -0.000000000000000000 ) ) ;
#11838=ORIENTED_EDGE ( 'NONE', *, *, #4999, .F. ) ;
#11845=ORIENTED_EDGE ( 'NONE', *, *, #11111, .F. ) ;
#11848=CYLINDRICAL_SURFACE ( 'NONE', #14153, 13.19999999999999929 ) ;
#11849=VERTEX_POINT ( 'NONE', #9899 ) ;
#11852=CARTESIAN_POINT ( 'NONE',  ( 0.1882238782932349475, -17.47009390565476750, -19.18368891937510412 ) ) ;
#11853=DIRECTION ( 'NONE',  ( -1.000000000000000000, -0.000000000000000000, -0.000000000000000000 ) ) ;
#11855=DIRECTION ( 'NONE',  ( 0.000000000000000000, -1.374038396813314756E-15, -1.000000000000000000 ) ) ;
#11856=DIRECTION ( 'NONE',  ( -1.000000000000000000, -0.000000000000000000, -0.000000000000000000 ) ) ;
#11859=DIRECTION ( 'NONE',  ( -1.000000000000000000, -0.000000000000000000, -0.000000000000000000 ) ) ;
#11861=EDGE_CURVE ( 'NONE', #5744, #389, #7756, .T. ) ;
#11862=EDGE_LOOP ( 'NONE', ( #5983, #12078, #10748, #6822, #9418, #8845 ) ) ;
#11863=CARTESIAN_POINT ( 'NONE',  ( 2.718184757033982990, 18.89296398180191616, 16.91181672897740640 ) ) ;
#11864=FACE_OUTER_BOUND ( 'NONE', #10939, .T. ) ;
#11865=CARTESIAN_POINT ( 'NONE',  ( 1.749999999999998002, 27.68468304288265358, -4.633866840648635410 ) ) ;
#11866=CARTESIAN_POINT ( 'NONE',  ( 2.257825467309740208, -3.467596033028475855, 26.83036154824992892 ) ) ;
#11869=B_SPLINE_CURVE_WITH_KNOTS ( 'NONE', 3,
 ( #1790, #9930, #5421, #12390 ),
 .UNSPECIFIED., .F., .F.,
 ( 4, 4 ),
 ( 0.005258214619651976202, 0.005948481662034167325 ),
 .UNSPECIFIED. ) ;
#11875=CARTESIAN_POINT ( 'NONE',  ( 2.789999999999999147, 24.63872515616082737, 2.336989772644355146 ) ) ;
#11885=DIRECTION ( 'NONE',  ( -1.000000000000000000, -0.000000000000000000, -0.000000000000000000 ) ) ;
#11888=EDGE_LOOP ( 'NONE', ( #11059, #15094, #12417, #8549 ) ) ;
#11891=AXIS2_PLACEMENT_3D ( 'NONE', #12364, #767, #11128 ) ;
#11894=EDGE_LOOP ( 'NONE', ( #2745, #2223, #10737, #8968, #2542, #719 ) ) ;
#11897=DIRECTION ( 'NONE',  ( -1.000000000000000000, -0.000000000000000000, 0.000000000000000000 ) ) ;
#11900=CARTESIAN_POINT ( 'NONE',  ( 2.604434514863826156, 10.67816411292164958, 23.63475234378986300 ) ) ;
#11903=DIRECTION ( 'NONE',  ( 0.000000000000000000, 0.000000000000000000, 1.000000000000000000 ) ) ;
#11904=EDGE_CURVE ( 'NONE', #7241, #6140, #129, .T. ) ;
#11912=DIRECTION ( 'NONE',  ( -1.000000000000000000, -0.000000000000000000, -0.000000000000000000 ) ) ;
#11915=AXIS2_PLACEMENT_3D ( 'NONE', #3921, #8599, #1690 ) ;
#11918=ORIENTED_EDGE ( 'NONE', *, *, #13585, .F. ) ;
#11919=LINE ( 'NONE', #4953, #74 ) ;
#11923=AXIS2_PLACEMENT_3D ( 'NONE', #15001, #9078, #7851 ) ;
#11926=CIRCLE ( 'NONE', #649, 24.12539914357697768 ) ;
#11927=CARTESIAN_POINT ( 'NONE',  ( 2.789999999999999147, 15.04425356660790136, -20.70663861606255196 ) ) ;
#11929=( GEOMETRIC_REPRESENTATION_CONTEXT ( 3 ) GLOBAL_UNCERTAINTY_ASSIGNED_CONTEXT ( ( #8848 ) ) GLOBAL_UNIT_ASSIGNED_CONTEXT ( ( #1546, #11450, #3089 ) ) REPRESENTATION_CONTEXT ( 'NONE', 'WORKASPACE' ) );
#11931=ORIENTED_EDGE ( 'NONE', *, *, #4513, .F. ) ;
#11934=ORIENTED_EDGE ( 'NONE', *, *, #1939, .F. ) ;
#11939=CARTESIAN_POINT ( 'NONE',  ( 0.7592463977762118343, 4.828194074574732930, -27.14986936243569460 ) ) ;
#11940=DIRECTION ( 'NONE',  ( 0.000000000000000000, 0.000000000000000000, 1.000000000000000000 ) ) ;
#11942=CIRCLE ( 'NONE', #13668, 28.06981291497571007 ) ;
#11947=CARTESIAN_POINT ( 'NONE',  ( 0.0003207540509381473352, -20.70663861606275447, -12.51925356660783528 ) ) ;
#11959=CARTESIAN_POINT ( 'NONE',  ( 2.789999999999999147, -15.74360496233394002, 18.28042085475272671 ) ) ;
#11962=ORIENTED_EDGE ( 'NONE', *, *, #8689, .T. ) ;
#11964=CARTESIAN_POINT ( 'NONE',  ( 0.000000000000000000, 18.28042085475300382, -15.74360496233363804 ) ) ;
#11973=EDGE_LOOP ( 'NONE', ( #223, #1650, #15035, #775 ) ) ;
#11974=ORIENTED_EDGE ( 'NONE', *, *, #11336, .F. ) ;
#11975=VERTEX_POINT ( 'NONE', #13521 ) ;
#11979=DIRECTION ( 'NONE',  ( -1.000000000000000000, -0.000000000000000000, -0.000000000000000000 ) ) ;
#11980=CARTESIAN_POINT ( 'NONE',  ( 0.006931069955678739909, -16.17493693894892104, 18.43696893154752914 ) ) ;
#11982=ADVANCED_FACE ( 'NONE', ( #8521 ), #2989, .T. ) ;
#11987=CARTESIAN_POINT ( 'NONE',  ( 2.789999999999999147, 15.04425356660790136, -20.70663861606255196 ) ) ;
#11988=B_SPLINE_CURVE_WITH_KNOTS ( 'NONE', 3,
 ( #6378, #450, #12127, #12359, #6303, #1618 ),
 .UNSPECIFIED., .F., .F.,
 ( 4, 2, 4 ),
 ( 0.0004963285629696456008, 0.002127826186449799806, 0.003759323809929954012 ),
 .UNSPECIFIED. ) ;
#11989=EDGE_CURVE ( 'NONE', #4328, #15073, #9674, .T. ) ;
#11991=ORIENTED_EDGE ( 'NONE', *, *, #12045, .T. ) ;
#11993=AXIS2_PLACEMENT_3D ( 'NONE', #815, #5522, #7898 ) ;
#11994=FACE_OUTER_BOUND ( 'NONE', #10819, .T. ) ;
#11999=ORIENTED_EDGE ( 'NONE', *, *, #842, .F. ) ;
#12003=AXIS2_PLACEMENT_3D ( 'NONE', #2704, #9909, #10994 ) ;
#12006=CARTESIAN_POINT ( 'NONE',  ( 1.749999999999998002, -27.68468304288255766, -4.633866840649213614 ) ) ;
#12008=CARTESIAN_POINT ( 'NONE',  ( 0.02436607992775978102, 2.336989772644613161, -24.63872515616080250 ) ) ;
#12009=EDGE_CURVE ( 'NONE', #1997, #85, #1627, .T. ) ;
#12010=CARTESIAN_POINT ( 'NONE',  ( 2.789999999999999147, -18.28042085475266276, -15.74360496233401996 ) ) ;
#12011=ORIENTED_EDGE ( 'NONE', *, *, #8072, .F. ) ;
#12012=CARTESIAN_POINT ( 'NONE',  ( 2.765633920072239516, -24.63872515616084513, 2.336989772644183283 ) ) ;
#12017=CIRCLE ( 'NONE', #741, 24.12539914357697413 ) ;
#12021=CARTESIAN_POINT ( 'NONE',  ( 0.02436607992776455150, 5.391175441198956086, -24.15498966839956907 ) ) ;
#12027=CYLINDRICAL_SURFACE ( 'NONE', #9793, 2.524999999999995914 ) ;
#12034=DIRECTION ( 'NONE',  ( 0.000000000000000000, -0.5877852522924743583, 0.8090169943749465631 ) ) ;
#12035=CARTESIAN_POINT ( 'NONE',  ( 2.783025306068355853, -16.17543236988001354, 18.43727551351025795 ) ) ;
#12038=CARTESIAN_POINT ( 'NONE',  ( 50.00050000000000239, 4.898587196589412829E-16, -4.000000000000000000 ) ) ;
#12042=CARTESIAN_POINT ( 'NONE',  ( 1.960886852992457241, 24.44424927289185945, 12.96989951879416125 ) ) ;
#12043=B_SPLINE_CURVE_WITH_KNOTS ( 'NONE', 3,
 ( #11112, #1676, #12341, #8653, #14584, #7371 ),
 .UNSPECIFIED., .F., .F.,
 ( 4, 2, 4 ),
 ( 4.462636882155291330E-07, 0.001879885203074804561, 0.003759324142461393896 ),
 .UNSPECIFIED. ) ;
#12044=CARTESIAN_POINT ( 'NONE',  ( 1.039999999999996039, 24.89775460606832169, 12.96210679857795256 ) ) ;
#12045=EDGE_CURVE ( 'NONE', #4786, #3966, #6390, .T. ) ;
#12047=CARTESIAN_POINT ( 'NONE',  ( 0.000000000000000000, 15.04425356660790136, -20.70663861606255196 ) ) ;
#12048=DIRECTION ( 'NONE',  ( 0.000000000000000000, 0.000000000000000000, 1.000000000000000000 ) ) ;
#12049=EDGE_LOOP ( 'NONE', ( #10549, #9750, #9311, #7753, #7495, #2384 ) ) ;
#12052=FACE_OUTER_BOUND ( 'NONE', #8989, .T. ) ;
#12055=CARTESIAN_POINT ( 'NONE',  ( 8.000000000000000000, 0.000000000000000000, 0.000000000000000000 ) ) ;
#12057=CARTESIAN_POINT ( 'NONE',  ( 2.789999999999999147, 24.15498966839970052, -5.391175441198366336 ) ) ;
#12059=CARTESIAN_POINT ( 'NONE',  ( 0.000000000000000000, -1.991882183130148087, -24.04302995059968140 ) ) ;
#12061=EDGE_CURVE ( 'NONE', #13607, #7326, #4732, .T. ) ;
#12063=VERTEX_POINT ( 'NONE', #6901 ) ;
#12064=ORIENTED_EDGE ( 'NONE', *, *, #10617, .T. ) ;
#12065=LINE ( 'NONE', #2779, #4561 ) ;
#12066=CARTESIAN_POINT ( 'NONE',  ( 2.789999999999999147, 25.59481291497571220, 0.000000000000000000 ) ) ;
#12077=DIRECTION ( 'NONE',  ( -1.000000000000000000, -0.000000000000000000, 0.000000000000000000 ) ) ;
#12078=ORIENTED_EDGE ( 'NONE', *, *, #1667, .F. ) ;
#12081=VERTEX_POINT ( 'NONE', #3369 ) ;
#12087=ORIENTED_EDGE ( 'NONE', *, *, #8691, .T. ) ;
#12089=CARTESIAN_POINT ( 'NONE',  ( 2.262072769566604080, -11.57956866523201178, -24.43806413951687873 ) ) ;
#12090=ADVANCED_FACE ( 'NONE', ( #8058 ), #4226, .T. ) ;
#12094=CYLINDRICAL_SURFACE ( 'NONE', #12494, 13.19999999999999929 ) ;
#12096=CARTESIAN_POINT ( 'NONE',  ( 2.789999999999999147, 15.74360496233381390, 18.28042085475283685 ) ) ;
#12098=LINE ( 'NONE', #11034, #5639 ) ;
#12100=ADVANCED_FACE ( 'NONE', ( #5462 ), #637, .T. ) ;
#12102=ORIENTED_EDGE ( 'NONE', *, *, #4419, .F. ) ;
#12104=VERTEX_POINT ( 'NONE', #13356 ) ;
#12106=LINE ( 'NONE', #7369, #6322 ) ;
#12111=ORIENTED_EDGE ( 'NONE', *, *, #6239, .T. ) ;
#12113=CARTESIAN_POINT ( 'NONE',  ( 2.789999999999999147, 0.000000000000000000, 0.000000000000000000 ) ) ;
#12114=VERTEX_POINT ( 'NONE', #5085 ) ;
#12117=CARTESIAN_POINT ( 'NONE',  ( 2.257825477245766432, -18.57583492944434411, 19.66801664102697345 ) ) ;
#12120=AXIS2_PLACEMENT_3D ( 'NONE', #9309, #999, #15003 ) ;
#12123=VERTEX_POINT ( 'NONE', #8520 ) ;
#12126=CARTESIAN_POINT ( 'NONE',  ( 2.789999999999999147, 24.04302995059966364, -1.991882183130384121 ) ) ;
#12127=CARTESIAN_POINT ( 'NONE',  ( 0.4314184204727332661, 23.43037373958377501, 12.94152279942384709 ) ) ;
#12131=AXIS2_PLACEMENT_3D ( 'NONE', #9843, #5240, #3931 ) ;
#12140=TOROIDAL_SURFACE ( 'NONE', #5307, 24.12539914357697768, 8.000000000000000000 ) ;
#12150=VERTEX_POINT ( 'NONE', #6373 ) ;
#12152=LINE ( 'NONE', #11314, #13366 ) ;
#12153=ADVANCED_FACE ( 'NONE', ( #2761 ), #9834, .F. ) ;
#12155=LINE ( 'NONE', #5196, #13601 ) ;
#12160=AXIS2_PLACEMENT_3D ( 'NONE', #7677, #5006, #5683 ) ;
#12161=EDGE_CURVE ( 'NONE', #447, #13730, #4337, .T. ) ;
#12167=B_SPLINE_CURVE_WITH_KNOTS ( 'NONE', 3,
 ( #6248, #14491, #3871, #8468, #8553, #7339 ),
 .UNSPECIFIED., .F., .F.,
 ( 4, 2, 4 ),
 ( 4.462636695653741059E-07, 0.001879885036799761131, 0.003759323809929956614 ),
 .UNSPECIFIED. ) ;
#12170=EDGE_CURVE ( 'NONE', #910, #7573, #9971, .T. ) ;
#12171=FACE_OUTER_BOUND ( 'NONE', #2922, .T. ) ;
#12173=ORIENTED_EDGE ( 'NONE', *, *, #1854, .T. ) ;
#12179=B_SPLINE_CURVE_WITH_KNOTS ( 'NONE', 3,
 ( #8980, #3227, #15057, #8062, #3155, #12737 ),
 .UNSPECIFIED., .F., .F.,
 ( 4, 2, 4 ),
 ( 2.586195665736120714E-07, 0.001878649493629689022, 0.003757040367692804708 ),
 .UNSPECIFIED. ) ;
#12180=DIRECTION ( 'NONE',  ( 0.000000000000000000, 0.000000000000000000, -1.000000000000000000 ) ) ;
#12188=VERTEX_POINT ( 'NONE', #4153 ) ;
#12190=CARTESIAN_POINT ( 'NONE',  ( 0.02436607992776064838, 5.391175441198615914, 24.15498966839965078 ) ) ;
#12197=CARTESIAN_POINT ( 'NONE',  ( 2.789999999999999147, 12.52067188844351442, 20.62201879784917935 ) ) ;
#12198=EDGE_LOOP ( 'NONE', ( #2303, #1879, #1548, #4373, #5952, #7689 ) ) ;
#12201=CARTESIAN_POINT ( 'NONE',  ( 1.749999999999998002, 0.000000000000000000, 0.000000000000000000 ) ) ;
#12205=ORIENTED_EDGE ( 'NONE', *, *, #11030, .F. ) ;
#12211=AXIS2_PLACEMENT_3D ( 'NONE', #7982, #1063, #4530 ) ;
#12212=ORIENTED_EDGE ( 'NONE', *, *, #8243, .F. ) ;
#12213=VECTOR ( 'NONE', #7100, 1000.000000000000000 ) ;
#12216=DIRECTION ( 'NONE',  ( -1.000000000000000000, 0.000000000000000000, 0.000000000000000000 ) ) ;
#12218=CARTESIAN_POINT ( 'NONE',  ( -5.209999999999999964, 0.000000000000000000, 0.000000000000000000 ) ) ;
#12220=EDGE_CURVE ( 'NONE', #6696, #13039, #5311, .T. ) ;
#12225=CARTESIAN_POINT ( 'NONE',  ( 2.783025325906566927, -2.249040938978666748, 24.42374957165204563 ) ) ;
#12226=ORIENTED_EDGE ( 'NONE', *, *, #8873, .F. ) ;
#12227=ORIENTED_EDGE ( 'NONE', *, *, #3929, .F. ) ;
#12229=CARTESIAN_POINT ( 'NONE',  ( 0.006931111373678920488, 22.53293026234503316, 9.685942809247130469 ) ) ;
#12233=VECTOR ( 'NONE', #4287, 1000.000000000000000 ) ;
#12236=DIRECTION ( 'NONE',  ( -1.000000000000000000, 0.000000000000000000, 0.000000000000000000 ) ) ;
#12237=ORIENTED_EDGE ( 'NONE', *, *, #10916, .T. ) ;
#12238=DIRECTION ( 'NONE',  ( -1.000000000000000000, -0.000000000000000000, -0.000000000000000000 ) ) ;
#12249=DIRECTION ( 'NONE',  ( 0.000000000000000000, 0.000000000000000000, 1.000000000000000000 ) ) ;
#12258=CYLINDRICAL_SURFACE ( 'NONE', #4648, 13.19999999999999574 ) ;
#12263=CARTESIAN_POINT ( 'NONE',  ( 0.02436607992776498519, 9.836394144775706394, 22.71065055754456097 ) ) ;
#12269=DIRECTION ( 'NONE',  ( -1.000000000000000000, -0.000000000000000000, -0.000000000000000000 ) ) ;
#12274=CARTESIAN_POINT ( 'NONE',  ( 2.789999999999999147, -2.133490293296841589, -24.22479935914661198 ) ) ;
#12276=CARTESIAN_POINT ( 'NONE',  ( 2.789999999999999147, -12.52067188844365830, 20.62201879784908698 ) ) ;
#12281=EDGE_CURVE ( 'NONE', #12104, #11073, #14643, .T. ) ;
#12284=ORIENTED_EDGE ( 'NONE', *, *, #14445, .T. ) ;
#12287=ORIENTED_EDGE ( 'NONE', *, *, #3826, .T. ) ;
#12288=ORIENTED_EDGE ( 'NONE', *, *, #3772, .T. ) ;
#12291=CARTESIAN_POINT ( 'NONE',  ( 2.765633920072235075, -12.59161484032896361, -21.30679549418645280 ) ) ;
#12292=DIRECTION ( 'NONE',  ( -1.000000000000000000, -0.000000000000000000, 0.000000000000000000 ) ) ;
#12297=EDGE_CURVE ( 'NONE', #7471, #13727, #8733, .T. ) ;
#12303=ORIENTED_EDGE ( 'NONE', *, *, #6706, .T. ) ;
#12304=ORIENTED_EDGE ( 'NONE', *, *, #4117, .T. ) ;
#12305=CARTESIAN_POINT ( 'NONE',  ( 2.783025336474041378, -12.53640742967737332, -21.08118142846917209 ) ) ;
#12307=FACE_OUTER_BOUND ( 'NONE', #5419, .T. ) ;
#12314=CARTESIAN_POINT ( 'NONE',  ( 2.718184749312773540, 2.576941577947758688, -25.22524549359947343 ) ) ;
#12315=DIRECTION ( 'NONE',  ( -1.000000000000000000, -0.000000000000000000, 0.000000000000000000 ) ) ;
#12318=CARTESIAN_POINT ( 'NONE',  ( 1.039999999999996705, -27.68468304288255410, -4.633866840649218055 ) ) ;
#12319=ORIENTED_EDGE ( 'NONE', *, *, #12406, .T. ) ;
#12320=EDGE_LOOP ( 'NONE', ( #8543, #14131, #7940, #2198, #14140, #6285, #640, #7139, #5409, #13588, #4227, #2345, #231, #7926, #4763, #5908, #4088, #7111, #13843, #6847, #5928, #8678, #7448, #14400, #10890, #11376, #2237, #6774, #10352, #6164, #2962, #8138, #2423, #570, #1562, #7992, #3699, #8800, #10500, #10027, #9783, #12953, #11689, #12472, #10857 ) ) ;
#12321=FACE_BOUND ( 'NONE', #259, .T. ) ;
#12327=DIRECTION ( 'NONE',  ( 1.000000000000000000, 0.000000000000000000, 0.000000000000000000 ) ) ;
#12331=DIRECTION ( 'NONE',  ( 1.000000000000000000, 0.000000000000000000, 0.000000000000000000 ) ) ;
#12341=CARTESIAN_POINT ( 'NONE',  ( 2.257825491203655943, -24.44564404695836402, -11.58891744060133355 ) ) ;
#12345=ADVANCED_FACE ( 'NONE', ( #759 ), #11426, .T. ) ;
#12347=CARTESIAN_POINT ( 'NONE',  ( -5.209999999999999964, 0.000000000000000000, 0.000000000000000000 ) ) ;
#12353=ORIENTED_EDGE ( 'NONE', *, *, #5999, .F. ) ;
#12359=CARTESIAN_POINT ( 'NONE',  ( 0.1587402281127123227, 22.38003579136345067, 12.81821841996081801 ) ) ;
#12360=EDGE_CURVE ( 'NONE', #949, #12913, #6824, .T. ) ;
#12362=CARTESIAN_POINT ( 'NONE',  ( 1.749999999999998002, 19.67366047555530528, 20.02152543075352753 ) ) ;
#12364=CARTESIAN_POINT ( 'NONE',  ( 2.789999999999999147, 0.000000000000000000, 0.000000000000000000 ) ) ;
#12365=CARTESIAN_POINT ( 'NONE',  ( 1.039999999999994929, -25.12109765559662833, 12.52377138324214023 ) ) ;
#12369=VECTOR ( 'NONE', #9557, 1000.000000000000000 ) ;
#12374=EDGE_CURVE ( 'NONE', #13280, #12872, #14149, .T. ) ;
#12383=AXIS2_PLACEMENT_3D ( 'NONE', #14834, #2149, #11296 ) ;
#12386=CYLINDRICAL_SURFACE ( 'NONE', #13474, 28.06981291497571362 ) ;
#12387=CARTESIAN_POINT ( 'NONE',  ( 0.02436607992775934733, -21.30679549418640306, 12.59161484032904887 ) ) ;
#12390=CARTESIAN_POINT ( 'NONE',  ( 0.02436607992776108206, -24.15498966839966855, 5.391175441198523544 ) ) ;
#12394=AXIS2_PLACEMENT_3D ( 'NONE', #8234, #2482, #230 ) ;
#12396=B_SPLINE_CURVE_WITH_KNOTS ( 'NONE', 3,
 ( #3301, #9223, #14920, #13759, #7764, #7688, #3234, #10368 ),
 .UNSPECIFIED., .F., .F.,
 ( 4, 2, 2, 4 ),
 ( 2.032124546189621919E-07, 0.001631739532304474910, 0.002447507692229407717, 0.003263275852154340524 ),
 .UNSPECIFIED. ) ;
#12399=CARTESIAN_POINT ( 'NONE',  ( -7.928732286808572430E-16, 18.34424029220111052, 15.96500990068130577 ) ) ;
#12401=ORIENTED_EDGE ( 'NONE', *, *, #4883, .T. ) ;
#12405=CYLINDRICAL_SURFACE ( 'NONE', #13869, 2.524999999999995914 ) ;
#12406=EDGE_CURVE ( 'NONE', #7326, #5643, #390, .T. ) ;
#12409=ORIENTED_EDGE ( 'NONE', *, *, #3772, .F. ) ;
#12412=ORIENTED_EDGE ( 'NONE', *, *, #420, .F. ) ;
#12414=CARTESIAN_POINT ( 'NONE',  ( 0.5279272933715190019, 18.56460150496967287, -19.66369668717012331 ) ) ;
#12417=ORIENTED_EDGE ( 'NONE', *, *, #321, .T. ) ;
#12419=CARTESIAN_POINT ( 'NONE',  ( 1.039999999999996705, -27.68468304288255410, -4.633866840649218055 ) ) ;
#12423=DIRECTION ( 'NONE',  ( -1.000000000000000000, 0.000000000000000000, 0.000000000000000000 ) ) ;
#12428=DIRECTION ( 'NONE',  ( -1.000000000000000000, -0.000000000000000000, -0.000000000000000000 ) ) ;
#12432=LINE ( 'NONE', #896, #526 ) ;
#12433=CARTESIAN_POINT ( 'NONE',  ( 0.02436607992776325046, -24.15498966839958683, -5.391175441198872598 ) ) ;
#12439=CARTESIAN_POINT ( 'NONE',  ( -10.00000000000000000, 0.000000000000000000, 0.000000000000000000 ) ) ;
#12441=ORIENTED_EDGE ( 'NONE', *, *, #5870, .T. ) ;
#12443=CIRCLE ( 'NONE', #12676, 2.524999999999995914 ) ;
#12446=CYLINDRICAL_SURFACE ( 'NONE', #12211, 28.06981291497571362 ) ;
#12449=FACE_OUTER_BOUND ( 'NONE', #3131, .T. ) ;
#12450=AXIS2_PLACEMENT_3D ( 'NONE', #9205, #2215, #8411 ) ;
#12451=CARTESIAN_POINT ( 'NONE',  ( 0.02436607992776411782, 22.71065055754465689, -9.836394144775473691 ) ) ;
#12456=CIRCLE ( 'NONE', #14424, 2.524999999999994582 ) ;
#12458=VECTOR ( 'NONE', #9604, 1000.000000000000000 ) ;
#12461=ORIENTED_EDGE ( 'NONE', *, *, #13802, .F. ) ;
#12462=ORIENTED_EDGE ( 'NONE', *, *, #10519, .F. ) ;
#12472=ORIENTED_EDGE ( 'NONE', *, *, #11067, .F. ) ;
#12475=EDGE_CURVE ( 'NONE', #1743, #12123, #14641, .T. ) ;
#12476=ADVANCED_FACE ( 'NONE', ( #2217 ), #10435, .T. ) ;
#12478=DIRECTION ( 'NONE',  ( -1.000000000000000000, 0.000000000000000000, 0.000000000000000000 ) ) ;
#12479=VECTOR ( 'NONE', #14258, 1000.000000000000000 ) ;
#12488=CARTESIAN_POINT ( 'NONE',  ( 0.000000000000000000, 5.535312321043032391, -23.48180575137725867 ) ) ;
#12489=EDGE_CURVE ( 'NONE', #1588, #7234, #8558, .T. ) ;
#12491=ORIENTED_EDGE ( 'NONE', *, *, #3845, .F. ) ;
#12492=CARTESIAN_POINT ( 'NONE',  ( 0.000000000000000000, 1.991882183130315953, 24.04302995059967074 ) ) ;
#12494=AXIS2_PLACEMENT_3D ( 'NONE', #410, #1575, #3803 ) ;
#12508=CARTESIAN_POINT ( 'NONE',  ( 0.02436607992776455150, -22.71065055754459650, 9.836394144775621129 ) ) ;
#12510=CARTESIAN_POINT ( 'NONE',  ( 0.02436607992776411782, -16.37294372382844543, -18.55949924794910544 ) ) ;
#12511=DIRECTION ( 'NONE',  ( 0.000000000000000000, 0.000000000000000000, 1.000000000000000000 ) ) ;
#12512=VERTEX_POINT ( 'NONE', #7260 ) ;
#12518=CARTESIAN_POINT ( 'NONE',  ( 2.789999999999999147, -7.909232158574647009, -21.81711360614308148 ) ) ;
#12521=VERTEX_POINT ( 'NONE', #6111 ) ;
#12529=CARTESIAN_POINT ( 'NONE',  ( 2.789999999999999147, 5.456805104201435164, -23.69843731927162978 ) ) ;
#12535=ORIENTED_EDGE ( 'NONE', *, *, #11618, .F. ) ;
#12539=CARTESIAN_POINT ( 'NONE',  ( 2.765633920072239071, -12.59161484032927092, 21.30679549418627161 ) ) ;
#12542=B_SPLINE_CURVE_WITH_KNOTS ( 'NONE', 3,
 ( #5687, #9139, #15139, #13897, #14912, #14993 ),
 .UNSPECIFIED., .F., .F.,
 ( 4, 2, 4 ),
 ( 2.132675795048140432E-07, 0.001878604073277005205, 0.003756994878974505639 ),
 .UNSPECIFIED. ) ;
#12548=VERTEX_POINT ( 'NONE', #5042 ) ;
#12550=CARTESIAN_POINT ( 'NONE',  ( 2.765633920072235963, -24.63872515616080960, -2.336989772644527008 ) ) ;
#12554=EDGE_CURVE ( 'NONE', #1582, #3392, #9482, .T. ) ;
#12556=CARTESIAN_POINT ( 'NONE',  ( 2.765633920072239516, -2.336989772644097574, -24.63872515616085224 ) ) ;
#12564=DIRECTION ( 'NONE',  ( 0.000000000000000000, 0.000000000000000000, 1.000000000000000000 ) ) ;
#12565=CARTESIAN_POINT ( 'NONE',  ( 2.765633920072238627, 12.59161484032942901, -21.30679549418617924 ) ) ;
#12566=ORIENTED_EDGE ( 'NONE', *, *, #2983, .F. ) ;
#12568=ORIENTED_EDGE ( 'NONE', *, *, #11578, .F. ) ;
#12572=DIRECTION ( 'NONE',  ( 1.000000000000000000, 0.000000000000000000, 0.000000000000000000 ) ) ;
#12573=CARTESIAN_POINT ( 'NONE',  ( 2.789999999999999147, 5.535312321042718864, 23.48180575137732262 ) ) ;
#12575=LINE ( 'NONE', #2049, #3655 ) ;
#12578=ORIENTED_EDGE ( 'NONE', *, *, #7788, .F. ) ;
#12580=DIRECTION ( 'NONE',  ( -1.000000000000000000, -0.000000000000000000, -0.000000000000000000 ) ) ;
#12581=DIRECTION ( 'NONE',  ( -1.000000000000000000, -0.000000000000000000, 0.000000000000000000 ) ) ;
#12584=CARTESIAN_POINT ( 'NONE',  ( 2.765633920072238627, 5.391175441198956086, -24.15498966839956907 ) ) ;
#12585=ORIENTED_EDGE ( 'NONE', *, *, #5405, .F. ) ;
#12587=DIRECTION ( 'NONE',  ( 0.000000000000000000, 0.000000000000000000, 1.000000000000000000 ) ) ;
#12590=CARTESIAN_POINT ( 'NONE',  ( 1.039999999999997593, 0.000000000000000000, 0.000000000000000000 ) ) ;
#12591=CARTESIAN_POINT ( 'NONE',  ( 9.603018496175287840E-16, -5.456805104200934231, -23.69843731927176123 ) ) ;
#12595=EDGE_CURVE ( 'NONE', #672, #5459, #11926, .T. ) ;
#12596=ORIENTED_EDGE ( 'NONE', *, *, #13476, .F. ) ;
#12598=CARTESIAN_POINT ( 'NONE',  ( 2.783069004973548033, 23.92277630352795370, 5.408431875071527450 ) ) ;
#12599=ORIENTED_EDGE ( 'NONE', *, *, #7651, .T. ) ;
#12607=ADVANCED_FACE ( 'NONE', ( #8858 ), #1647, .T. ) ;
#12609=ORIENTED_EDGE ( 'NONE', *, *, #1840, .T. ) ;
#12611=CARTESIAN_POINT ( 'NONE',  ( 0.000000000000000000, 0.000000000000000000, 0.000000000000000000 ) ) ;
#12614=AXIS2_PLACEMENT_3D ( 'NONE', #7462, #13527, #766 ) ;
#12619=DIRECTION ( 'NONE',  ( 1.000000000000000000, 0.000000000000000000, 0.000000000000000000 ) ) ;
#12624=DIRECTION ( 'NONE',  ( -1.000000000000000000, -0.000000000000000000, -0.000000000000000000 ) ) ;
#12625=AXIS2_PLACEMENT_3D ( 'NONE', #183, #8184, #1123 ) ;
#12626=CIRCLE ( 'NONE', #604, 28.06981291497571362 ) ;
#12630=CYLINDRICAL_SURFACE ( 'NONE', #8465, 13.19999999999999929 ) ;
#12633=CARTESIAN_POINT ( 'NONE',  ( 2.789999999999999147, -7.909232158574988958, 24.34211360614297348 ) ) ;
#12643=CARTESIAN_POINT ( 'NONE',  ( 1.749999999999998002, 0.000000000000000000, 0.000000000000000000 ) ) ;
#12644=CARTESIAN_POINT ( 'NONE',  ( 2.789999999999999147, 0.000000000000000000, 0.000000000000000000 ) ) ;
#12645=CARTESIAN_POINT ( 'NONE',  ( 2.604434404052931473, -17.45907811351440841, -19.17825124759797006 ) ) ;
#12650=CARTESIAN_POINT ( 'NONE',  ( 2.718184757033984766, -16.91181672897746324, 18.89296398180185932 ) ) ;
#12662=DIRECTION ( 'NONE',  ( 0.000000000000000000, 0.9510565162951498674, 0.3090169943749583870 ) ) ;
#12663=CARTESIAN_POINT ( 'NONE',  ( 0.000000000000000000, -5.535312321042547445, -23.48180575137738302 ) ) ;
#12671=B_SPLINE_CURVE_WITH_KNOTS ( 'NONE', 3,
 ( #15200, #3721, #24, #2569 ),
 .UNSPECIFIED., .F., .F.,
 ( 4, 4 ),
 ( 0.005258120783916792398, 0.005948386350302926374 ),
 .UNSPECIFIED. ) ;
#12672=CARTESIAN_POINT ( 'NONE',  ( 0.000000000000000000, 15.04425356660760293, 20.70663861606276868 ) ) ;
#12676=AXIS2_PLACEMENT_3D ( 'NONE', #2114, #13867, #9041 ) ;
#12678=ORIENTED_EDGE ( 'NONE', *, *, #8349, .T. ) ;
#12683=EDGE_CURVE ( 'NONE', #14255, #9774, #7009, .T. ) ;
#12688=ORIENTED_EDGE ( 'NONE', *, *, #13560, .T. ) ;
#12691=CARTESIAN_POINT ( 'NONE',  ( 1.039999999999996483, 4.147968289691283950, 27.76164181293052735 ) ) ;
#12717=DIRECTION ( 'NONE',  ( 0.000000000000000000, 0.000000000000000000, 1.000000000000000000 ) ) ;
#12719=FACE_OUTER_BOUND ( 'NONE', #10541, .T. ) ;
#12725=DIRECTION ( 'NONE',  ( -1.000000000000000000, 0.000000000000000000, -0.000000000000000000 ) ) ;
#12728=FACE_OUTER_BOUND ( 'NONE', #3565, .T. ) ;
#12730=ORIENTED_EDGE ( 'NONE', *, *, #2301, .F. ) ;
#12733=DIRECTION ( 'NONE',  ( -1.000000000000000000, -0.000000000000000000, -0.000000000000000000 ) ) ;
#12734=CARTESIAN_POINT ( 'NONE',  ( 2.718131847775120402, 5.344160105509049963, -24.78765742476133482 ) ) ;
#12737=CARTESIAN_POINT ( 'NONE',  ( 1.749999999999998002, -25.12109765559663188, 12.52377138324213668 ) ) ;
#12738=CARTESIAN_POINT ( 'NONE',  ( 1.749999999999998002, -19.67366047555515252, -20.02152543075368030 ) ) ;
#12740=CARTESIAN_POINT ( 'NONE',  ( 2.789999999999999147, 0.000000000000000000, 0.000000000000000000 ) ) ;
#12741=CARTESIAN_POINT ( 'NONE',  ( 2.765633920072238627, -21.30679549418621832, -12.59161484032935618 ) ) ;
#12750=LINE ( 'NONE', #1072, #3833 ) ;
#12751=CARTESIAN_POINT ( 'NONE',  ( 2.790000000000000036, 23.69843731927168662, 5.456805104201184697 ) ) ;
#12752=ORIENTED_EDGE ( 'NONE', *, *, #9953, .T. ) ;
#12758=EDGE_CURVE ( 'NONE', #7028, #1566, #10363, .T. ) ;
#12761=DIRECTION ( 'NONE',  ( 0.000000000000000000, 0.000000000000000000, 1.000000000000000000 ) ) ;
#12764=CARTESIAN_POINT ( 'NONE',  ( 2.765633920072238627, -21.30679549418621832, -12.59161484032935618 ) ) ;
#12766=CARTESIAN_POINT ( 'NONE',  ( 1.749999999999998002, -4.633866840648726004, -27.68468304288263582 ) ) ;
#12775=DIRECTION ( 'NONE',  ( 0.000000000000000000, 0.000000000000000000, 1.000000000000000000 ) ) ;
#12776=ORIENTED_EDGE ( 'NONE', *, *, #13416, .F. ) ;
#12777=FACE_OUTER_BOUND ( 'NONE', #10586, .T. ) ;
#12781=ORIENTED_EDGE ( 'NONE', *, *, #2644, .F. ) ;
#12783=CARTESIAN_POINT ( 'NONE',  ( 2.257825477245765988, -19.66801664102690239, -18.57583492944443293 ) ) ;
#12786=CARTESIAN_POINT ( 'NONE',  ( 0.006974663525957706944, 21.08118142846903353, 12.53640742967760602 ) ) ;
#12794=CARTESIAN_POINT ( 'NONE',  ( -10.00000000000000000, 0.000000000000000000, 0.000000000000000000 ) ) ;
#12796=CARTESIAN_POINT ( 'NONE',  ( 0.000000000000000000, 15.04425356660790136, -18.18163861606255338 ) ) ;
#12798=VECTOR ( 'NONE', #755, 1000.000000000000000 ) ;
#12800=B_SPLINE_CURVE_WITH_KNOTS ( 'NONE', 3,
 ( #5803, #4658, #9335, #14016 ),
 .UNSPECIFIED., .F., .F.,
 ( 4, 4 ),
 ( 2.135345996173299606E-07, 0.0006888010880210790939 ),
 .UNSPECIFIED. ) ;
#12801=EDGE_CURVE ( 'NONE', #6027, #12188, #615, .T. ) ;
#12808=DIRECTION ( 'NONE',  ( 1.000000000000000000, 0.000000000000000000, -0.000000000000000000 ) ) ;
#12810=CARTESIAN_POINT ( 'NONE',  ( 2.789999999999999147, 20.62201879784931435, -12.52067188844328882 ) ) ;
#12812=CIRCLE ( 'NONE', #5480, 2.524999999999996358 ) ;
#12816=VERTEX_POINT ( 'NONE', #14159 ) ;
#12817=CARTESIAN_POINT ( 'NONE',  ( 0.02436607992775978102, -12.59161484032896361, -21.30679549418645280 ) ) ;
#12820=ADVANCED_FACE ( 'NONE', ( #11768 ), #305, .T. ) ;
#12827=CARTESIAN_POINT ( 'NONE',  ( 2.765633920072235075, -12.59161484032896361, -21.30679549418645280 ) ) ;
#12828=CARTESIAN_POINT ( 'NONE',  ( 1.824075699840007170, -24.74770846292491910, 12.96726489871182153 ) ) ;
#12830=DIRECTION ( 'NONE',  ( -1.000000000000000000, -0.000000000000000000, -0.000000000000000000 ) ) ;
#12831=VERTEX_POINT ( 'NONE', #10778 ) ;
#12840=ORIENTED_EDGE ( 'NONE', *, *, #1370, .T. ) ;
#12842=ORIENTED_EDGE ( 'NONE', *, *, #8072, .T. ) ;
#12846=CYLINDRICAL_SURFACE ( 'NONE', #576, 28.06981291497571362 ) ;
#12849=VECTOR ( 'NONE', #13948, 1000.000000000000000 ) ;
#12853=CARTESIAN_POINT ( 'NONE',  ( 2.718184757033982102, -18.89296398180179537, -16.91181672897754495 ) ) ;
#12854=EDGE_LOOP ( 'NONE', ( #10703, #14318, #9059, #13606 ) ) ;
#12855=EDGE_LOOP ( 'NONE', ( #14828, #10228, #8829, #8318 ) ) ;
#12857=CIRCLE ( 'NONE', #8943, 24.12539914357697768 ) ;
#12858=LINE ( 'NONE', #10502, #12479 ) ;
#12859=ADVANCED_FACE ( 'NONE', ( #11994 ), #229, .T. ) ;
#12861=DIRECTION ( 'NONE',  ( -1.000000000000000000, 0.000000000000000000, -0.000000000000000000 ) ) ;
#12867=CARTESIAN_POINT ( 'NONE',  ( 2.789999999999999147, 24.04302995059966364, 1.991882183130384121 ) ) ;
#12868=CARTESIAN_POINT ( 'NONE',  ( 0.1882239034349757756, -12.84621645676860702, 22.54313264455009147 ) ) ;
#12870=AXIS2_PLACEMENT_3D ( 'NONE', #1983, #5520, #9198 ) ;
#12872=VERTEX_POINT ( 'NONE', #1479 ) ;
#12874=ORIENTED_EDGE ( 'NONE', *, *, #12683, .T. ) ;
#12875=EDGE_CURVE ( 'NONE', #5202, #3390, #13094, .T. ) ;
#12876=FACE_OUTER_BOUND ( 'NONE', #6175, .T. ) ;
#12881=DIRECTION ( 'NONE',  ( 0.000000000000000000, 0.000000000000000000, 1.000000000000000000 ) ) ;
#12882=CARTESIAN_POINT ( 'NONE',  ( 0.006974657972265005043, 23.92335783895637746, 5.408388659524176134 ) ) ;
#12893=VERTEX_POINT ( 'NONE', #10553 ) ;
#12897=CARTESIAN_POINT ( 'NONE',  ( 2.789999999999999147, -23.48180575137734039, 5.535312321042630934 ) ) ;
#12902=B_SPLINE_CURVE_WITH_KNOTS ( 'NONE', 3,
 ( #13053, #3468, #8373, #10465 ),
 .UNSPECIFIED., .F., .F.,
 ( 4, 4 ),
 ( 0.005258139959819239928, 0.005948405594583421920 ),
 .UNSPECIFIED. ) ;
#12904=ORIENTED_EDGE ( 'NONE', *, *, #10774, .T. ) ;
#12905=CARTESIAN_POINT ( 'NONE',  ( 2.789999999999999147, -24.04302995059966719, 1.991882183130210482 ) ) ;
#12907=AXIS2_PLACEMENT_3D ( 'NONE', #10585, #34, #12951 ) ;
#12910=ORIENTED_EDGE ( 'NONE', *, *, #11338, .F. ) ;
#12913=VERTEX_POINT ( 'NONE', #3695 ) ;
#12920=CIRCLE ( 'NONE', #14418, 2.524999999999995914 ) ;
#12922=CARTESIAN_POINT ( 'NONE',  ( 1.039999999999999147, 12.52377138324259676, -25.12109765559640095 ) ) ;
#12924=CARTESIAN_POINT ( 'NONE',  ( 1.039999999999998259, 12.52377138324223615, 25.12109765559657859 ) ) ;
#12925=LINE ( 'NONE', #14173, #12849 ) ;
#12926=CIRCLE ( 'NONE', #10248, 28.06981291497571007 ) ;
#12931=CIRCLE ( 'NONE', #10743, 28.06981291497571362 ) ;
#12933=EDGE_LOOP ( 'NONE', ( #3193, #2744, #8979, #11197, #15126, #12578 ) ) ;
#12937=CARTESIAN_POINT ( 'NONE',  ( 2.788130827028544534, 20.90869469097885158, -12.51925356660739297 ) ) ;
#12941=CYLINDRICAL_SURFACE ( 'NONE', #12625, 28.06981291497571362 ) ;
#12942=CYLINDRICAL_SURFACE ( 'NONE', #7089, 2.524999999999995914 ) ;
#12943=EDGE_CURVE ( 'NONE', #8603, #2360, #8923, .T. ) ;
#12944=AXIS2_PLACEMENT_3D ( 'NONE', #14885, #4508, #3134 ) ;
#12945=AXIS2_PLACEMENT_3D ( 'NONE', #8362, #124, #1015 ) ;
#12949=CARTESIAN_POINT ( 'NONE',  ( 0.02436607992775934733, -2.336989772644440855, 24.63872515616082026 ) ) ;
#12950=DIRECTION ( 'NONE',  ( -1.000000000000000000, -0.000000000000000000, -0.000000000000000000 ) ) ;
#12951=DIRECTION ( 'NONE',  ( 0.000000000000000000, 0.000000000000000000, 1.000000000000000000 ) ) ;
#12953=ORIENTED_EDGE ( 'NONE', *, *, #1791, .F. ) ;
#12954=AXIS2_PLACEMENT_3D ( 'NONE', #14605, #10361, #13823 ) ;
#12957=ORIENTED_EDGE ( 'NONE', *, *, #1126, .F. ) ;
#12961=B_SPLINE_CURVE_WITH_KNOTS ( 'NONE', 3,
 ( #1948, #6633, #11152, #11312, #6470, #1691 ),
 .UNSPECIFIED., .F., .F.,
 ( 4, 2, 4 ),
 ( 4.462636793144160676E-07, 0.001879885123570646096, 0.003759323983461977832 ),
 .UNSPECIFIED. ) ;
#12966=EDGE_LOOP ( 'NONE', ( #11526, #14986 ) ) ;
#12978=EDGE_LOOP ( 'NONE', ( #7277, #7581, #10637, #2560 ) ) ;
#12983=CARTESIAN_POINT ( 'NONE',  ( 4.098876516494237640E-16, -15.96500990068138570, 18.34424029220106078 ) ) ;
#12987=CYLINDRICAL_SURFACE ( 'NONE', #5581, 13.19999999999999929 ) ;
#12994=EDGE_CURVE ( 'NONE', #10552, #3410, #5789, .T. ) ;
#12995=DIRECTION ( 'NONE',  ( -1.000000000000000000, -0.000000000000000000, -0.000000000000000000 ) ) ;
#12996=ORIENTED_EDGE ( 'NONE', *, *, #364, .F. ) ;
#12997=CARTESIAN_POINT ( 'NONE',  ( 2.789999999999999147, -7.909232158574647009, -24.34211360614308006 ) ) ;
#13001=DIRECTION ( 'NONE',  ( 0.000000000000000000, 0.000000000000000000, 1.000000000000000000 ) ) ;
#13003=DIRECTION ( 'NONE',  ( -1.000000000000000000, -0.000000000000000000, -0.000000000000000000 ) ) ;
#13005=ORIENTED_EDGE ( 'NONE', *, *, #14242, .T. ) ;
#13006=EDGE_CURVE ( 'NONE', #14624, #7854, #12065, .T. ) ;
#13007=ADVANCED_FACE ( 'NONE', ( #14777 ), #6465, .T. ) ;
#13009=ORIENTED_EDGE ( 'NONE', *, *, #7945, .T. ) ;
#13011=CARTESIAN_POINT ( 'NONE',  ( 2.789999999999999147, 7.909232158575156824, -24.34211360614291664 ) ) ;
#13012=CARTESIAN_POINT ( 'NONE',  ( 0.000000000000000000, 18.28042085475278000, 15.74360496233386719 ) ) ;
#13015=CARTESIAN_POINT ( 'NONE',  ( 0.0001048300153468720319, 20.67846228565678146, -12.51925356660738053 ) ) ;
#13017=CARTESIAN_POINT ( 'NONE',  ( 0.000000000000000000, -22.25075486061745167, 9.324097380959385006 ) ) ;
#13018=ORIENTED_EDGE ( 'NONE', *, *, #9700, .F. ) ;
#13019=CARTESIAN_POINT ( 'NONE',  ( 2.765633920072242180, 22.71065055754465689, -9.836394144775473691 ) ) ;
#13022=CARTESIAN_POINT ( 'NONE',  ( 0.000000000000000000, -20.62201879784905501, -12.52067188844372936 ) ) ;
#13023=EDGE_CURVE ( 'NONE', #14244, #8517, #5800, .T. ) ;
#13024=ORIENTED_EDGE ( 'NONE', *, *, #2884, .F. ) ;
#13027=EDGE_CURVE ( 'NONE', #8127, #5482, #2851, .T. ) ;
#13029=LINE ( 'NONE', #11875, #3386 ) ;
#13032=CARTESIAN_POINT ( 'NONE',  ( 0.1855657389739088781, -25.39738473785004302, 5.253342437939627629 ) ) ;
#13035=EDGE_CURVE ( 'NONE', #15218, #9857, #13539, .T. ) ;
#13037=CARTESIAN_POINT ( 'NONE',  ( 1.039999999999995817, -27.76164181293048472, -4.147968289691575272 ) ) ;
#13038=DIRECTION ( 'NONE',  ( 0.000000000000000000, 0.000000000000000000, 1.000000000000000000 ) ) ;
#13039=VERTEX_POINT ( 'NONE', #14549 ) ;
#13040=CARTESIAN_POINT ( 'NONE',  ( 2.789999999999999147, 20.62201879784912606, 12.52067188844359080 ) ) ;
#13044=ORIENTED_EDGE ( 'NONE', *, *, #646, .F. ) ;
#13047=CARTESIAN_POINT ( 'NONE',  ( 1.039999999999996039, 27.68468304288258963, 4.633866840649018215 ) ) ;
#13048=CARTESIAN_POINT ( 'NONE',  ( 2.783025342027734439, -23.92335783895641299, 5.408388659523998498 ) ) ;
#13053=CARTESIAN_POINT ( 'NONE',  ( 2.789999999999999147, -12.52067188844365830, 20.62201879784908698 ) ) ;
#13054=ORIENTED_EDGE ( 'NONE', *, *, #6466, .F. ) ;
#13057=ORIENTED_EDGE ( 'NONE', *, *, #2679, .F. ) ;
#13058=CARTESIAN_POINT ( 'NONE',  ( 2.789999999999999147, 14.18181402625769749, -19.91106274590499225 ) ) ;
#13061=EDGE_LOOP ( 'NONE', ( #6660, #14705, #8439, #2635, #5395, #9230 ) ) ;
#13063=CARTESIAN_POINT ( 'NONE',  ( 2.790000000000076419, -22.38018801136469094, -9.515416771311432598 ) ) ;
#13068=EDGE_CURVE ( 'NONE', #7278, #4522, #7472, .T. ) ;
#13069=DIRECTION ( 'NONE',  ( -1.000000000000000000, 0.000000000000000000, -0.000000000000000000 ) ) ;
#13071=ORIENTED_EDGE ( 'NONE', *, *, #7585, .T. ) ;
#13074=DIRECTION ( 'NONE',  ( -1.000000000000000000, -0.000000000000000000, -0.000000000000000000 ) ) ;
#13080=CARTESIAN_POINT ( 'NONE',  ( 2.789999999999999147, -15.04425356660744839, -18.18163861606288378 ) ) ;
#13082=DIRECTION ( 'NONE',  ( -1.000000000000000000, -0.000000000000000000, -0.000000000000000000 ) ) ;
#13093=DIRECTION ( 'NONE',  ( 1.000000000000000000, 0.000000000000000000, 0.000000000000000000 ) ) ;
#13094=B_SPLINE_CURVE_WITH_KNOTS ( 'NONE', 3,
 ( #4794, #9545, #13233, #2711, #11687, #11835 ),
 .UNSPECIFIED., .F., .F.,
 ( 4, 2, 4 ),
 ( 2.032124546189621919E-07, 0.001878594002992306630, 0.003756984793529993989 ),
 .UNSPECIFIED. ) ;
#13095=CYLINDRICAL_SURFACE ( 'NONE', #12907, 2.524999999999995914 ) ;
#13098=AXIS2_PLACEMENT_3D ( 'NONE', #2068, #11587, #6835 ) ;
#13103=APPLICATION_CONTEXT ( 'automotive_design' ) ;
#13104=DIRECTION ( 'NONE',  ( -1.000000000000000000, -0.000000000000000000, -0.000000000000000000 ) ) ;
#13111=CARTESIAN_POINT ( 'NONE',  ( 2.789999999999999147, -20.62201879784904079, -12.52067188844374179 ) ) ;
#13112=CARTESIAN_POINT ( 'NONE',  ( 0.07181523211952839381, -10.24584646439522828, -23.19431517146944088 ) ) ;
#13113=VECTOR ( 'NONE', #1341, 1000.000000000000000 ) ;
#13114=EDGE_CURVE ( 'NONE', #1743, #9942, #3090, .T. ) ;
#13118=CARTESIAN_POINT ( 'NONE',  ( 0.1882238782932344479, 19.18368891937516452, -17.47009390565470000 ) ) ;
#13120=CIRCLE ( 'NONE', #13874, 2.524999999999996358 ) ;
#13129=AXIS2_PLACEMENT_3D ( 'NONE', #1965, #4494, #1027 ) ;
#13130=CARTESIAN_POINT ( 'NONE',  ( 2.031033491000347357, 12.05173163741723030, 24.80232951178382805 ) ) ;
#13144=ORIENTED_EDGE ( 'NONE', *, *, #6839, .F. ) ;
#13149=ORIENTED_EDGE ( 'NONE', *, *, #10056, .T. ) ;
#13153=CARTESIAN_POINT ( 'NONE',  ( -5.209999999999999964, 0.000000000000000000, 0.000000000000000000 ) ) ;
#13154=EDGE_LOOP ( 'NONE', ( #347, #9333, #8377, #5926 ) ) ;
#13155=CARTESIAN_POINT ( 'NONE',  ( 1.749999999999998002, 0.000000000000000000, 0.000000000000000000 ) ) ;
#13163=CARTESIAN_POINT ( 'NONE',  ( 2.783025306068355853, -18.43727551351019045, -16.17543236988008815 ) ) ;
#13165=AXIS2_PLACEMENT_3D ( 'NONE', #1794, #4105, #8785 ) ;
#13166=EDGE_CURVE ( 'NONE', #9661, #9629, #11455, .T. ) ;
#13173=AXIS2_PLACEMENT_3D ( 'NONE', #6520, #14755, #13208 ) ;
#13176=EDGE_CURVE ( 'NONE', #5857, #2934, #7075, .T. ) ;
#13180=ORIENTED_EDGE ( 'NONE', *, *, #13431, .F. ) ;
#13185=CARTESIAN_POINT ( 'NONE',  ( -7.625032001148274383E-14, 9.515416771311183908, 22.38018801136479397 ) ) ;
#13188=ORIENTED_EDGE ( 'NONE', *, *, #9923, .F. ) ;
#13191=DIRECTION ( 'NONE',  ( -1.000000000000000000, -0.000000000000000000, -0.000000000000000000 ) ) ;
#13192=DIRECTION ( 'NONE',  ( -1.000000000000000000, -0.000000000000000000, -0.000000000000000000 ) ) ;
#13196=CARTESIAN_POINT ( 'NONE',  ( 2.789999999999999147, -19.91106274590524094, 14.18181402625735466 ) ) ;
#13202=CARTESIAN_POINT ( 'NONE',  ( 2.765633920072238627, 12.59161484032942901, -21.30679549418617924 ) ) ;
#13203=ORIENTED_EDGE ( 'NONE', *, *, #321, .F. ) ;
#13206=EDGE_CURVE ( 'NONE', #13461, #13319, #2628, .T. ) ;
#13208=DIRECTION ( 'NONE',  ( 0.000000000000000000, 0.000000000000000000, 1.000000000000000000 ) ) ;
#13210=CIRCLE ( 'NONE', #3166, 2.524999999999995914 ) ;
#13211=CIRCLE ( 'NONE', #10523, 2.524999999999995914 ) ;
#13215=EDGE_LOOP ( 'NONE', ( #2035, #8564, #14459, #8935, #9207, #5329 ) ) ;
#13216=ORIENTED_EDGE ( 'NONE', *, *, #12281, .F. ) ;
#13224=DIRECTION ( 'NONE',  ( -1.000000000000000000, -0.000000000000000000, -0.000000000000000000 ) ) ;
#13225=CARTESIAN_POINT ( 'NONE',  ( 2.718131914667133220, 23.19485392143227642, -10.24630254990492340 ) ) ;
#13228=DIRECTION ( 'NONE',  ( -1.000000000000000000, -0.000000000000000000, -0.000000000000000000 ) ) ;
#13230=ORIENTED_EDGE ( 'NONE', *, *, #7486, .T. ) ;
#13231=ORIENTED_EDGE ( 'NONE', *, *, #11861, .F. ) ;
#13233=CARTESIAN_POINT ( 'NONE',  ( 2.604434283110813819, -22.53097606932974983, -12.84444904262050002 ) ) ;
#13239=VERTEX_POINT ( 'NONE', #9316 ) ;
#13242=VECTOR ( 'NONE', #3247, 1000.000000000000000 ) ;
#13243=CARTESIAN_POINT ( 'NONE',  ( 2.789999999999999147, 15.04425356660790136, -20.70663861606255196 ) ) ;
#13246=CARTESIAN_POINT ( 'NONE',  ( 0.000000000000000000, -25.59481291497571220, -1.787276233276378314E-13 ) ) ;
#13250=ORIENTED_EDGE ( 'NONE', *, *, #14274, .T. ) ;
#13254=DIRECTION ( 'NONE',  ( 0.000000000000000000, 0.000000000000000000, 1.000000000000000000 ) ) ;
#13257=CARTESIAN_POINT ( 'NONE',  ( 2.783068930044319433, 18.43696893154781691, -16.17493693894858353 ) ) ;
#13262=DIRECTION ( 'NONE',  ( -1.000000000000000000, -0.000000000000000000, -0.000000000000000000 ) ) ;
#13267=EDGE_CURVE ( 'NONE', #952, #4433, #11942, .T. ) ;
#13273=LINE ( 'NONE', #12038, #9568 ) ;
#13274=CARTESIAN_POINT ( 'NONE',  ( -7.922038997698610785E-14, 18.34439787333529992, -15.96555658743743145 ) ) ;
#13278=DIRECTION ( 'NONE',  ( -1.000000000000000000, -0.000000000000000000, -0.000000000000000000 ) ) ;
#13280=VERTEX_POINT ( 'NONE', #13047 ) ;
#13281=EDGE_CURVE ( 'NONE', #5202, #4588, #14142, .T. ) ;
#13283=CARTESIAN_POINT ( 'NONE',  ( 0.006974771092476448643, 22.53337530003417655, -9.686319561460717154 ) ) ;
#13291=CARTESIAN_POINT ( 'NONE',  ( -10.00000000000000000, 0.000000000000000000, 0.000000000000000000 ) ) ;
#13292=CARTESIAN_POINT ( 'NONE',  ( 2.765633920072242180, 22.71065055754465689, -9.836394144775473691 ) ) ;
#13299=ORIENTED_EDGE ( 'NONE', *, *, #6490, .F. ) ;
#13300=CARTESIAN_POINT ( 'NONE',  ( 2.789999999999999147, -12.52067188844336165, -20.62201879784926462 ) ) ;
#13301=CARTESIAN_POINT ( 'NONE',  ( 1.749999999999998002, 19.67366047555558950, -20.02152543075324687 ) ) ;
#13303=EDGE_CURVE ( 'NONE', #7479, #6398, #10174, .T. ) ;
#13307=ORIENTED_EDGE ( 'NONE', *, *, #10519, .T. ) ;
#13310=CARTESIAN_POINT ( 'NONE',  ( 0.5279273381794633568, -3.461047254864449307, 26.82026385750176445 ) ) ;
#13315=CARTESIAN_POINT ( 'NONE',  ( 5.366045694719498695E-16, 9.514945144209063344, -22.37986894186662923 ) ) ;
#13316=ORIENTED_EDGE ( 'NONE', *, *, #13717, .F. ) ;
#13317=DIRECTION ( 'NONE',  ( -1.000000000000000000, 0.000000000000000000, 0.000000000000000000 ) ) ;
#13318=CARTESIAN_POINT ( 'NONE',  ( 2.789999999999999147, 7.772527002114431482, 23.17675759782044054 ) ) ;
#13319=VERTEX_POINT ( 'NONE', #10763 ) ;
#13321=DIRECTION ( 'NONE',  ( 0.000000000000000000, 0.000000000000000000, 1.000000000000000000 ) ) ;
#13328=ORIENTED_EDGE ( 'NONE', *, *, #4607, .F. ) ;
#13329=CARTESIAN_POINT ( 'NONE',  ( 0.000000000000000000, 2.680914349914567470E-13, -25.59481291497571220 ) ) ;
#13334=VERTEX_POINT ( 'NONE', #8526 ) ;
#13337=ORIENTED_EDGE ( 'NONE', *, *, #2538, .T. ) ;
#13339=DIRECTION ( 'NONE',  ( 0.000000000000000000, 0.000000000000000000, 1.000000000000000000 ) ) ;
#13346=DIRECTION ( 'NONE',  ( 0.000000000000000000, 0.000000000000000000, 1.000000000000000000 ) ) ;
#13352=CARTESIAN_POINT ( 'NONE',  ( -5.209999999999999964, 0.000000000000000000, 0.000000000000000000 ) ) ;
#13356=CARTESIAN_POINT ( 'NONE',  ( 2.765633920072234631, 5.391175441198615914, 24.15498966839965078 ) ) ;
#13364=CARTESIAN_POINT ( 'NONE',  ( -5.209999999999999964, 0.000000000000000000, 0.000000000000000000 ) ) ;
#13366=VECTOR ( 'NONE', #4645, 1000.000000000000000 ) ;
#13368=CARTESIAN_POINT ( 'NONE',  ( 1.749999999999998002, 25.12109765559671004, -12.52377138324198391 ) ) ;
#13369=ADVANCED_FACE ( 'NONE', ( #12052 ), #14163, .T. ) ;
#13371=DIRECTION ( 'NONE',  ( -1.000000000000000000, -0.000000000000000000, -0.000000000000000000 ) ) ;
#13377=ORIENTED_EDGE ( 'NONE', *, *, #10388, .F. ) ;
#13380=CARTESIAN_POINT ( 'NONE',  ( 1.039999999999997593, 0.000000000000000000, 0.000000000000000000 ) ) ;
#13382=ORIENTED_EDGE ( 'NONE', *, *, #6985, .F. ) ;
#13383=DIRECTION ( 'NONE',  ( -1.000000000000000000, -0.000000000000000000, -0.000000000000000000 ) ) ;
#13388=CARTESIAN_POINT ( 'NONE',  ( 8.000000000000000000, 0.000000000000000000, 0.000000000000000000 ) ) ;
#13389=DIRECTION ( 'NONE',  ( 0.000000000000000000, 0.000000000000000000, 1.000000000000000000 ) ) ;
#13392=DIRECTION ( 'NONE',  ( 0.000000000000000000, 1.374038396813314559E-15, -1.000000000000000000 ) ) ;
#13394=EDGE_LOOP ( 'NONE', ( #9562, #311, #9043, #4734, #1727, #1355, #15183, #5252 ) ) ;
#13400=CARTESIAN_POINT ( 'NONE',  ( 0.000000000000000000, -24.04302995059967429, 1.991882183130232242 ) ) ;
#13401=CARTESIAN_POINT ( 'NONE',  ( 1.749999999999998002, -25.12109765559663188, 12.52377138324213668 ) ) ;
#13403=EDGE_CURVE ( 'NONE', #11628, #11722, #2477, .T. ) ;
#13411=CARTESIAN_POINT ( 'NONE',  ( -5.209999999999999964, 0.000000000000000000, 0.000000000000000000 ) ) ;
#13413=CARTESIAN_POINT ( 'NONE',  ( 0.02436607992776151574, -18.55949924794880346, -16.37294372382878649 ) ) ;
#13414=DIRECTION ( 'NONE',  ( -1.000000000000000000, -0.000000000000000000, 0.000000000000000000 ) ) ;
#13415=ORIENTED_EDGE ( 'NONE', *, *, #7686, .T. ) ;
#13416=EDGE_CURVE ( 'NONE', #12831, #1110, #6068, .T. ) ;
#13417=ORIENTED_EDGE ( 'NONE', *, *, #10293, .F. ) ;
#13424=LINE ( 'NONE', #3978, #11157 ) ;
#13427=FACE_OUTER_BOUND ( 'NONE', #8546, .T. ) ;
#13429=CARTESIAN_POINT ( 'NONE',  ( 0.02436607992776151574, -18.55949924794880346, -16.37294372382878649 ) ) ;
#13431=EDGE_CURVE ( 'NONE', #9808, #10254, #3217, .T. ) ;
#13432=ORIENTED_EDGE ( 'NONE', *, *, #3467, .T. ) ;
#13434=AXIS2_PLACEMENT_3D ( 'NONE', #9479, #14177, #1329 ) ;
#13436=DIRECTION ( 'NONE',  ( 0.000000000000000000, 0.000000000000000000, 1.000000000000000000 ) ) ;
#13437=ORIENTED_EDGE ( 'NONE', *, *, #7270, .T. ) ;
#13446=CARTESIAN_POINT ( 'NONE',  ( 2.789999999999999147, -23.17675759782046541, 7.772527002114348882 ) ) ;
#13450=LINE ( 'NONE', #12057, #14728 ) ;
#13457=ORIENTED_EDGE ( 'NONE', *, *, #1586, .F. ) ;
#13458=ORIENTED_EDGE ( 'NONE', *, *, #14949, .T. ) ;
#13459=CARTESIAN_POINT ( 'NONE',  ( 1.394999999999999574, -24.89775460606841406, 12.96210679857778025 ) ) ;
#13460=CARTESIAN_POINT ( 'NONE',  ( 2.601776121706765199, 17.47009390565519382, -19.18368891937472043 ) ) ;
#13461=VERTEX_POINT ( 'NONE', #8667 ) ;
#13464=B_SPLINE_CURVE_WITH_KNOTS ( 'NONE', 3,
 ( #6081, #10768, #11132, #456, #6309, #14385 ),
 .UNSPECIFIED., .F., .F.,
 ( 4, 2, 4 ),
 ( 2.321268216997094965E-07, 0.001878622960950499009, 0.003757013795079297992 ),
 .UNSPECIFIED. ) ;
#13471=DIRECTION ( 'NONE',  ( 0.000000000000000000, 0.000000000000000000, 1.000000000000000000 ) ) ;
#13473=VECTOR ( 'NONE', #2893, 1000.000000000000000 ) ;
#13474=AXIS2_PLACEMENT_3D ( 'NONE', #1864, #11151, #11940 ) ;
#13475=DIRECTION ( 'NONE',  ( -1.000000000000000000, 0.000000000000000000, -0.000000000000000000 ) ) ;
#13476=EDGE_CURVE ( 'NONE', #10133, #14329, #5236, .T. ) ;
#13482=ORIENTED_EDGE ( 'NONE', *, *, #11467, .T. ) ;
#13486=ADVANCED_FACE ( 'NONE', ( #10138 ), #763, .T. ) ;
#13492=CARTESIAN_POINT ( 'NONE',  ( 2.789999999999999147, 24.44424927289185945, -0.2301004812058395077 ) ) ;
#13495=B_SPLINE_CURVE_WITH_KNOTS ( 'NONE', 3,
 ( #14749, #3280, #14817, #2127 ),
 .UNSPECIFIED., .F., .F.,
 ( 4, 4 ),
 ( 0.005258110598983609975, 0.005948376585272729597 ),
 .UNSPECIFIED. ) ;
#13508=CARTESIAN_POINT ( 'NONE',  ( 0.000000000000000000, 23.48180575137729775, 5.535312321042836103 ) ) ;
#13515=CARTESIAN_POINT ( 'NONE',  ( 2.765633920072238183, 2.336989772644269436, 24.63872515616083447 ) ) ;
#13516=CARTESIAN_POINT ( 'NONE',  ( 0.02436607992776064838, 12.59161484032912171, 21.30679549418635688 ) ) ;
#13517=ADVANCED_FACE ( 'NONE', ( #3293 ), #7755, .F. ) ;
#13519=ORIENTED_EDGE ( 'NONE', *, *, #4266, .T. ) ;
#13520=DIRECTION ( 'NONE',  ( 0.000000000000000000, 0.000000000000000000, 1.000000000000000000 ) ) ;
#13521=CARTESIAN_POINT ( 'NONE',  ( 1.749999999999998002, 24.89775460606832524, 12.96210679857795256 ) ) ;
#13527=DIRECTION ( 'NONE',  ( -1.000000000000000000, -0.000000000000000000, -0.000000000000000000 ) ) ;
#13528=CARTESIAN_POINT ( 'NONE',  ( 1.039999999999997593, 0.000000000000000000, 0.000000000000000000 ) ) ;
#13529=CARTESIAN_POINT ( 'NONE',  ( 2.031033491000349134, 24.80232951178394885, -12.05173163741697451 ) ) ;
#13534=ORIENTED_EDGE ( 'NONE', *, *, #742, .T. ) ;
#13536=ORIENTED_EDGE ( 'NONE', *, *, #14074, .T. ) ;
#13537=ORIENTED_EDGE ( 'NONE', *, *, #4266, .F. ) ;
#13539=LINE ( 'NONE', #13459, #5061 ) ;
#13542=CARTESIAN_POINT ( 'NONE',  ( 4.424224194511527805E-17, 20.65025570340106853, -12.51972505884970488 ) ) ;
#13547=DIRECTION ( 'NONE',  ( -1.000000000000000000, -0.000000000000000000, -0.000000000000000000 ) ) ;
#13549=ORIENTED_EDGE ( 'NONE', *, *, #10773, .T. ) ;
#13552=CARTESIAN_POINT ( 'NONE',  ( 2.789999999999999147, -12.52067188844336165, -20.62201879784926462 ) ) ;
#13555=LINE ( 'NONE', #1963, #1934 ) ;
#13556=CIRCLE ( 'NONE', #7182, 24.12539914357697413 ) ;
#13559=CARTESIAN_POINT ( 'NONE',  ( 0.1855655959470664251, -17.45907811351468553, 19.17825124759772493 ) ) ;
#13560=EDGE_CURVE ( 'NONE', #7568, #13720, #11291, .T. ) ;
#13561=ORIENTED_EDGE ( 'NONE', *, *, #10613, .T. ) ;
#13563=EDGE_CURVE ( 'NONE', #14234, #446, #3136, .T. ) ;
#13565=DIRECTION ( 'NONE',  ( -1.000000000000000000, -0.000000000000000000, -0.000000000000000000 ) ) ;
#13570=ORIENTED_EDGE ( 'NONE', *, *, #876, .F. ) ;
#13578=CARTESIAN_POINT ( 'NONE',  ( 0.000000000000000000, 5.535312321042724193, 23.48180575137730841 ) ) ;
#13582=CYLINDRICAL_SURFACE ( 'NONE', #13797, 28.06981291497571362 ) ;
#13584=EDGE_LOOP ( 'NONE', ( #8146, #8430, #10169, #4 ) ) ;
#13585=EDGE_CURVE ( 'NONE', #14933, #10147, #12179, .T. ) ;
#13588=ORIENTED_EDGE ( 'NONE', *, *, #3917, .F. ) ;
#13592=CARTESIAN_POINT ( 'NONE',  ( 0.006974657972266078837, 5.408388659524427489, -23.92335783895632417 ) ) ;
#13594=CARTESIAN_POINT ( 'NONE',  ( 0.02436607992775978102, 24.63872515616082737, 2.336989772644355146 ) ) ;
#13595=ADVANCED_FACE ( 'NONE', ( #1998 ), #6681, .T. ) ;
#13596=EDGE_CURVE ( 'NONE', #807, #14075, #5110, .T. ) ;
#13598=CARTESIAN_POINT ( 'NONE',  ( 0.5279273746168616777, 26.57710921259767645, -4.996265754456091557 ) ) ;
#13601=VECTOR ( 'NONE', #12077, 1000.000000000000000 ) ;
#13605=EDGE_LOOP ( 'NONE', ( #4874, #14411, #2724, #11019, #14864, #2764, #12609 ) ) ;
#13606=ORIENTED_EDGE ( 'NONE', *, *, #5595, .T. ) ;
#13607=VERTEX_POINT ( 'NONE', #4917 ) ;
#13613=CARTESIAN_POINT ( 'NONE',  ( 0.000000000000000000, 7.909232158575156824, -24.34211360614291664 ) ) ;
#13619=FACE_OUTER_BOUND ( 'NONE', #8030, .T. ) ;
#13621=AXIS2_PLACEMENT_3D ( 'NONE', #13196, #352, #1748 ) ;
#13632=DIRECTION ( 'NONE',  ( -1.000000000000000000, -0.000000000000000000, -0.000000000000000000 ) ) ;
#13637=DIRECTION ( 'NONE',  ( 0.000000000000000000, 0.000000000000000000, 1.000000000000000000 ) ) ;
#13638=EDGE_LOOP ( 'NONE', ( #8207, #7244, #13875, #7770 ) ) ;
#13639=CARTESIAN_POINT ( 'NONE',  ( 0.02436607992776064838, 18.55949924794892780, 16.37294372382865504 ) ) ;
#13640=DIRECTION ( 'NONE',  ( 0.000000000000000000, 0.000000000000000000, 1.000000000000000000 ) ) ;
#13642=ADVANCED_FACE ( 'NONE', ( #15221 ), #4754, .F. ) ;
#13645=CARTESIAN_POINT ( 'NONE',  ( 2.601776105308175602, -25.78859396478526023, -2.857713464478961463 ) ) ;
#13647=VERTEX_POINT ( 'NONE', #4690 ) ;
#13655=AXIS2_PLACEMENT_3D ( 'NONE', #5750, #1563, #8475 ) ;
#13656=CARTESIAN_POINT ( 'NONE',  ( 2.789999999999999147, 1.991882183130632589, -24.04302995059963877 ) ) ;
#13657=DIRECTION ( 'NONE',  ( 0.000000000000000000, 0.000000000000000000, 1.000000000000000000 ) ) ;
#13661=CARTESIAN_POINT ( 'NONE',  ( 2.789999999999999147, -12.59161484032896361, -21.30679549418645280 ) ) ;
#13666=CARTESIAN_POINT ( 'NONE',  ( -5.209999999999999964, 0.000000000000000000, 0.000000000000000000 ) ) ;
#13668=AXIS2_PLACEMENT_3D ( 'NONE', #4856, #6996, #4707 ) ;
#13670=ORIENTED_EDGE ( 'NONE', *, *, #15215, .F. ) ;
#13673=CARTESIAN_POINT ( 'NONE',  ( 2.789999999999999147, -15.04425356660744839, -18.18163861606288378 ) ) ;
#13674=ADVANCED_FACE ( 'NONE', ( #9359 ), #7281, .T. ) ;
#13675=DIRECTION ( 'NONE',  ( -1.000000000000000000, -0.000000000000000000, -0.000000000000000000 ) ) ;
#13677=CARTESIAN_POINT ( 'NONE',  ( 0.02436607992776238310, -12.59161484032927092, 21.30679549418627161 ) ) ;
#13679=EDGE_CURVE ( 'NONE', #12512, #316, #12926, .T. ) ;
#13680=DIRECTION ( 'NONE',  ( -1.000000000000000000, -0.000000000000000000, -0.000000000000000000 ) ) ;
#13683=CARTESIAN_POINT ( 'NONE',  ( 0.000000000000000000, 24.04302995059966364, -1.991882183130399664 ) ) ;
#13685=CIRCLE ( 'NONE', #14438, 28.06981291497571007 ) ;
#13690=B_SPLINE_CURVE_WITH_KNOTS ( 'NONE', 3,
 ( #4923, #9366, #2295, #5917, #11743, #13037 ),
 .UNSPECIFIED., .F., .F.,
 ( 4, 2, 4 ),
 ( 2.132675795045741476E-07, 0.001878604073277002386, 0.003756994878974500435 ),
 .UNSPECIFIED. ) ;
#13692=EDGE_CURVE ( 'NONE', #9808, #14563, #6320, .T. ) ;
#13693=ORIENTED_EDGE ( 'NONE', *, *, #2983, .T. ) ;
#13694=ORIENTED_EDGE ( 'NONE', *, *, #5278, .F. ) ;
#13702=CARTESIAN_POINT ( 'NONE',  ( 2.789999999999999147, 9.324097380959445402, 22.25075486061742325 ) ) ;
#13706=CIRCLE ( 'NONE', #7819, 28.06981291497571007 ) ;
#13709=TOROIDAL_SURFACE ( 'NONE', #2801, 24.12539914357697768, 8.000000000000000000 ) ;
#13710=AXIS2_PLACEMENT_3D ( 'NONE', #13411, #7430, #2889 ) ;
#13714=B_SPLINE_CURVE_WITH_KNOTS ( 'NONE', 3,
 ( #8721, #339, #2742, #2894 ),
 .UNSPECIFIED., .F., .F.,
 ( 4, 4 ),
 ( 0.005258110598983608240, 0.005948376585272733934 ),
 .UNSPECIFIED. ) ;
#13717=EDGE_CURVE ( 'NONE', #2934, #1779, #13029, .T. ) ;
#13720=VERTEX_POINT ( 'NONE', #197 ) ;
#13723=CIRCLE ( 'NONE', #5113, 2.524999999999995470 ) ;
#13725=CARTESIAN_POINT ( 'NONE',  ( 2.765633920072235519, 9.836394144776026138, -22.71065055754441531 ) ) ;
#13727=VERTEX_POINT ( 'NONE', #3740 ) ;
#13730=VERTEX_POINT ( 'NONE', #8418 ) ;
#13732=DIRECTION ( 'NONE',  ( 0.000000000000000000, 0.000000000000000000, 1.000000000000000000 ) ) ;
#13745=ORIENTED_EDGE ( 'NONE', *, *, #434, .T. ) ;
#13746=EDGE_CURVE ( 'NONE', #1373, #3861, #11264, .T. ) ;
#13751=DIRECTION ( 'NONE',  ( 0.000000000000000000, 0.000000000000000000, 1.000000000000000000 ) ) ;
#13758=CARTESIAN_POINT ( 'NONE',  ( 2.789999999999999147, -18.28042085475289369, 15.74360496233375173 ) ) ;
#13759=CARTESIAN_POINT ( 'NONE',  ( 2.430066721642811345, 23.15620303736532293, 12.90954937922509238 ) ) ;
#13764=EDGE_CURVE ( 'NONE', #5744, #4588, #11536, .T. ) ;
#13766=SHAPE_REPRESENTATION_RELATIONSHIP ( 'NONE' , 'NONE' ,  #14263, #1226 ) ;
#13767=B_SPLINE_CURVE_WITH_KNOTS ( 'NONE', 3,
 ( #11782, #5951, #12783, #2267, #12853, #6953 ),
 .UNSPECIFIED., .F., .F.,
 ( 4, 2, 4 ),
 ( 4.462636808935014747E-07, 0.001879885123572234236, 0.003759323983463574645 ),
 .UNSPECIFIED. ) ;
#13771=CARTESIAN_POINT ( 'NONE',  ( 2.765633920072235963, 24.63872515616082737, 2.336989772644355146 ) ) ;
#13773=CARTESIAN_POINT ( 'NONE',  ( 1.394999999999999574, -27.76164181293054511, 4.147968289691193355 ) ) ;
#13774=ADVANCED_FACE ( 'NONE', ( #6278 ), #8275, .T. ) ;
#13775=EDGE_LOOP ( 'NONE', ( #3804, #6192, #10491, #8247 ) ) ;
#13779=EDGE_CURVE ( 'NONE', #6121, #1565, #922, .T. ) ;
#13780=VERTEX_POINT ( 'NONE', #4053 ) ;
#13783=ORIENTED_EDGE ( 'NONE', *, *, #13166, .F. ) ;
#13790=CARTESIAN_POINT ( 'NONE',  ( 2.789999999999999147, 22.25075486061738772, 9.324097380959527115 ) ) ;
#13794=DIRECTION ( 'NONE',  ( 0.000000000000000000, 0.000000000000000000, 1.000000000000000000 ) ) ;
#13795=CARTESIAN_POINT ( 'NONE',  ( 2.257825467309738876, -26.83036154824992536, -3.467596033028569114 ) ) ;
#13796=VERTEX_POINT ( 'NONE', #270 ) ;
#13797=AXIS2_PLACEMENT_3D ( 'NONE', #4449, #3061, #11501 ) ;
#13799=EDGE_CURVE ( 'NONE', #4798, #2853, #7793, .T. ) ;
#13801=CYLINDRICAL_SURFACE ( 'NONE', #2406, 13.19999999999999929 ) ;
#13802=EDGE_CURVE ( 'NONE', #4132, #13815, #9655, .T. ) ;
#13804=CARTESIAN_POINT ( 'NONE',  ( 0.000000000000000000, -20.62201879784905501, -12.52067188844372936 ) ) ;
#13811=VECTOR ( 'NONE', #1955, 1000.000000000000000 ) ;
#13812=DIRECTION ( 'NONE',  ( -1.000000000000000000, 0.000000000000000000, 0.000000000000000000 ) ) ;
#13815=VERTEX_POINT ( 'NONE', #8727 ) ;
#13817=CARTESIAN_POINT ( 'NONE',  ( 2.604434261026090436, 5.253342437940084153, -25.39738473784996131 ) ) ;
#13818=EDGE_LOOP ( 'NONE', ( #1599, #10317, #8768, #3678 ) ) ;
#13822=ORIENTED_EDGE ( 'NONE', *, *, #9318, .T. ) ;
#13823=DIRECTION ( 'NONE',  ( 0.000000000000000000, 0.000000000000000000, 1.000000000000000000 ) ) ;
#13835=CARTESIAN_POINT ( 'NONE',  ( 2.789999999999999147, 15.04425356660790136, -20.70663861606255196 ) ) ;
#13837=B_SPLINE_CURVE_WITH_KNOTS ( 'NONE', 3,
 ( #315, #14321, #3784, #9860 ),
 .UNSPECIFIED., .F., .F.,
 ( 4, 4 ),
 ( 0.005258110598983608240, 0.005948376585272733066 ),
 .UNSPECIFIED. ) ;
#13838=CARTESIAN_POINT ( 'NONE',  ( 2.789999999999999147, -24.44424927289185590, 12.96989951879399072 ) ) ;
#13839=EDGE_CURVE ( 'NONE', #2696, #11370, #14293, .T. ) ;
#13843=ORIENTED_EDGE ( 'NONE', *, *, #1648, .F. ) ;
#13844=CIRCLE ( 'NONE', #7951, 28.06981291497571007 ) ;
#13846=DIRECTION ( 'NONE',  ( -1.000000000000000000, -0.000000000000000000, -0.000000000000000000 ) ) ;
#13851=ORIENTED_EDGE ( 'NONE', *, *, #5247, .T. ) ;
#13853=DIRECTION ( 'NONE',  ( -1.000000000000000000, 0.000000000000000000, 0.000000000000000000 ) ) ;
#13854=VERTEX_POINT ( 'NONE', #11270 ) ;
#13857=AXIS2_PLACEMENT_3D ( 'NONE', #1902, #8961, #6595 ) ;
#13862=CARTESIAN_POINT ( 'NONE',  ( 2.604434404052932805, -19.17825124759790256, 17.45907811351449368 ) ) ;
#13863=CARTESIAN_POINT ( 'NONE',  ( 0.02436607992776498519, 9.836394144775706394, 22.71065055754456097 ) ) ;
#13865=EDGE_LOOP ( 'NONE', ( #10205, #1232, #14253, #6232, #11559, #14330 ) ) ;
#13866=CARTESIAN_POINT ( 'NONE',  ( 0.000000000000000000, 15.04425356660790136, -20.70663861606255196 ) ) ;
#13867=DIRECTION ( 'NONE',  ( -1.000000000000000000, -0.000000000000000000, -0.000000000000000000 ) ) ;
#13868=VERTEX_POINT ( 'NONE', #5445 ) ;
#13869=AXIS2_PLACEMENT_3D ( 'NONE', #9105, #15024, #8020 ) ;
#13873=ADVANCED_FACE ( 'NONE', ( #3046 ), #10192, .T. ) ;
#13874=AXIS2_PLACEMENT_3D ( 'NONE', #12066, #11836, #4948 ) ;
#13875=ORIENTED_EDGE ( 'NONE', *, *, #7954, .T. ) ;
#13878=DIRECTION ( 'NONE',  ( 0.000000000000000000, 0.000000000000000000, 1.000000000000000000 ) ) ;
#13885=LINE ( 'NONE', #7903, #12798 ) ;
#13891=CARTESIAN_POINT ( 'NONE',  ( 0.000000000000000000, 2.680914349914567470E-13, -25.59481291497571220 ) ) ;
#13894=EDGE_LOOP ( 'NONE', ( #6753, #13670, #4634, #8166 ) ) ;
#13896=AXIS2_PLACEMENT_3D ( 'NONE', #14528, #6297, #2609 ) ;
#13897=CARTESIAN_POINT ( 'NONE',  ( 2.262072661820536013, 26.82026385750178932, -3.461047254864356049 ) ) ;
#13903=DIRECTION ( 'NONE',  ( 0.000000000000000000, 0.000000000000000000, 1.000000000000000000 ) ) ;
#13906=CARTESIAN_POINT ( 'NONE',  ( 2.789999999999999147, 18.55949924794916228, -16.37294372382838148 ) ) ;
#13911=AXIS2_PLACEMENT_3D ( 'NONE', #6481, #13317, #12249 ) ;
#13915=VECTOR ( 'NONE', #10715, 1000.000000000000000 ) ;
#13916=PRESENTATION_STYLE_ASSIGNMENT (( #5554 ) ) ;
#13918=VERTEX_POINT ( 'NONE', #14884 ) ;
#13922=CARTESIAN_POINT ( 'NONE',  ( 2.790000000000000036, 0.000000000000000000, 0.000000000000000000 ) ) ;
#13923=DIRECTION ( 'NONE',  ( -1.000000000000000000, 0.000000000000000000, 0.000000000000000000 ) ) ;
#13924=CARTESIAN_POINT ( 'NONE',  ( 2.789999999999999147, -21.30679549418640306, 12.59161484032904887 ) ) ;
#13925=AXIS2_PLACEMENT_3D ( 'NONE', #4280, #12572, #6887 ) ;
#13928=DIRECTION ( 'NONE',  ( 1.000000000000000000, 0.000000000000000000, 0.000000000000000000 ) ) ;
#13932=AXIS2_PLACEMENT_3D ( 'NONE', #2500, #7115, #15202 ) ;
#13933=CARTESIAN_POINT ( 'NONE',  ( 0.7589665349472707323, -4.828387785247840291, -27.14933624560912762 ) ) ;
#13934=CARTESIAN_POINT ( 'NONE',  ( 2.789999999999999147, -24.04302995059964587, -1.991882183130548878 ) ) ;
#13938=ORIENTED_EDGE ( 'NONE', *, *, #2059, .F. ) ;
#13939=TOROIDAL_SURFACE ( 'NONE', #10508, 24.12539914357697413, 8.000000000000000000 ) ;
#13945=CARTESIAN_POINT ( 'NONE',  ( 0.000000000000000000, 24.04302995059966364, -1.991882183130399664 ) ) ;
#13946=EDGE_CURVE ( 'NONE', #5632, #10903, #14186, .T. ) ;
#13948=DIRECTION ( 'NONE',  ( -1.000000000000000000, 0.000000000000000000, 0.000000000000000000 ) ) ;
#13949=VECTOR ( 'NONE', #2347, 1000.000000000000000 ) ;
#13950=ORIENTED_EDGE ( 'NONE', *, *, #6239, .F. ) ;
#13952=EDGE_CURVE ( 'NONE', #5611, #4786, #8598, .T. ) ;
#13955=B_SPLINE_CURVE_WITH_KNOTS ( 'NONE', 3,
 ( #6253, #11090, #7566, #10932, #400, #1417 ),
 .UNSPECIFIED., .F., .F.,
 ( 4, 2, 4 ),
 ( 2.032124546190077199E-07, 0.001878594002992309232, 0.003756984793529999193 ),
 .UNSPECIFIED. ) ;
#13959=CARTESIAN_POINT ( 'NONE',  ( 0.02436607992776325046, -24.15498966839958683, -5.391175441198872598 ) ) ;
#13972=DIRECTION ( 'NONE',  ( -1.000000000000000000, -0.000000000000000000, -0.000000000000000000 ) ) ;
#13976=VERTEX_POINT ( 'NONE', #1042 ) ;
#13977=EDGE_LOOP ( 'NONE', ( #11182, #12064, #7588, #5812 ) ) ;
#13980=CARTESIAN_POINT ( 'NONE',  ( 2.765633920072238183, -5.391175441198789109, 24.15498966839961170 ) ) ;
#13982=CARTESIAN_POINT ( 'NONE',  ( 0.02436607992776758727, 24.15498966839963302, 5.391175441198700291 ) ) ;
#13983=EDGE_CURVE ( 'NONE', #552, #13334, #5671, .T. ) ;
#13988=EDGE_CURVE ( 'NONE', #7573, #3010, #11345, .T. ) ;
#13992=ORIENTED_EDGE ( 'NONE', *, *, #11479, .F. ) ;
#13994=ORIENTED_EDGE ( 'NONE', *, *, #11467, .F. ) ;
#13995=ORIENTED_EDGE ( 'NONE', *, *, #7233, .T. ) ;
#13996=VECTOR ( 'NONE', #11643, 1000.000000000000000 ) ;
#14000=CARTESIAN_POINT ( 'NONE',  ( 0.02436607992775891365, -24.63872515616080960, -2.336989772644527008 ) ) ;
#14004=CARTESIAN_POINT ( 'NONE',  ( 0.02436607992775761261, 22.71065055754452544, 9.836394144775786330 ) ) ;
#14010=ORIENTED_EDGE ( 'NONE', *, *, #13035, .F. ) ;
#14012=B_SPLINE_CURVE_WITH_KNOTS ( 'NONE', 3,
 ( #13301, #706, #8771, #13460, #2941, #7700 ),
 .UNSPECIFIED., .F., .F.,
 ( 4, 2, 4 ),
 ( 4.462636793130641501E-07, 0.001879885123570645879, 0.003759323983461978699 ),
 .UNSPECIFIED. ) ;
#14013=CARTESIAN_POINT ( 'NONE',  ( 0.8291131470075020493, -24.44424927289185590, 12.96989951879399072 ) ) ;
#14014=ORIENTED_EDGE ( 'NONE', *, *, #5920, .F. ) ;
#14016=CARTESIAN_POINT ( 'NONE',  ( 0.000000000000000000, -1.991882183130148087, -24.04302995059968140 ) ) ;
#14033=ORIENTED_EDGE ( 'NONE', *, *, #10856, .F. ) ;
#14038=AXIS2_PLACEMENT_3D ( 'NONE', #14824, #5527, #1911 ) ;
#14044=CARTESIAN_POINT ( 'NONE',  ( 2.783025325906567371, 2.249040938978837278, -24.42374957165203142 ) ) ;
#14046=CARTESIAN_POINT ( 'NONE',  ( -10.00000000000000000, 0.000000000000000000, 0.000000000000000000 ) ) ;
#14047=CARTESIAN_POINT ( 'NONE',  ( 2.030753602223783538, 4.828194074574346573, 27.14986936243576565 ) ) ;
#14049=CIRCLE ( 'NONE', #2511, 24.12539914357697413 ) ;
#14055=CARTESIAN_POINT ( 'NONE',  ( 0.006974663525958337516, -12.53640742967767885, 21.08118142846899801 ) ) ;
#14056=ORIENTED_EDGE ( 'NONE', *, *, #5242, .T. ) ;
#14070=LINE ( 'NONE', #2394, #11519 ) ;
#14074=EDGE_CURVE ( 'NONE', #3861, #13918, #7333, .T. ) ;
#14075=VERTEX_POINT ( 'NONE', #6339 ) ;
#14079=ORIENTED_EDGE ( 'NONE', *, *, #3826, .F. ) ;
#14082=B_SPLINE_CURVE_WITH_KNOTS ( 'NONE', 3,
 ( #1835, #13283, #1612, #14373 ),
 .UNSPECIFIED., .F., .F.,
 ( 4, 4 ),
 ( 3.059063720795852959E-07, 0.0006888942284914018055 ),
 .UNSPECIFIED. ) ;
#14085=VERTEX_POINT ( 'NONE', #7351 ) ;
#14087=B_SPLINE_CURVE_WITH_KNOTS ( 'NONE', 3,
 ( #9791, #8467, #14488, #6020 ),
 .UNSPECIFIED., .F., .F.,
 ( 4, 4 ),
 ( 0.005258105385878687407, 0.005948373736081388405 ),
 .UNSPECIFIED. ) ;
#14088=CARTESIAN_POINT ( 'NONE',  ( 2.262072706628479146, -19.66369668717046437, 18.56460150496932116 ) ) ;
#14089=AXIS2_PLACEMENT_3D ( 'NONE', #7327, #3546, #10698 ) ;
#14093=ORIENTED_EDGE ( 'NONE', *, *, #14618, .T. ) ;
#14096=LINE ( 'NONE', #1112, #13915 ) ;
#14097=ORIENTED_EDGE ( 'NONE', *, *, #6466, .T. ) ;
#14101=CARTESIAN_POINT ( 'NONE',  ( 2.789999999999999147, -12.59161484032927092, 21.30679549418627161 ) ) ;
#14105=CARTESIAN_POINT ( 'NONE',  ( 0.02436607992775934733, -21.30679549418640306, 12.59161484032904887 ) ) ;
#14107=CARTESIAN_POINT ( 'NONE',  ( 0.000000000000000000, -18.28042085475288303, 15.74360496233377305 ) ) ;
#14109=LINE ( 'NONE', #8123, #14202 ) ;
#14114=AXIS2_PLACEMENT_3D ( 'NONE', #8339, #11856, #10642 ) ;
#14118=ORIENTED_EDGE ( 'NONE', *, *, #8052, .T. ) ;
#14121=CARTESIAN_POINT ( 'NONE',  ( 2.789999999999999147, 0.000000000000000000, 0.000000000000000000 ) ) ;
#14122=CARTESIAN_POINT ( 'NONE',  ( 0.006974657972265168107, -5.408388659524262287, 23.92335783895635970 ) ) ;
#14126=CARTESIAN_POINT ( 'NONE',  ( 2.601776091974069338, 5.251266773802368171, 25.40949241676355541 ) ) ;
#14131=ORIENTED_EDGE ( 'NONE', *, *, #13799, .T. ) ;
#14135=ORIENTED_EDGE ( 'NONE', *, *, #876, .T. ) ;
#14137=EDGE_CURVE ( 'NONE', #1390, #6218, #4869, .T. ) ;
#14140=ORIENTED_EDGE ( 'NONE', *, *, #10030, .F. ) ;
#14142=LINE ( 'NONE', #9531, #3854 ) ;
#14143=DIRECTION ( 'NONE',  ( -1.000000000000000000, 0.000000000000000000, 0.000000000000000000 ) ) ;
#14144=EDGE_CURVE ( 'NONE', #11100, #12913, #6040, .T. ) ;
#14149=CIRCLE ( 'NONE', #2125, 28.06981291497571007 ) ;
#14153=AXIS2_PLACEMENT_3D ( 'NONE', #4733, #8111, #9561 ) ;
#14157=AXIS2_PLACEMENT_3D ( 'NONE', #462, #1850, #14387 ) ;
#14159=CARTESIAN_POINT ( 'NONE',  ( 1.749999999999998002, 12.52377138324259143, -25.12109765559640451 ) ) ;
#14161=VERTEX_POINT ( 'NONE', #5561 ) ;
#14163=TOROIDAL_SURFACE ( 'NONE', #10961, 24.12539914357697413, 8.000000000000000000 ) ;
#14166=ADVANCED_FACE ( 'NONE', ( #12321, #11457 ), #9234, .F. ) ;
#14168=CIRCLE ( 'NONE', #13434, 28.06981291497571362 ) ;
#14172=CARTESIAN_POINT ( 'NONE',  ( 0.02436607992776498519, 9.836394144775706394, 22.71065055754456097 ) ) ;
#14173=CARTESIAN_POINT ( 'NONE',  ( 2.789999999999999147, 24.44424927289185945, 12.96989951879416125 ) ) ;
#14175=ORIENTED_EDGE ( 'NONE', *, *, #14545, .T. ) ;
#14177=DIRECTION ( 'NONE',  ( -1.000000000000000000, -0.000000000000000000, -0.000000000000000000 ) ) ;
#14179=AXIS2_PLACEMENT_3D ( 'NONE', #5295, #1746, #13339 ) ;
#14186=CIRCLE ( 'NONE', #15175, 24.12539914357697413 ) ;
#14189=CARTESIAN_POINT ( 'NONE',  ( 0.0003207540509378258692, 20.70663861606293921, -12.51925356660738053 ) ) ;
#14193=CARTESIAN_POINT ( 'NONE',  ( 1.749999999999998002, 20.02152543075346003, 19.67366047555537634 ) ) ;
#14195=CARTESIAN_POINT ( 'NONE',  ( 1.394999999999999574, -24.89775460606823287, -12.96210679857813908 ) ) ;
#14196=DIRECTION ( 'NONE',  ( -1.000000000000000000, -0.000000000000000000, -0.000000000000000000 ) ) ;
#14202=VECTOR ( 'NONE', #12725, 1000.000000000000000 ) ;
#14208=CARTESIAN_POINT ( 'NONE',  ( 8.000000000000000000, 0.000000000000000000, 0.000000000000000000 ) ) ;
#14209=B_SPLINE_CURVE_WITH_KNOTS ( 'NONE', 3,
 ( #4637, #2699, #11900, #5011, #13130, #3530 ),
 .UNSPECIFIED., .F., .F.,
 ( 4, 2, 4 ),
 ( 2.586195665699493951E-07, 0.001878649493629688805, 0.003757040367692807744 ),
 .UNSPECIFIED. ) ;
#14215=CARTESIAN_POINT ( 'NONE',  ( 0.000000000000000000, -20.70663861606260170, -15.04425356660783031 ) ) ;
#14216=CARTESIAN_POINT ( 'NONE',  ( 0.006931038682727856497, -12.53626894672812853, -21.08061549536629187 ) ) ;
#14217=AXIS2_PLACEMENT_3D ( 'NONE', #8406, #1344, #1657 ) ;
#14224=ORIENTED_EDGE ( 'NONE', *, *, #146, .T. ) ;
#14226=CARTESIAN_POINT ( 'NONE',  ( 1.394999999999999574, 27.68468304288259318, 4.633866840649019103 ) ) ;
#14227=CARTESIAN_POINT ( 'NONE',  ( 1.039999999999999369, -12.52377138324206918, -25.12109765559666741 ) ) ;
#14229=CIRCLE ( 'NONE', #2939, 28.06981291497571362 ) ;
#14231=CARTESIAN_POINT ( 'NONE',  ( 2.765633920072234631, 16.37294372382885044, -18.55949924794875017 ) ) ;
#14233=EDGE_CURVE ( 'NONE', #5968, #11548, #14646, .T. ) ;
#14234=VERTEX_POINT ( 'NONE', #10381 ) ;
#14239=CARTESIAN_POINT ( 'NONE',  ( 2.257825491203654611, 24.44564404695844573, 11.58891744060115947 ) ) ;
#14242=EDGE_CURVE ( 'NONE', #10147, #9857, #934, .T. ) ;
#14244=VERTEX_POINT ( 'NONE', #12827 ) ;
#14251=CARTESIAN_POINT ( 'NONE',  ( 2.789999999999999147, 0.000000000000000000, 0.000000000000000000 ) ) ;
#14253=ORIENTED_EDGE ( 'NONE', *, *, #14847, .F. ) ;
#14255=VERTEX_POINT ( 'NONE', #10237 ) ;
#14256=ORIENTED_EDGE ( 'NONE', *, *, #6381, .F. ) ;
#14258=DIRECTION ( 'NONE',  ( -1.000000000000000000, 0.000000000000000000, -0.000000000000000000 ) ) ;
#14263=SHAPE_REPRESENTATION ( 'short pitch roller chain wheel_s_iso_Chain wheel ISO - 20Z 05B-1 --20SA8.0N', ( #1376 ), #11929 ) ;
#14270=CARTESIAN_POINT ( 'NONE',  ( 0.0001048950922011769414, -20.67847077765692632, -12.51925356660783351 ) ) ;
#14273=VERTEX_POINT ( 'NONE', #5862 ) ;
#14274=EDGE_CURVE ( 'NONE', #1566, #1423, #6077, .T. ) ;
#14278=ADVANCED_FACE ( 'NONE', ( #2390 ), #7324, .T. ) ;
#14280=CARTESIAN_POINT ( 'NONE',  ( 2.789999999999999147, -15.04425356660744839, -20.70663861606288236 ) ) ;
#14283=ORIENTED_EDGE ( 'NONE', *, *, #13679, .F. ) ;
#14288=CARTESIAN_POINT ( 'NONE',  ( 0.000000000000000000, 0.000000000000000000, 4.000000000000000000 ) ) ;
#14291=CARTESIAN_POINT ( 'NONE',  ( 0.000000000000000000, -12.52067188844364587, 20.62201879784910119 ) ) ;
#14293=B_SPLINE_CURVE_WITH_KNOTS ( 'NONE', 3,
 ( #2901, #6426, #11340, #965, #10115, #11490 ),
 .UNSPECIFIED., .F., .F.,
 ( 4, 2, 4 ),
 ( 2.132675795051084930E-07, 0.001878604073277006722, 0.003756994878974508241 ),
 .UNSPECIFIED. ) ;
#14306=CARTESIAN_POINT ( 'NONE',  ( 0.000000000000000000, -20.62201879784923264, 12.52067188844344336 ) ) ;
#14308=AXIS2_PLACEMENT_3D ( 'NONE', #11927, #14560, #8628 ) ;
#14309=B_SPLINE_CURVE_WITH_KNOTS ( 'NONE', 3,
 ( #5747, #3362, #9416, #10733, #7195, #3505 ),
 .UNSPECIFIED., .F., .F.,
 ( 4, 2, 4 ),
 ( 4.462636793131339774E-07, 0.001879885123570645012, 0.003759323983461976965 ),
 .UNSPECIFIED. ) ;
#14310=B_SPLINE_CURVE_WITH_KNOTS ( 'NONE', 3,
 ( #4861, #12983, #11980, #1386 ),
 .UNSPECIFIED., .F., .F.,
 ( 4, 4 ),
 ( 0.005258110598983628189, 0.005948376585272736536 ),
 .UNSPECIFIED. ) ;
#14318=ORIENTED_EDGE ( 'NONE', *, *, #8964, .F. ) ;
#14319=CARTESIAN_POINT ( 'NONE',  ( 2.789999999999999147, -23.48180575137726223, -5.535312321042966666 ) ) ;
#14320=CARTESIAN_POINT ( 'NONE',  ( 0.07186813532171169860, -2.577209017047189299, 25.22589920183361301 ) ) ;
#14321=CARTESIAN_POINT ( 'NONE',  ( 2.790000000000000480, 15.96500990068124715, 18.34424029220116736 ) ) ;
#14325=FACE_OUTER_BOUND ( 'NONE', #4031, .T. ) ;
#14329=VERTEX_POINT ( 'NONE', #60 ) ;
#14330=ORIENTED_EDGE ( 'NONE', *, *, #8292, .F. ) ;
#14333=CARTESIAN_POINT ( 'NONE',  ( 1.039999999999996261, 12.96210679857786197, 24.89775460606836788 ) ) ;
#14334=EDGE_CURVE ( 'NONE', #3966, #5767, #691, .T. ) ;
#14341=FACE_OUTER_BOUND ( 'NONE', #12855, .T. ) ;
#14342=TOROIDAL_SURFACE ( 'NONE', #9914, 24.12539914357697768, 8.000000000000000000 ) ;
#14349=ORIENTED_EDGE ( 'NONE', *, *, #13585, .T. ) ;
#14355=CARTESIAN_POINT ( 'NONE',  ( 0.07186808533286707934, 10.24630254990548650, -23.19485392143201707 ) ) ;
#14357=FACE_OUTER_BOUND ( 'NONE', #11230, .T. ) ;
#14361=CARTESIAN_POINT ( 'NONE',  ( 1.039999999999996705, -20.02152543075331081, -19.67366047555552555 ) ) ;
#14362=CARTESIAN_POINT ( 'NONE',  ( 1.039999999999999369, -12.52377138324206918, -25.12109765559666741 ) ) ;
#14363=AXIS2_PLACEMENT_3D ( 'NONE', #14046, #8281, #5915 ) ;
#14366=VERTEX_POINT ( 'NONE', #14227 ) ;
#14368=CARTESIAN_POINT ( 'NONE',  ( 2.765633920072242624, 9.836394144775706394, 22.71065055754456097 ) ) ;
#14373=CARTESIAN_POINT ( 'NONE',  ( 0.000000000000000000, 22.25075486061751207, -9.324097380959241121 ) ) ;
#14376=ORIENTED_EDGE ( 'NONE', *, *, #3663, .F. ) ;
#14377=DIRECTION ( 'NONE',  ( 0.000000000000000000, 0.000000000000000000, 1.000000000000000000 ) ) ;
#14380=VECTOR ( 'NONE', #5253, 1000.000000000000000 ) ;
#14382=DIRECTION ( 'NONE',  ( -1.000000000000000000, -0.000000000000000000, -0.000000000000000000 ) ) ;
#14385=CARTESIAN_POINT ( 'NONE',  ( 1.749999999999998002, 20.02152543075374069, -19.67366047555509212 ) ) ;
#14387=DIRECTION ( 'NONE',  ( 0.000000000000000000, 0.000000000000000000, 1.000000000000000000 ) ) ;
#14389=B_SPLINE_CURVE_WITH_KNOTS ( 'NONE', 3,
 ( #10937, #12399, #4028, #11021 ),
 .UNSPECIFIED., .F., .F.,
 ( 4, 4 ),
 ( 0.005258110598983589158, 0.005948376585272731332 ),
 .UNSPECIFIED. ) ;
#14400=ORIENTED_EDGE ( 'NONE', *, *, #6970, .F. ) ;
#14401=CARTESIAN_POINT ( 'NONE',  ( 0.0003207540509378258692, 20.70663861606293921, -12.51925356660738053 ) ) ;
#14408=EDGE_CURVE ( 'NONE', #495, #14244, #14811, .T. ) ;
#14411=ORIENTED_EDGE ( 'NONE', *, *, #13027, .F. ) ;
#14418=AXIS2_PLACEMENT_3D ( 'NONE', #13866, #6499, #4664 ) ;
#14420=ADVANCED_FACE ( 'NONE', ( #5239 ), #5319, .T. ) ;
#14421=B_SPLINE_CURVE_WITH_KNOTS ( 'NONE', 3,
 ( #7791, #14863, #866, #14948, #4257, #14787, #3253, #10091 ),
 .UNSPECIFIED., .F., .F.,
 ( 4, 2, 2, 4 ),
 ( 2.032124546156068561E-07, 0.001631739532304432192, 0.002447507692229335726, 0.003263275852154239043 ),
 .UNSPECIFIED. ) ;
#14424=AXIS2_PLACEMENT_3D ( 'NONE', #5068, #3906, #12034 ) ;
#14425=EDGE_CURVE ( 'NONE', #4113, #11392, #8947, .T. ) ;
#14430=DIRECTION ( 'NONE',  ( 0.000000000000000000, 0.9510565162951567508, -0.3090169943749379589 ) ) ;
#14433=EDGE_CURVE ( 'NONE', #2534, #13239, #3930, .T. ) ;
#14435=ORIENTED_EDGE ( 'NONE', *, *, #8691, .F. ) ;
#14438=AXIS2_PLACEMENT_3D ( 'NONE', #3723, #11715, #9274 ) ;
#14441=CARTESIAN_POINT ( 'NONE',  ( 1.749999999999998002, -4.147968289691086774, -27.76164181293056288 ) ) ;
#14442=CYLINDRICAL_SURFACE ( 'NONE', #1100, 13.19999999999999929 ) ;
#14445=EDGE_CURVE ( 'NONE', #14273, #12521, #3161, .T. ) ;
#14451=CARTESIAN_POINT ( 'NONE',  ( 2.789999999999999591, 2.133490293297010343, 24.22479935914660132 ) ) ;
#14453=CARTESIAN_POINT ( 'NONE',  ( 2.765633920072234631, -21.30679549418640306, 12.59161484032904887 ) ) ;
#14455=EDGE_CURVE ( 'NONE', #14511, #10310, #1608, .T. ) ;
#14459=ORIENTED_EDGE ( 'NONE', *, *, #12009, .T. ) ;
#14465=DIRECTION ( 'NONE',  ( -1.000000000000000000, -0.000000000000000000, 0.000000000000000000 ) ) ;
#14466=DIRECTION ( 'NONE',  ( -1.000000000000000000, -0.000000000000000000, -0.000000000000000000 ) ) ;
#14469=EDGE_CURVE ( 'NONE', #3403, #6654, #10421, .T. ) ;
#14475=CARTESIAN_POINT ( 'NONE',  ( 0.006930995026448713570, 5.408431875071442185, 23.92277630352796791 ) ) ;
#14488=CARTESIAN_POINT ( 'NONE',  ( 2.783068888626319293, -22.53293026234510776, 9.685942809246967045 ) ) ;
#14490=ADVANCED_FACE ( 'NONE', ( #7541 ), #523, .T. ) ;
#14491=CARTESIAN_POINT ( 'NONE',  ( 0.7592463965288815952, 12.98165646470117274, -24.32906614999601302 ) ) ;
#14506=DIRECTION ( 'NONE',  ( 0.000000000000000000, 0.000000000000000000, 1.000000000000000000 ) ) ;
#14511=VERTEX_POINT ( 'NONE', #3297 ) ;
#14521=CARTESIAN_POINT ( 'NONE',  ( 0.5279272933715204452, -19.66369668717018726, -18.56460150496961248 ) ) ;
#14528=CARTESIAN_POINT ( 'NONE',  ( 1.749999999999998002, 0.000000000000000000, 0.000000000000000000 ) ) ;
#14531=ORIENTED_EDGE ( 'NONE', *, *, #520, .T. ) ;
#14532=DIRECTION ( 'NONE',  ( -1.000000000000000000, -0.000000000000000000, -0.000000000000000000 ) ) ;
#14537=EDGE_CURVE ( 'NONE', #5734, #1566, #13706, .T. ) ;
#14539=ORIENTED_EDGE ( 'NONE', *, *, #4622, .F. ) ;
#14540=B_SPLINE_CURVE_WITH_KNOTS ( 'NONE', 3,
 ( #14004, #5644, #6703, #10318, #11383, #4559 ),
 .UNSPECIFIED., .F., .F.,
 ( 4, 2, 4 ),
 ( 2.586195665686417350E-07, 0.001878649493629684251, 0.003757040367692799938 ),
 .UNSPECIFIED. ) ;
#14541=DIRECTION ( 'NONE',  ( 0.000000000000000000, 0.000000000000000000, 1.000000000000000000 ) ) ;
#14545=EDGE_CURVE ( 'NONE', #1997, #14980, #10517, .T. ) ;
#14548=ORIENTED_EDGE ( 'NONE', *, *, #14455, .T. ) ;
#14549=CARTESIAN_POINT ( 'NONE',  ( 0.000000000000000000, -7.909232158574647009, -21.81711360614308148 ) ) ;
#14552=UNCERTAINTY_MEASURE_WITH_UNIT (LENGTH_MEASURE( 1.000000000000000082E-05 ), #10078, 'distance_accuracy_value', 'NONE');
#14556=FACE_OUTER_BOUND ( 'NONE', #14883, .T. ) ;
#14560=DIRECTION ( 'NONE',  ( -1.000000000000000000, 0.000000000000000000, -0.000000000000000000 ) ) ;
#14561=EDGE_CURVE ( 'NONE', #5438, #13461, #1056, .T. ) ;
#14563=VERTEX_POINT ( 'NONE', #2067 ) ;
#14570=EDGE_CURVE ( 'NONE', #14980, #14624, #8519, .T. ) ;
#14573=DIRECTION ( 'NONE',  ( 1.000000000000000000, -0.000000000000000000, -0.000000000000000000 ) ) ;
#14577=DIRECTION ( 'NONE',  ( -1.000000000000000000, 0.000000000000000000, 0.000000000000000000 ) ) ;
#14581=ORIENTED_EDGE ( 'NONE', *, *, #376, .F. ) ;
#14582=CARTESIAN_POINT ( 'NONE',  ( 0.07181525480391401373, -21.92234060054336098, -12.74223776959224708 ) ) ;
#14584=CARTESIAN_POINT ( 'NONE',  ( 2.718184767880468922, -23.19431517146925970, -10.24584646439563507 ) ) ;
#14585=CARTESIAN_POINT ( 'NONE',  ( 2.765633920072235963, -5.391175441198450713, -24.15498966839968276 ) ) ;
#14590=CARTESIAN_POINT ( 'NONE',  ( 0.1882238552569854284, -10.68696068830390900, -23.64332819722392287 ) ) ;
#14591=ORIENTED_EDGE ( 'NONE', *, *, #9566, .T. ) ;
#14595=EDGE_LOOP ( 'NONE', ( #8365, #10154, #7306, #9833, #2280, #2478 ) ) ;
#14603=CARTESIAN_POINT ( 'NONE',  ( 2.789999999999999147, -16.37294372382871188, 18.55949924794887096 ) ) ;
#14605=CARTESIAN_POINT ( 'NONE',  ( 2.789999999999999147, -19.64056340710884996, 14.55412442567610931 ) ) ;
#14608=AXIS2_PLACEMENT_3D ( 'NONE', #12644, #10420, #13878 ) ;
#14609=AXIS2_PLACEMENT_3D ( 'NONE', #2090, #13928, #6782 ) ;
#14610=AXIS2_PLACEMENT_3D ( 'NONE', #13364, #13224, #7464 ) ;
#14611=CYLINDRICAL_SURFACE ( 'NONE', #11282, 2.524999999999995914 ) ;
#14613=EDGE_CURVE ( 'NONE', #1296, #6140, #11461, .T. ) ;
#14615=B_SPLINE_CURVE_WITH_KNOTS ( 'NONE', 3,
 ( #1848, #12529, #5622, #10145 ),
 .UNSPECIFIED., .F., .F.,
 ( 4, 4 ),
 ( 0.005258214619651957987, 0.005948481662034167325 ),
 .UNSPECIFIED. ) ;
#14616=CARTESIAN_POINT ( 'NONE',  ( -8.051804217113518143E-16, 5.456805104201102985, 23.69843731927169728 ) ) ;
#14618=EDGE_CURVE ( 'NONE', #8930, #9372, #10045, .T. ) ;
#14624=VERTEX_POINT ( 'NONE', #7914 ) ;
#14632=ORIENTED_EDGE ( 'NONE', *, *, #14408, .F. ) ;
#14637=CARTESIAN_POINT ( 'NONE',  ( 1.039999999999997371, 25.12109765559653596, 12.52377138324232675 ) ) ;
#14638=DIRECTION ( 'NONE',  ( 0.000000000000000000, 0.000000000000000000, 1.000000000000000000 ) ) ;
#14640=CARTESIAN_POINT ( 'NONE',  ( 0.02436607992776064838, 12.59161484032912171, 21.30679549418635688 ) ) ;
#14641=CIRCLE ( 'NONE', #3835, 2.524999999999995914 ) ;
#14643=B_SPLINE_CURVE_WITH_KNOTS ( 'NONE', 3,
 ( #7676, #11287, #9064, #8976 ),
 .UNSPECIFIED., .F., .F.,
 ( 4, 4 ),
 ( 1.981826382900813409E-07, 0.0006887856082032216450 ),
 .UNSPECIFIED. ) ;
#14644=ORIENTED_EDGE ( 'NONE', *, *, #11818, .T. ) ;
#14645=ORIENTED_EDGE ( 'NONE', *, *, #1290, .T. ) ;
#14646=LINE ( 'NONE', #13838, #1172 ) ;
#14647=DIRECTION ( 'NONE',  ( 0.000000000000000000, 1.374038396813314756E-15, -1.000000000000000000 ) ) ;
#14648=EDGE_CURVE ( 'NONE', #12150, #6879, #9743, .T. ) ;
#14655=CARTESIAN_POINT ( 'NONE',  ( 0.1855655959470679794, 19.17825124759777822, 17.45907811351462158 ) ) ;
#14665=CARTESIAN_POINT ( 'NONE',  ( 0.07181525068722571792, -25.22524549359951962, 2.576941577947320372 ) ) ;
#14666=CARTESIAN_POINT ( 'NONE',  ( 0.5279272304333949561, 11.57956866523252870, -24.43806413951663004 ) ) ;
#14669=LINE ( 'NONE', #3052, #9204 ) ;
#14671=CARTESIAN_POINT ( 'NONE',  ( 2.789999999999999147, 7.909232158575156824, -24.34211360614291664 ) ) ;
#14678=CARTESIAN_POINT ( 'NONE',  ( 2.631259771887293653, -22.38003579136350396, 12.81821841996065636 ) ) ;
#14681=AXIS2_PLACEMENT_3D ( 'NONE', #1672, #12269, #2677 ) ;
#14686=ORIENTED_EDGE ( 'NONE', *, *, #7651, .F. ) ;
#14689=DIRECTION ( 'NONE',  ( 0.000000000000000000, 0.3090169943749544457, -0.9510565162951513107 ) ) ;
#14690=CARTESIAN_POINT ( 'NONE',  ( 2.257825462012207129, -12.96514671151749631, -23.74442027961374890 ) ) ;
#14698=VECTOR ( 'NONE', #5227, 1000.000000000000000 ) ;
#14699=VECTOR ( 'NONE', #5739, 1000.000000000000000 ) ;
#14701=ORIENTED_EDGE ( 'NONE', *, *, #11826, .T. ) ;
#14705=ORIENTED_EDGE ( 'NONE', *, *, #8488, .F. ) ;
#14708=( NAMED_UNIT ( * ) SI_UNIT ( $, .STERADIAN. ) SOLID_ANGLE_UNIT ( ) );
#14716=ORIENTED_EDGE ( 'NONE', *, *, #7270, .F. ) ;
#14719=VECTOR ( 'NONE', #7189, 1000.000000000000000 ) ;
#14720=CARTESIAN_POINT ( 'NONE',  ( 2.789999999999999147, 21.30679549418631780, 12.59161484032919986 ) ) ;
#14725=ORIENTED_EDGE ( 'NONE', *, *, #2318, .F. ) ;
#14727=CARTESIAN_POINT ( 'NONE',  ( 0.02436607992776758727, 24.15498966839963302, 5.391175441198700291 ) ) ;
#14728=VECTOR ( 'NONE', #2845, 1000.000000000000000 ) ;
#14729=EDGE_CURVE ( 'NONE', #1373, #383, #4850, .T. ) ;
#14730=FACE_OUTER_BOUND ( 'NONE', #13638, .T. ) ;
#14733=FACE_OUTER_BOUND ( 'NONE', #11894, .T. ) ;
#14735=CARTESIAN_POINT ( 'NONE',  ( 0.07186811453410731076, 16.91241718342026346, -18.89333555428536826 ) ) ;
#14737=ORIENTED_EDGE ( 'NONE', *, *, #14561, .F. ) ;
#14740=EDGE_CURVE ( 'NONE', #3394, #495, #6132, .T. ) ;
#14746=CARTESIAN_POINT ( 'NONE',  ( 2.765633920072235963, -24.63872515616080960, -2.336989772644527008 ) ) ;
#14748=DIRECTION ( 'NONE',  ( 0.000000000000000000, 0.000000000000000000, 1.000000000000000000 ) ) ;
#14749=CARTESIAN_POINT ( 'NONE',  ( 2.789999999999999147, -15.74360496233368245, -18.28042085475295409 ) ) ;
#14755=DIRECTION ( 'NONE',  ( -1.000000000000000000, -0.000000000000000000, -0.000000000000000000 ) ) ;
#14772=CARTESIAN_POINT ( 'NONE',  ( 2.789999999999999147, 5.391175441198956086, -24.15498966839956907 ) ) ;
#14776=EDGE_LOOP ( 'NONE', ( #12904, #1026, #8593, #10339, #925, #3583 ) ) ;
#14777=FACE_OUTER_BOUND ( 'NONE', #12978, .T. ) ;
#14785=DIRECTION ( 'NONE',  ( 0.000000000000000000, 0.000000000000000000, 1.000000000000000000 ) ) ;
#14786=AXIS2_PLACEMENT_3D ( 'NONE', #2984, #10349, #7747 ) ;
#14787=CARTESIAN_POINT ( 'NONE',  ( 0.6180618139040615633, -23.93436800624301242, 12.96259772325168314 ) ) ;
#14793=VERTEX_POINT ( 'NONE', #10660 ) ;
#14794=CARTESIAN_POINT ( 'NONE',  ( 2.765633920072235075, 24.63872515616082737, -2.336989772644355590 ) ) ;
#14798=ORIENTED_EDGE ( 'NONE', *, *, #6108, .F. ) ;
#14801=CARTESIAN_POINT ( 'NONE',  ( 1.039999999999995595, 20.02152543075345648, 19.67366047555537278 ) ) ;
#14809=EDGE_CURVE ( 'NONE', #2825, #8456, #12043, .T. ) ;
#14811=B_SPLINE_CURVE_WITH_KNOTS ( 'NONE', 3,
 ( #4076, #7615, #14690, #4159, #10907, #12291 ),
 .UNSPECIFIED., .F., .F.,
 ( 4, 2, 4 ),
 ( 4.462636695616422376E-07, 0.001879885036799763083, 0.003759323809929964420 ),
 .UNSPECIFIED. ) ;
#14815=DIRECTION ( 'NONE',  ( -1.000000000000000000, 0.000000000000000000, 0.000000000000000000 ) ) ;
#14817=CARTESIAN_POINT ( 'NONE',  ( 2.783068930044319877, -16.17493693894864393, -18.43696893154776006 ) ) ;
#14820=EDGE_CURVE ( 'NONE', #2289, #6867, #12456, .T. ) ;
#14821=VERTEX_POINT ( 'NONE', #7595 ) ;
#14824=CARTESIAN_POINT ( 'NONE',  ( 2.789999999999999147, 24.34211360614300190, 7.909232158574900140 ) ) ;
#14827=DIRECTION ( 'NONE',  ( 0.000000000000000000, 0.000000000000000000, 1.000000000000000000 ) ) ;
#14828=ORIENTED_EDGE ( 'NONE', *, *, #14233, .F. ) ;
#14830=CARTESIAN_POINT ( 'NONE',  ( 1.749999999999998002, 0.000000000000000000, 0.000000000000000000 ) ) ;
#14834=CARTESIAN_POINT ( 'NONE',  ( -10.00000000000000000, 0.000000000000000000, 0.000000000000000000 ) ) ;
#14836=B_SPLINE_CURVE_WITH_KNOTS ( 'NONE', 3,
 ( #10945, #8486, #13257, #3889 ),
 .UNSPECIFIED., .F., .F.,
 ( 4, 4 ),
 ( 0.005258110598983608240, 0.005948376585272727862 ),
 .UNSPECIFIED. ) ;
#14840=ORIENTED_EDGE ( 'NONE', *, *, #5456, .F. ) ;
#14843=AXIS2_PLACEMENT_3D ( 'NONE', #847, #4628, #8077 ) ;
#14847=EDGE_CURVE ( 'NONE', #11410, #8704, #7487, .T. ) ;
#14851=CARTESIAN_POINT ( 'NONE',  ( 2.718184749312774873, 25.22524549359950541, 2.576941577947493567 ) ) ;
#14857=EDGE_LOOP ( 'NONE', ( #2965, #9140, #64, #7223 ) ) ;
#14860=CARTESIAN_POINT ( 'NONE',  ( 2.790000000000000036, -23.69843731927165109, -5.456805104201351675 ) ) ;
#14861=CARTESIAN_POINT ( 'NONE',  ( 1.039999999999997593, 0.000000000000000000, 0.000000000000000000 ) ) ;
#14862=AXIS2_PLACEMENT_3D ( 'NONE', #7474, #4249, #8924 ) ;
#14863=CARTESIAN_POINT ( 'NONE',  ( 0.06562551705663710599, -21.84204283372370625, 12.72258903105631234 ) ) ;
#14864=ORIENTED_EDGE ( 'NONE', *, *, #9318, .F. ) ;
#14871=CARTESIAN_POINT ( 'NONE',  ( 0.000000000000000000, 0.000000000000000000, 0.000000000000000000 ) ) ;
#14876=DIRECTION ( 'NONE',  ( 0.000000000000000000, 0.000000000000000000, 1.000000000000000000 ) ) ;
#14877=DIRECTION ( 'NONE',  ( -1.000000000000000000, 0.000000000000000000, 0.000000000000000000 ) ) ;
#14878=ORIENTED_EDGE ( 'NONE', *, *, #1816, .T. ) ;
#14880=DIRECTION ( 'NONE',  ( -1.000000000000000000, 0.000000000000000000, 0.000000000000000000 ) ) ;
#14883=EDGE_LOOP ( 'NONE', ( #302, #5835, #5004, #5385, #1628, #806, #3840 ) ) ;
#14884=CARTESIAN_POINT ( 'NONE',  ( 0.000000000000000000, -24.04302995059967429, 1.991882183130232242 ) ) ;
#14885=CARTESIAN_POINT ( 'NONE',  ( -10.00000000000000000, 0.000000000000000000, 0.000000000000000000 ) ) ;
#14899=CARTESIAN_POINT ( 'NONE',  ( 1.039999999999997593, 0.000000000000000000, 0.000000000000000000 ) ) ;
#14907=CARTESIAN_POINT ( 'NONE',  ( 2.789999999999999147, -20.62201879784921843, 12.52067188844344336 ) ) ;
#14908=ORIENTED_EDGE ( 'NONE', *, *, #8873, .T. ) ;
#14912=CARTESIAN_POINT ( 'NONE',  ( 2.031033471609898555, 27.31260702007175567, -3.797536611356413516 ) ) ;
#14918=AXIS2_PLACEMENT_3D ( 'NONE', #6349, #13414, #13794 ) ;
#14920=CARTESIAN_POINT ( 'NONE',  ( 2.632969638839692372, 22.37100459959346566, 12.81671916049022641 ) ) ;
#14921=ORIENTED_EDGE ( 'NONE', *, *, #14740, .F. ) ;
#14922=DIRECTION ( 'NONE',  ( -1.000000000000000000, -0.000000000000000000, -0.000000000000000000 ) ) ;
#14929=AXIS2_PLACEMENT_3D ( 'NONE', #4973, #11859, #5208 ) ;
#14930=EDGE_CURVE ( 'NONE', #7234, #3861, #1818, .T. ) ;
#14932=ORIENTED_EDGE ( 'NONE', *, *, #8353, .F. ) ;
#14933=VERTEX_POINT ( 'NONE', #5151 ) ;
#14934=CARTESIAN_POINT ( 'NONE',  ( 1.749999999999998002, 27.76164181293051669, 4.147968289691386090 ) ) ;
#14937=ADVANCED_FACE ( 'NONE', ( #6429 ), #6508, .T. ) ;
#14939=CARTESIAN_POINT ( 'NONE',  ( 0.006931111373678406143, -9.685942809247212182, 22.53293026234500473 ) ) ;
#14948=CARTESIAN_POINT ( 'NONE',  ( 0.3599332783571699279, -23.15620303736534069, 12.90954937922492007 ) ) ;
#14949=EDGE_CURVE ( 'NONE', #12521, #5940, #8031, .T. ) ;
#14951=AXIS2_PLACEMENT_3D ( 'NONE', #11330, #10106, #10261 ) ;
#14952=VERTEX_POINT ( 'NONE', #7896 ) ;
#14955=EDGE_CURVE ( 'NONE', #11975, #13815, #7301, .T. ) ;
#14956=ORIENTED_EDGE ( 'NONE', *, *, #11158, .T. ) ;
#14961=DIRECTION ( 'NONE',  ( 0.000000000000000000, 0.000000000000000000, 1.000000000000000000 ) ) ;
#14962=AXIS2_PLACEMENT_3D ( 'NONE', #8268, #12950, #2439 ) ;
#14965=CARTESIAN_POINT ( 'NONE',  ( 0.5279272933715194460, 19.66369668717032937, 18.56460150496945971 ) ) ;
#14966=DIRECTION ( 'NONE',  ( 1.000000000000000000, 0.000000000000000000, 0.000000000000000000 ) ) ;
#14968=CARTESIAN_POINT ( 'NONE',  ( 0.02436607992776411782, -24.63872515616084513, 2.336989772644183283 ) ) ;
#14970=ORIENTED_EDGE ( 'NONE', *, *, #7629, .T. ) ;
#14971=VERTEX_POINT ( 'NONE', #3050 ) ;
#14976=DIRECTION ( 'NONE',  ( 0.000000000000000000, 0.000000000000000000, 1.000000000000000000 ) ) ;
#14978=DIRECTION ( 'NONE',  ( -1.000000000000000000, -0.000000000000000000, 0.000000000000000000 ) ) ;
#14979=CARTESIAN_POINT ( 'NONE',  ( -10.00000000000000000, 0.000000000000000000, 0.000000000000000000 ) ) ;
#14980=VERTEX_POINT ( 'NONE', #3137 ) ;
#14982=FACE_OUTER_BOUND ( 'NONE', #15065, .T. ) ;
#14984=AXIS2_PLACEMENT_3D ( 'NONE', #2524, #7208, #4760 ) ;
#14986=ORIENTED_EDGE ( 'NONE', *, *, #14648, .F. ) ;
#14993=CARTESIAN_POINT ( 'NONE',  ( 1.749999999999998002, 27.76164181293051669, -4.147968289691384314 ) ) ;
#14995=CARTESIAN_POINT ( 'NONE',  ( 2.765633920072234631, 16.37294372382885044, -18.55949924794875017 ) ) ;
#15001=CARTESIAN_POINT ( 'NONE',  ( 1.039999999999997593, 0.000000000000000000, 0.000000000000000000 ) ) ;
#15003=DIRECTION ( 'NONE',  ( 0.000000000000000000, 0.000000000000000000, 1.000000000000000000 ) ) ;
#15005=VERTEX_POINT ( 'NONE', #12508 ) ;
#15011=DIRECTION ( 'NONE',  ( -1.000000000000000000, 0.000000000000000000, 0.000000000000000000 ) ) ;
#15015=CARTESIAN_POINT ( 'NONE',  ( 0.5321745227542316048, 19.66801664102731095, -18.57583492944399950 ) ) ;
#15018=LINE ( 'NONE', #8784, #6934 ) ;
#15020=DIRECTION ( 'NONE',  ( 0.000000000000000000, 1.000000000000000000, 1.099230717450651647E-14 ) ) ;
#15024=DIRECTION ( 'NONE',  ( -1.000000000000000000, -0.000000000000000000, 0.000000000000000000 ) ) ;
#15033=VERTEX_POINT ( 'NONE', #8042 ) ;
#15034=CARTESIAN_POINT ( 'NONE',  ( 2.765633920072237295, 12.59161484032912171, 21.30679549418635688 ) ) ;
#15035=ORIENTED_EDGE ( 'NONE', *, *, #9017, .T. ) ;
#15037=EDGE_CURVE ( 'NONE', #11822, #269, #7101, .T. ) ;
#15038=TOROIDAL_SURFACE ( 'NONE', #1040, 24.12539914357697413, 8.000000000000000000 ) ;
#15041=DIRECTION ( 'NONE',  ( 0.000000000000000000, 0.000000000000000000, 1.000000000000000000 ) ) ;
#15050=FACE_OUTER_BOUND ( 'NONE', #3043, .T. ) ;
#15053=DIRECTION ( 'NONE',  ( -1.000000000000000000, -0.000000000000000000, -0.000000000000000000 ) ) ;
#15057=CARTESIAN_POINT ( 'NONE',  ( 2.604434514863827488, -23.63475234378990208, 10.67816411292155543 ) ) ;
#15062=CARTESIAN_POINT ( 'NONE',  ( 2.789999999999999147, 0.000000000000000000, 0.000000000000000000 ) ) ;
#15064=CARTESIAN_POINT ( 'NONE',  ( 1.039999999999995595, 20.02152543075345648, 19.67366047555537278 ) ) ;
#15065=EDGE_LOOP ( 'NONE', ( #12461, #8791, #14435, #5441 ) ) ;
#15069=ORIENTED_EDGE ( 'NONE', *, *, #5514, .T. ) ;
#15073=VERTEX_POINT ( 'NONE', #9123 ) ;
#15075=CARTESIAN_POINT ( 'NONE',  ( 0.000000000000000000, 0.000000000000000000, 0.000000000000000000 ) ) ;
#15077=DIRECTION ( 'NONE',  ( -0.000000000000000000, 0.000000000000000000, 1.000000000000000000 ) ) ;
#15078=CARTESIAN_POINT ( 'NONE',  ( 1.894355403937850069, -24.59653223688283674, 12.96989951879399072 ) ) ;
#15080=UNCERTAINTY_MEASURE_WITH_UNIT (LENGTH_MEASURE( 1.000000000000000082E-05 ), #11232, 'distance_accuracy_value', 'NONE');
#15083=EDGE_CURVE ( 'NONE', #4155, #5857, #9277, .T. ) ;
#15084=VERTEX_POINT ( 'NONE', #13012 ) ;
#15085=TOROIDAL_SURFACE ( 'NONE', #7469, 24.12539914357697768, 8.000000000000000000 ) ;
#15086=CARTESIAN_POINT ( 'NONE',  ( 8.000000000000000000, 0.000000000000000000, 0.000000000000000000 ) ) ;
#15092=DIRECTION ( 'NONE',  ( -1.000000000000000000, -0.000000000000000000, 0.000000000000000000 ) ) ;
#15093=CARTESIAN_POINT ( 'NONE',  ( 1.394999999999999574, 4.147968289691286614, 27.76164181293053090 ) ) ;
#15094=ORIENTED_EDGE ( 'NONE', *, *, #1057, .T. ) ;
#15096=EDGE_CURVE ( 'NONE', #5438, #626, #94, .T. ) ;
#15098=CARTESIAN_POINT ( 'NONE',  ( 2.789999999999999147, 20.70663861606293210, -15.04425356660737556 ) ) ;
#15102=STYLED_ITEM('',(#15265),#8904);
#15111=AXIS2_PLACEMENT_3D ( 'NONE', #8101, #10705, #1180 ) ;
#15112=EDGE_CURVE ( 'NONE', #7568, #14980, #4518, .T. ) ;
#15116=CARTESIAN_POINT ( 'NONE',  ( 0.02436607992776455150, 21.30679549418631780, 12.59161484032919986 ) ) ;
#15118=EDGE_CURVE ( 'NONE', #6121, #15033, #1415, .T. ) ;
#15121=CYLINDRICAL_SURFACE ( 'NONE', #12870, 13.19999999999999929 ) ;
#15122=CARTESIAN_POINT ( 'NONE',  ( 1.749999999999998002, -19.67366047555515252, -20.02152543075368030 ) ) ;
#15125=AXIS2_PLACEMENT_3D ( 'NONE', #3099, #10086, #3017 ) ;
#15126=ORIENTED_EDGE ( 'NONE', *, *, #4556, .T. ) ;
#15130=CARTESIAN_POINT ( 'NONE',  ( 5.566640002541124371E-16, 15.96500990068152426, -18.34424029220094354 ) ) ;
#15132=CARTESIAN_POINT ( 'NONE',  ( 2.783068945535914551, -24.42321038836784197, 2.248820353272884542 ) ) ;
#15139=CARTESIAN_POINT ( 'NONE',  ( 2.604434325169353581, 25.77772010606605946, -2.851997810081738027 ) ) ;
#15144=FACE_OUTER_BOUND ( 'NONE', #9726, .T. ) ;
#15145=CARTESIAN_POINT ( 'NONE',  ( 0.000000000000000000, -18.28042085475266632, -15.74360496233403239 ) ) ;
#15148=ORIENTED_EDGE ( 'NONE', *, *, #12374, .F. ) ;
#15155=AXIS2_PLACEMENT_3D ( 'NONE', #4747, #6045, #2508 ) ;
#15157=ORIENTED_EDGE ( 'NONE', *, *, #4570, .F. ) ;
#15164=DIRECTION ( 'NONE',  ( -1.000000000000000000, -0.000000000000000000, -0.000000000000000000 ) ) ;
#15165=ADVANCED_FACE ( 'NONE', ( #10504 ), #7266, .T. ) ;
#15170=VECTOR ( 'NONE', #12216, 1000.000000000000000 ) ;
#15171=DIRECTION ( 'NONE',  ( -1.000000000000000000, -0.000000000000000000, -0.000000000000000000 ) ) ;
#15173=CARTESIAN_POINT ( 'NONE',  ( 2.789999999999999147, 20.62201879784912606, 12.52067188844359080 ) ) ;
#15175=AXIS2_PLACEMENT_3D ( 'NONE', #6663, #4358, #5667 ) ;
#15183=ORIENTED_EDGE ( 'NONE', *, *, #8488, .T. ) ;
#15184=TOROIDAL_SURFACE ( 'NONE', #7071, 24.12539914357697768, 8.000000000000000000 ) ;
#15187=FACE_OUTER_BOUND ( 'NONE', #5990, .T. ) ;
#15189=DIRECTION ( 'NONE',  ( -1.000000000000000000, 0.000000000000000000, -0.000000000000000000 ) ) ;
#15196=DIRECTION ( 'NONE',  ( -1.000000000000000000, -0.000000000000000000, -0.000000000000000000 ) ) ;
#15200=CARTESIAN_POINT ( 'NONE',  ( 0.000000000000000000, -24.04302995059965653, -1.991882183130557094 ) ) ;
#15202=DIRECTION ( 'NONE',  ( 0.000000000000000000, 0.000000000000000000, 1.000000000000000000 ) ) ;
#15203=CARTESIAN_POINT ( 'NONE',  ( 1.749999999999998002, 19.67366047555558950, -20.02152543075324687 ) ) ;
#15206=VECTOR ( 'NONE', #15189, 1000.000000000000000 ) ;
#15209=ORIENTED_EDGE ( 'NONE', *, *, #14930, .T. ) ;
#15213=FACE_OUTER_BOUND ( 'NONE', #13154, .T. ) ;
#15215=EDGE_CURVE ( 'NONE', #9774, #7336, #13685, .T. ) ;
#15218=VERTEX_POINT ( 'NONE', #8259 ) ;
#15221=FACE_OUTER_BOUND ( 'NONE', #1761, .T. ) ;
#15259=COLOUR_RGB('Sky Blue',0.24,0.69,0.87);
#15260=FILL_AREA_STYLE_COLOUR('',#15259);
#15261=FILL_AREA_STYLE('',(#15260));
#15262=SURFACE_STYLE_FILL_AREA(#15261);
#15263=SURFACE_SIDE_STYLE('',(#15262));
#15264=SURFACE_STYLE_USAGE(.BOTH.,#15263);
#15265=PRESENTATION_STYLE_ASSIGNMENT((#15264));
ENDSEC;
END-ISO-10303-21;
